ISO-10303-21;
HEADER;
/* Generated by software containing ST-Developer
 * from STEP Tools, Inc. (www.steptools.com) 
 */

FILE_DESCRIPTION(
/* description */ ('Independent maintained push-to-latch/pull-to-reset mushroom-operator 
CAD. Two opposed spring-loaded ball detents in turned circular seats b
ias both travel stops; direct normally-closed bridge opens6mm when pre
ssed. Rounded palm/pull rim, captured head screw, removable detent clo
sures, native Coil spring families, insulated shared terminals and ord
inary machining features. Manual geometric states and ideal same-mater
ial spring-energy direction only; no electrical/safety certification, 
force/contact dynamics, wear, load or life rating. Requested blue/gray
 visual palette, not safety identification. External wiring/anchors an
d application engineering omitted.'),
/* implementation_level */ '2;1');

FILE_NAME(
/* name */ 'Socket head cap screw M3x10.step',
/* time_stamp */ '2026-11-08T17:54:26-08:00',
/* author */ (''),
/* organization */ (''),
/* preprocessor_version */ 'ST-DEVELOPER v20.2',
/* originating_system */ 'Autodesk Translation Framework v15.17.0.0',
/* authorisation */ '');

FILE_SCHEMA (('AUTOMOTIVE_DESIGN { 1 0 10303 214 3 1 1 }'));
ENDSEC;

DATA;
#10=MECHANICAL_DESIGN_GEOMETRIC_PRESENTATION_REPRESENTATION('',(#205),#43980);
#149=CONICAL_SURFACE('',#12188,0.1,0.785398163397448);
#171=SHAPE_REPRESENTATION_RELATIONSHIP('SRR','None',#44071,#188);
#188=ADVANCED_BREP_SHAPE_REPRESENTATION('',(#222),#43978);
#205=STYLED_ITEM('',(#44160),#222);
#222=MANIFOLD_SOLID_BREP('Body1',#11246);
#254=B_SPLINE_SURFACE_WITH_KNOTS('',3,3,((#41937,#41938,#41939,#41940,#41941,
#41942,#41943,#41944,#41945,#41946,#41947,#41948,#41949,#41950,#41951,#41952,
#41953,#41954,#41955,#41956,#41957,#41958,#41959,#41960,#41961,#41962,#41963,
#41964,#41965,#41966,#41967,#41968,#41969,#41970,#41971,#41972,#41973,#41974,
#41975,#41976,#41977,#41978,#41979,#41980,#41981,#41982,#41983,#41984,#41985,
#41986,#41987,#41988,#41989,#41990,#41991,#41992,#41993,#41994,#41995,#41996,
#41997,#41998,#41999,#42000,#42001,#42002,#42003,#42004,#42005,#42006,#42007,
#42008,#42009,#42010,#42011,#42012,#42013,#42014,#42015,#42016,#42017,#42018,
#42019,#42020,#42021,#42022,#42023,#42024,#42025,#42026,#42027,#42028,#42029,
#42030,#42031,#42032,#42033,#42034,#42035,#42036,#42037,#42038,#42039,#42040,
#42041,#42042,#42043,#42044,#42045,#42046,#42047,#42048,#42049,#42050,#42051,
#42052,#42053,#42054,#42055,#42056,#42057),(#42058,#42059,#42060,#42061,
#42062,#42063,#42064,#42065,#42066,#42067,#42068,#42069,#42070,#42071,#42072,
#42073,#42074,#42075,#42076,#42077,#42078,#42079,#42080,#42081,#42082,#42083,
#42084,#42085,#42086,#42087,#42088,#42089,#42090,#42091,#42092,#42093,#42094,
#42095,#42096,#42097,#42098,#42099,#42100,#42101,#42102,#42103,#42104,#42105,
#42106,#42107,#42108,#42109,#42110,#42111,#42112,#42113,#42114,#42115,#42116,
#42117,#42118,#42119,#42120,#42121,#42122,#42123,#42124,#42125,#42126,#42127,
#42128,#42129,#42130,#42131,#42132,#42133,#42134,#42135,#42136,#42137,#42138,
#42139,#42140,#42141,#42142,#42143,#42144,#42145,#42146,#42147,#42148,#42149,
#42150,#42151,#42152,#42153,#42154,#42155,#42156,#42157,#42158,#42159,#42160,
#42161,#42162,#42163,#42164,#42165,#42166,#42167,#42168,#42169,#42170,#42171,
#42172,#42173,#42174,#42175,#42176,#42177,#42178),(#42179,#42180,#42181,
#42182,#42183,#42184,#42185,#42186,#42187,#42188,#42189,#42190,#42191,#42192,
#42193,#42194,#42195,#42196,#42197,#42198,#42199,#42200,#42201,#42202,#42203,
#42204,#42205,#42206,#42207,#42208,#42209,#42210,#42211,#42212,#42213,#42214,
#42215,#42216,#42217,#42218,#42219,#42220,#42221,#42222,#42223,#42224,#42225,
#42226,#42227,#42228,#42229,#42230,#42231,#42232,#42233,#42234,#42235,#42236,
#42237,#42238,#42239,#42240,#42241,#42242,#42243,#42244,#42245,#42246,#42247,
#42248,#42249,#42250,#42251,#42252,#42253,#42254,#42255,#42256,#42257,#42258,
#42259,#42260,#42261,#42262,#42263,#42264,#42265,#42266,#42267,#42268,#42269,
#42270,#42271,#42272,#42273,#42274,#42275,#42276,#42277,#42278,#42279,#42280,
#42281,#42282,#42283,#42284,#42285,#42286,#42287,#42288,#42289,#42290,#42291,
#42292,#42293,#42294,#42295,#42296,#42297,#42298,#42299),(#42300,#42301,
#42302,#42303,#42304,#42305,#42306,#42307,#42308,#42309,#42310,#42311,#42312,
#42313,#42314,#42315,#42316,#42317,#42318,#42319,#42320,#42321,#42322,#42323,
#42324,#42325,#42326,#42327,#42328,#42329,#42330,#42331,#42332,#42333,#42334,
#42335,#42336,#42337,#42338,#42339,#42340,#42341,#42342,#42343,#42344,#42345,
#42346,#42347,#42348,#42349,#42350,#42351,#42352,#42353,#42354,#42355,#42356,
#42357,#42358,#42359,#42360,#42361,#42362,#42363,#42364,#42365,#42366,#42367,
#42368,#42369,#42370,#42371,#42372,#42373,#42374,#42375,#42376,#42377,#42378,
#42379,#42380,#42381,#42382,#42383,#42384,#42385,#42386,#42387,#42388,#42389,
#42390,#42391,#42392,#42393,#42394,#42395,#42396,#42397,#42398,#42399,#42400,
#42401,#42402,#42403,#42404,#42405,#42406,#42407,#42408,#42409,#42410,#42411,
#42412,#42413,#42414,#42415,#42416,#42417,#42418,#42419,#42420)),
 .UNSPECIFIED.,.F.,.F.,.F.,(4,4),(4,1,1,1,1,1,1,1,1,1,1,1,1,1,1,1,1,1,1,
1,1,1,1,1,1,1,1,1,1,1,1,1,1,1,1,1,1,1,1,1,1,1,1,1,1,1,1,1,1,1,1,1,1,1,1,
1,1,1,1,1,1,1,1,1,1,1,1,1,1,1,1,1,1,1,1,1,1,1,1,1,1,1,1,1,1,1,1,1,1,1,1,
1,1,1,1,1,1,1,1,1,1,1,1,1,1,1,1,1,1,1,1,1,1,1,1,1,1,1,4),(0.,0.0329955678841871),
(11.6159397475003,12.6087096497013,13.6014795519022,14.5942494541031,15.5870193563041,
16.579789258505,17.5725591607059,18.5653290629068,19.5580989651078,20.5508688673087,
21.5436387695096,22.5364086717106,23.5291785739115,24.5219484761124,25.5147183783134,
26.5074882805143,27.5002581827152,28.4930280849161,29.4857979871171,30.478567889318,
31.4713377915189,32.4641076937199,33.4568775959208,34.4496474981217,35.4424174003227,
36.4351873025236,37.4279572047245,38.4207271069255,39.4134970091264,40.4062669113273,
41.3990368135282,42.3918067157292,43.3845766179301,44.377346520131,45.370116422332,
46.3628863245329,47.3556562267338,48.3484261289348,49.3411960311357,50.3339659333366,
51.3267358355376,52.3195057377385,53.3122756399394,54.3050455421403,55.2978154443413,
56.2905853465422,57.2833552487431,58.2761251509441,59.268895053145,60.2616649553459,
61.2544348575469,62.2472047597478,63.2399746619487,64.2327445641497,65.2255144663506,
66.2182843685515,67.2110542707524,68.2038241729534,69.1965940751543,70.1893639773552,
71.1821338795562,72.1749037817571,73.167673683958,74.160443586159,75.1532134883599,
76.1459833905608,77.1387532927618,78.1315231949627,79.1242930971636,80.1170629993645,
81.1098329015655,82.1026028037664,83.0953727059673,84.0881426081683,85.0809125103692,
86.0736824125701,87.0664523147711,88.059222216972,89.0519921191729,90.0447620213739,
91.0375319235748,92.0303018257757,93.0230717279766,94.0158416301776,95.0086115323785,
96.0013814345794,96.9941513367804,97.9869212389813,98.9796911411822,99.9724610433832,
100.965230945584,101.958000847785,102.950770749986,103.943540652187,104.936310554388,
105.929080456589,106.92185035879,107.914620260991,108.907390163192,109.900160065392,
110.892929967593,111.885699869794,112.878469771995,113.871239674196,114.864009576397,
115.856779478598,116.849549380799,117.842319283,118.835089185201,119.827859087402,
120.820628989603,121.813398891804,122.806168794005,123.798938696205,124.791708598406,
125.784478500607,126.777248402808,127.770018305009,128.76278820721),
 .UNSPECIFIED.);
#255=B_SPLINE_SURFACE_WITH_KNOTS('',3,3,((#42516,#42517,#42518,#42519,#42520,
#42521,#42522,#42523,#42524,#42525,#42526,#42527,#42528,#42529,#42530,#42531,
#42532,#42533,#42534,#42535,#42536,#42537,#42538,#42539,#42540,#42541,#42542,
#42543,#42544,#42545,#42546,#42547,#42548,#42549,#42550,#42551,#42552,#42553,
#42554,#42555,#42556,#42557,#42558,#42559,#42560,#42561,#42562,#42563,#42564,
#42565,#42566,#42567,#42568,#42569,#42570,#42571,#42572,#42573,#42574,#42575,
#42576,#42577,#42578,#42579,#42580,#42581,#42582,#42583,#42584,#42585,#42586,
#42587,#42588,#42589,#42590,#42591,#42592,#42593,#42594,#42595,#42596,#42597,
#42598,#42599,#42600,#42601,#42602,#42603,#42604,#42605,#42606,#42607,#42608,
#42609,#42610,#42611,#42612,#42613,#42614,#42615,#42616,#42617,#42618,#42619,
#42620,#42621,#42622,#42623,#42624,#42625,#42626,#42627,#42628,#42629,#42630,
#42631,#42632,#42633,#42634,#42635,#42636,#42637,#42638),(#42639,#42640,
#42641,#42642,#42643,#42644,#42645,#42646,#42647,#42648,#42649,#42650,#42651,
#42652,#42653,#42654,#42655,#42656,#42657,#42658,#42659,#42660,#42661,#42662,
#42663,#42664,#42665,#42666,#42667,#42668,#42669,#42670,#42671,#42672,#42673,
#42674,#42675,#42676,#42677,#42678,#42679,#42680,#42681,#42682,#42683,#42684,
#42685,#42686,#42687,#42688,#42689,#42690,#42691,#42692,#42693,#42694,#42695,
#42696,#42697,#42698,#42699,#42700,#42701,#42702,#42703,#42704,#42705,#42706,
#42707,#42708,#42709,#42710,#42711,#42712,#42713,#42714,#42715,#42716,#42717,
#42718,#42719,#42720,#42721,#42722,#42723,#42724,#42725,#42726,#42727,#42728,
#42729,#42730,#42731,#42732,#42733,#42734,#42735,#42736,#42737,#42738,#42739,
#42740,#42741,#42742,#42743,#42744,#42745,#42746,#42747,#42748,#42749,#42750,
#42751,#42752,#42753,#42754,#42755,#42756,#42757,#42758,#42759,#42760,#42761),
(#42762,#42763,#42764,#42765,#42766,#42767,#42768,#42769,#42770,#42771,
#42772,#42773,#42774,#42775,#42776,#42777,#42778,#42779,#42780,#42781,#42782,
#42783,#42784,#42785,#42786,#42787,#42788,#42789,#42790,#42791,#42792,#42793,
#42794,#42795,#42796,#42797,#42798,#42799,#42800,#42801,#42802,#42803,#42804,
#42805,#42806,#42807,#42808,#42809,#42810,#42811,#42812,#42813,#42814,#42815,
#42816,#42817,#42818,#42819,#42820,#42821,#42822,#42823,#42824,#42825,#42826,
#42827,#42828,#42829,#42830,#42831,#42832,#42833,#42834,#42835,#42836,#42837,
#42838,#42839,#42840,#42841,#42842,#42843,#42844,#42845,#42846,#42847,#42848,
#42849,#42850,#42851,#42852,#42853,#42854,#42855,#42856,#42857,#42858,#42859,
#42860,#42861,#42862,#42863,#42864,#42865,#42866,#42867,#42868,#42869,#42870,
#42871,#42872,#42873,#42874,#42875,#42876,#42877,#42878,#42879,#42880,#42881,
#42882,#42883,#42884),(#42885,#42886,#42887,#42888,#42889,#42890,#42891,
#42892,#42893,#42894,#42895,#42896,#42897,#42898,#42899,#42900,#42901,#42902,
#42903,#42904,#42905,#42906,#42907,#42908,#42909,#42910,#42911,#42912,#42913,
#42914,#42915,#42916,#42917,#42918,#42919,#42920,#42921,#42922,#42923,#42924,
#42925,#42926,#42927,#42928,#42929,#42930,#42931,#42932,#42933,#42934,#42935,
#42936,#42937,#42938,#42939,#42940,#42941,#42942,#42943,#42944,#42945,#42946,
#42947,#42948,#42949,#42950,#42951,#42952,#42953,#42954,#42955,#42956,#42957,
#42958,#42959,#42960,#42961,#42962,#42963,#42964,#42965,#42966,#42967,#42968,
#42969,#42970,#42971,#42972,#42973,#42974,#42975,#42976,#42977,#42978,#42979,
#42980,#42981,#42982,#42983,#42984,#42985,#42986,#42987,#42988,#42989,#42990,
#42991,#42992,#42993,#42994,#42995,#42996,#42997,#42998,#42999,#43000,#43001,
#43002,#43003,#43004,#43005,#43006,#43007)),.UNSPECIFIED.,.F.,.F.,.F.,(4,
4),(4,1,1,1,1,1,1,1,1,1,1,1,1,1,1,1,1,1,1,1,1,1,1,1,1,1,1,1,1,1,1,1,1,1,
1,1,1,1,1,1,1,1,1,1,1,1,1,1,1,1,1,1,1,1,1,1,1,1,1,1,1,1,1,1,1,1,1,1,1,1,
1,1,1,1,1,1,1,1,1,1,1,1,1,1,1,1,1,1,1,1,1,1,1,1,1,1,1,1,1,1,1,1,1,1,1,1,
1,1,1,1,1,1,1,1,1,1,1,1,1,1,4),(0.,0.0329955678841871),(8.30203615430831,
9.29553633041689,10.2890365065255,11.282536682634,12.2760368587426,13.2695370348512,
14.2630372109598,15.2565373870684,16.2500375631769,17.2435377392855,18.2370379153941,
19.2305380915027,20.2240382676113,21.2175384437198,22.2110386198284,23.204538795937,
24.1980389720456,25.1915391481542,26.1850393242627,27.1785395003713,28.1720396764799,
29.1655398525885,30.1590400286971,31.1525402048056,32.1460403809142,33.1395405570228,
34.1330407331314,35.1265409092399,36.1200410853485,37.1135412614571,38.1070414375657,
39.1005416136743,40.0940417897828,41.0875419658914,42.081042142,43.0745423181086,
44.0680424942172,45.0615426703257,46.0550428464343,47.0485430225429,48.0420431986515,
49.0355433747601,50.0290435508686,51.0225437269772,52.0160439030858,53.0095440791944,
54.003044255303,54.9965444314115,55.9900446075201,56.9835447836287,57.9770449597373,
58.9705451358458,59.9640453119544,60.957545488063,61.9510456641716,62.9445458402802,
63.9380460163887,64.9315461924973,65.9250463686059,66.9185465447145,67.9120467208231,
68.9055468969316,69.8990470730402,70.8925472491488,71.8860474252574,72.879547601366,
73.8730477774745,74.8665479535831,75.8600481296917,76.8535483058003,77.8470484819088,
78.8405486580174,79.834048834126,80.8275490102346,81.8210491863432,82.8145493624517,
83.8080495385603,84.8015497146689,85.7950498907775,86.7885500668861,87.7820502429946,
88.7755504191032,89.7690505952118,90.7625507713204,91.756050947429,92.7495511235375,
93.7430512996461,94.7365514757547,95.7300516518633,96.7235518279718,97.7170520040804,
98.710552180189,99.7040523562976,100.697552532406,101.691052708515,102.684552884623,
103.678053060732,104.67155323684,105.665053412949,106.658553589058,107.652053765166,
108.645553941275,109.639054117383,110.632554293492,111.626054469601,112.619554645709,
113.613054821818,114.606554997926,115.600055174035,116.593555350143,117.587055526252,
118.580555702361,119.574055878469,120.567556054578,121.561056230686,122.554556406795,
123.548056582903,124.541556759012,125.535056935121,126.528557111229,127.522057287338),
 .UNSPECIFIED.);
#327=FACE_BOUND('',#1774,.T.);
#328=FACE_BOUND('',#1777,.T.);
#464=PLANE('',#12194);
#465=PLANE('',#12195);
#466=PLANE('',#12196);
#467=PLANE('',#12197);
#468=PLANE('',#12198);
#469=PLANE('',#12199);
#470=PLANE('',#12200);
#471=PLANE('',#12201);
#472=PLANE('',#12205);
#473=PLANE('',#12206);
#1034=FACE_OUTER_BOUND('',#1725,.T.);
#1035=FACE_OUTER_BOUND('',#1726,.T.);
#1036=FACE_OUTER_BOUND('',#1727,.T.);
#1037=FACE_OUTER_BOUND('',#1728,.T.);
#1038=FACE_OUTER_BOUND('',#1729,.T.);
#1039=FACE_OUTER_BOUND('',#1730,.T.);
#1040=FACE_OUTER_BOUND('',#1731,.T.);
#1041=FACE_OUTER_BOUND('',#1732,.T.);
#1042=FACE_OUTER_BOUND('',#1733,.T.);
#1043=FACE_OUTER_BOUND('',#1734,.T.);
#1044=FACE_OUTER_BOUND('',#1735,.T.);
#1045=FACE_OUTER_BOUND('',#1736,.T.);
#1046=FACE_OUTER_BOUND('',#1737,.T.);
#1047=FACE_OUTER_BOUND('',#1738,.T.);
#1048=FACE_OUTER_BOUND('',#1739,.T.);
#1049=FACE_OUTER_BOUND('',#1740,.T.);
#1050=FACE_OUTER_BOUND('',#1741,.T.);
#1051=FACE_OUTER_BOUND('',#1742,.T.);
#1052=FACE_OUTER_BOUND('',#1743,.T.);
#1053=FACE_OUTER_BOUND('',#1744,.T.);
#1054=FACE_OUTER_BOUND('',#1745,.T.);
#1055=FACE_OUTER_BOUND('',#1746,.T.);
#1056=FACE_OUTER_BOUND('',#1747,.T.);
#1057=FACE_OUTER_BOUND('',#1748,.T.);
#1058=FACE_OUTER_BOUND('',#1749,.T.);
#1059=FACE_OUTER_BOUND('',#1750,.T.);
#1060=FACE_OUTER_BOUND('',#1751,.T.);
#1061=FACE_OUTER_BOUND('',#1752,.T.);
#1062=FACE_OUTER_BOUND('',#1753,.T.);
#1063=FACE_OUTER_BOUND('',#1754,.T.);
#1064=FACE_OUTER_BOUND('',#1755,.T.);
#1065=FACE_OUTER_BOUND('',#1756,.T.);
#1066=FACE_OUTER_BOUND('',#1757,.T.);
#1067=FACE_OUTER_BOUND('',#1758,.T.);
#1068=FACE_OUTER_BOUND('',#1759,.T.);
#1069=FACE_OUTER_BOUND('',#1760,.T.);
#1070=FACE_OUTER_BOUND('',#1761,.T.);
#1071=FACE_OUTER_BOUND('',#1762,.T.);
#1072=FACE_OUTER_BOUND('',#1763,.T.);
#1073=FACE_OUTER_BOUND('',#1764,.T.);
#1074=FACE_OUTER_BOUND('',#1765,.T.);
#1075=FACE_OUTER_BOUND('',#1766,.T.);
#1076=FACE_OUTER_BOUND('',#1767,.T.);
#1077=FACE_OUTER_BOUND('',#1768,.T.);
#1078=FACE_OUTER_BOUND('',#1769,.T.);
#1079=FACE_OUTER_BOUND('',#1770,.T.);
#1080=FACE_OUTER_BOUND('',#1771,.T.);
#1081=FACE_OUTER_BOUND('',#1772,.T.);
#1082=FACE_OUTER_BOUND('',#1773,.T.);
#1083=FACE_OUTER_BOUND('',#1775,.T.);
#1084=FACE_OUTER_BOUND('',#1776,.T.);
#1085=FACE_OUTER_BOUND('',#1778,.T.);
#1725=EDGE_LOOP('',(#9799,#9800,#9801,#9802));
#1726=EDGE_LOOP('',(#9803,#9804,#9805,#9806));
#1727=EDGE_LOOP('',(#9807,#9808,#9809,#9810));
#1728=EDGE_LOOP('',(#9811,#9812,#9813,#9814));
#1729=EDGE_LOOP('',(#9815,#9816,#9817,#9818));
#1730=EDGE_LOOP('',(#9819,#9820,#9821,#9822));
#1731=EDGE_LOOP('',(#9823,#9824,#9825,#9826));
#1732=EDGE_LOOP('',(#9827,#9828,#9829,#9830));
#1733=EDGE_LOOP('',(#9831,#9832,#9833,#9834));
#1734=EDGE_LOOP('',(#9835,#9836,#9837,#9838));
#1735=EDGE_LOOP('',(#9839,#9840,#9841,#9842));
#1736=EDGE_LOOP('',(#9843,#9844,#9845,#9846));
#1737=EDGE_LOOP('',(#9847,#9848,#9849,#9850));
#1738=EDGE_LOOP('',(#9851,#9852,#9853,#9854));
#1739=EDGE_LOOP('',(#9855,#9856,#9857,#9858));
#1740=EDGE_LOOP('',(#9859,#9860,#9861,#9862));
#1741=EDGE_LOOP('',(#9863,#9864,#9865,#9866));
#1742=EDGE_LOOP('',(#9867,#9868,#9869,#9870));
#1743=EDGE_LOOP('',(#9871,#9872,#9873,#9874));
#1744=EDGE_LOOP('',(#9875,#9876,#9877,#9878));
#1745=EDGE_LOOP('',(#9879,#9880,#9881,#9882));
#1746=EDGE_LOOP('',(#9883,#9884,#9885,#9886));
#1747=EDGE_LOOP('',(#9887,#9888,#9889,#9890));
#1748=EDGE_LOOP('',(#9891,#9892,#9893,#9894));
#1749=EDGE_LOOP('',(#9895,#9896,#9897,#9898));
#1750=EDGE_LOOP('',(#9899,#9900,#9901,#9902));
#1751=EDGE_LOOP('',(#9903,#9904,#9905,#9906));
#1752=EDGE_LOOP('',(#9907,#9908,#9909,#9910));
#1753=EDGE_LOOP('',(#9911,#9912,#9913,#9914));
#1754=EDGE_LOOP('',(#9915,#9916,#9917,#9918));
#1755=EDGE_LOOP('',(#9919,#9920,#9921,#9922));
#1756=EDGE_LOOP('',(#9923,#9924,#9925,#9926));
#1757=EDGE_LOOP('',(#9927,#9928,#9929,#9930));
#1758=EDGE_LOOP('',(#9931,#9932,#9933,#9934));
#1759=EDGE_LOOP('',(#9935,#9936,#9937,#9938));
#1760=EDGE_LOOP('',(#9939,#9940,#9941,#9942));
#1761=EDGE_LOOP('',(#9943,#9944,#9945,#9946,#9947,#9948,#9949,#9950));
#1762=EDGE_LOOP('',(#9951,#9952,#9953,#9954,#9955,#9956,#9957,#9958,#9959,
#9960,#9961,#9962,#9963,#9964,#9965,#9966,#9967,#9968,#9969,#9970,#9971,
#9972,#9973,#9974,#9975,#9976,#9977,#9978,#9979,#9980,#9981,#9982,#9983,
#9984,#9985,#9986,#9987,#9988,#9989,#9990));
#1763=EDGE_LOOP('',(#9991,#9992,#9993,#9994));
#1764=EDGE_LOOP('',(#9995,#9996,#9997,#9998,#9999,#10000,#10001,#10002,
#10003,#10004,#10005,#10006,#10007,#10008,#10009,#10010,#10011,#10012,#10013,
#10014,#10015,#10016,#10017,#10018,#10019,#10020,#10021,#10022,#10023,#10024,
#10025,#10026,#10027,#10028,#10029,#10030,#10031,#10032,#10033,#10034,#10035));
#1765=EDGE_LOOP('',(#10036,#10037,#10038,#10039));
#1766=EDGE_LOOP('',(#10040,#10041,#10042,#10043));
#1767=EDGE_LOOP('',(#10044,#10045,#10046,#10047));
#1768=EDGE_LOOP('',(#10048,#10049,#10050,#10051));
#1769=EDGE_LOOP('',(#10052,#10053,#10054,#10055));
#1770=EDGE_LOOP('',(#10056,#10057,#10058,#10059));
#1771=EDGE_LOOP('',(#10060,#10061,#10062,#10063));
#1772=EDGE_LOOP('',(#10064,#10065,#10066,#10067,#10068,#10069));
#1773=EDGE_LOOP('',(#10070));
#1774=EDGE_LOOP('',(#10071,#10072,#10073,#10074));
#1775=EDGE_LOOP('',(#10075,#10076,#10077,#10078));
#1776=EDGE_LOOP('',(#10079));
#1777=EDGE_LOOP('',(#10080,#10081,#10082,#10083,#10084,#10085));
#1778=EDGE_LOOP('',(#10086));
#1978=CIRCLE('',#12151,0.14635);
#1979=CIRCLE('',#12170,0.117775);
#1980=CIRCLE('',#12189,0.14635);
#1981=CIRCLE('',#12190,0.05);
#1982=CIRCLE('',#12192,0.117775);
#1983=CIRCLE('',#12202,0.3);
#1984=CIRCLE('',#12204,0.3);
#2732=B_SPLINE_CURVE_WITH_KNOTS('',3,(#40452,#40453,#40454,#40455,#40456,
#40457,#40458,#40459,#40460,#40461),.UNSPECIFIED.,.F.,.F.,(4,3,3,4),(-4.09202352044855,
-3.97107960880372,-2.97830970660279,-2.07317267331974),.UNSPECIFIED.);
#2733=B_SPLINE_CURVE_WITH_KNOTS('',3,(#40464,#40465,#40466,#40467,#40468,
#40469,#40470),.UNSPECIFIED.,.F.,.F.,(4,3,4),(0.,0.993500176108578,1.12274180646087),
 .UNSPECIFIED.);
#2734=B_SPLINE_CURVE_WITH_KNOTS('',3,(#40475,#40476,#40477,#40478,#40479,
#40480,#40481,#40482,#40483,#40484,#40485,#40486,#40487,#40488,#40489,#40490,
#40491,#40492,#40493,#40494,#40495,#40496),.UNSPECIFIED.,.F.,.F.,(4,3,3,
3,3,3,3,4),(-10.3752088276281,-9.92769902200931,-8.93492911980838,-7.94215921760745,
-6.94938931540652,-5.95661941320559,-4.96384951100465,-4.09202352044855),
 .UNSPECIFIED.);
#2735=B_SPLINE_CURVE_WITH_KNOTS('',3,(#40497,#40498,#40499,#40500,#40501,
#40502,#40503,#40504,#40505,#40506,#40507,#40508,#40509,#40510,#40511,#40512,
#40513,#40514,#40515,#40516,#40517,#40518),.UNSPECIFIED.,.F.,.F.,(4,3,3,
3,3,3,3,4),(1.12274180646087,1.98700035221716,2.98050052832574,3.97400070443431,
4.96750088054289,5.96100105665147,6.95450123276005,7.40592711364046),
 .UNSPECIFIED.);
#2736=B_SPLINE_CURVE_WITH_KNOTS('',3,(#40523,#40524,#40525,#40526,#40527,
#40528,#40529,#40530,#40531,#40532,#40533,#40534,#40535,#40536,#40537,#40538,
#40539,#40540,#40541,#40542,#40543,#40544),.UNSPECIFIED.,.F.,.F.,(4,3,3,
3,3,3,3,4),(-16.6583941348077,-15.8843184352149,-14.891548533014,-13.898778630813,
-12.9060087286121,-11.9132388264112,-10.9204689242102,-10.3752088276281),
 .UNSPECIFIED.);
#2737=B_SPLINE_CURVE_WITH_KNOTS('',3,(#40545,#40546,#40547,#40548,#40549,
#40550,#40551,#40552,#40553,#40554,#40555,#40556,#40557,#40558,#40559,#40560,
#40561,#40562,#40563,#40564,#40565,#40566),.UNSPECIFIED.,.F.,.F.,(4,3,3,
3,3,3,3,4),(7.40592711364046,7.94800140886863,8.94150158497721,9.93500176108579,
10.9285019371944,11.922002113303,12.9155022894115,13.68911242082),
 .UNSPECIFIED.);
#2738=B_SPLINE_CURVE_WITH_KNOTS('',3,(#40571,#40572,#40573,#40574,#40575,
#40576,#40577,#40578,#40579,#40580,#40581,#40582,#40583,#40584,#40585,#40586,
#40587,#40588,#40589,#40590,#40591,#40592,#40593,#40594,#40595),
 .UNSPECIFIED.,.F.,.F.,(4,3,3,3,3,3,3,3,4),(-22.9415794419873,-22.8337077506214,
-21.8409378484205,-20.8481679462195,-19.8553980440186,-18.8626281418177,
-17.8698582396168,-16.8770883374158,-16.6583941348077),.UNSPECIFIED.);
#2739=B_SPLINE_CURVE_WITH_KNOTS('',3,(#40596,#40597,#40598,#40599,#40600,
#40601,#40602,#40603,#40604,#40605,#40606,#40607,#40608,#40609,#40610,#40611,
#40612,#40613,#40614,#40615,#40616,#40617,#40618,#40619,#40620),
 .UNSPECIFIED.,.F.,.F.,(4,3,3,3,3,3,3,3,4),(13.68911242082,13.9090024655201,
14.9025026416287,15.8960028177373,16.8895029938458,17.8830031699544,18.876503346063,
19.8700035221716,19.9722977279996),.UNSPECIFIED.);
#2740=B_SPLINE_CURVE_WITH_KNOTS('',3,(#40625,#40626,#40627,#40628,#40629,
#40630,#40631,#40632,#40633,#40634,#40635,#40636,#40637,#40638,#40639,#40640,
#40641,#40642,#40643,#40644,#40645,#40646),.UNSPECIFIED.,.F.,.F.,(4,3,3,
3,3,3,3,4),(-29.2247647491669,-28.790327163827,-27.7975572616261,-26.8047873594251,
-25.8120174572242,-24.8192475550233,-23.8264776528223,-22.9415794419873),
 .UNSPECIFIED.);
#2741=B_SPLINE_CURVE_WITH_KNOTS('',3,(#40647,#40648,#40649,#40650,#40651,
#40652,#40653,#40654,#40655,#40656,#40657,#40658,#40659,#40660,#40661,#40662,
#40663,#40664,#40665,#40666,#40667,#40668),.UNSPECIFIED.,.F.,.F.,(4,3,3,
3,3,3,3,4),(19.9722977279996,20.8635036982802,21.8570038743887,22.8505040504973,
23.8440042266059,24.8375044027145,25.8310045788231,26.2554830351792),
 .UNSPECIFIED.);
#2742=B_SPLINE_CURVE_WITH_KNOTS('',3,(#40673,#40674,#40675,#40676,#40677,
#40678,#40679,#40680,#40681,#40682,#40683,#40684,#40685,#40686,#40687,#40688,
#40689,#40690,#40691,#40692,#40693,#40694),.UNSPECIFIED.,.F.,.F.,(4,3,3,
3,3,3,3,4),(-35.5079500563465,-34.7469465770326,-33.7541766748316,-32.7614067726307,
-31.7686368704298,-30.7758669682288,-29.7830970660279,-29.2247647491669),
 .UNSPECIFIED.);
#2743=B_SPLINE_CURVE_WITH_KNOTS('',3,(#40695,#40696,#40697,#40698,#40699,
#40700,#40701,#40702,#40703,#40704,#40705,#40706,#40707,#40708,#40709,#40710,
#40711,#40712,#40713,#40714,#40715,#40716),.UNSPECIFIED.,.F.,.F.,(4,3,3,
3,3,3,3,4),(26.2554830351792,26.8245047549316,27.8180049310402,28.8115051071488,
29.8050052832574,30.798505459366,31.7920056354745,32.5386683423588),
 .UNSPECIFIED.);
#2744=B_SPLINE_CURVE_WITH_KNOTS('',3,(#40721,#40722,#40723,#40724,#40725,
#40726,#40727,#40728,#40729,#40730,#40731,#40732,#40733,#40734,#40735,#40736,
#40737,#40738,#40739,#40740,#40741,#40742,#40743,#40744,#40745),
 .UNSPECIFIED.,.F.,.F.,(4,3,3,3,3,3,3,3,4),(-41.7911353635261,-41.6963358924391,
-40.7035659902382,-39.7107960880372,-38.7180261858363,-37.7252562836354,
-36.7324863814344,-35.7397164792335,-35.5079500563465),.UNSPECIFIED.);
#2745=B_SPLINE_CURVE_WITH_KNOTS('',3,(#40746,#40747,#40748,#40749,#40750,
#40751,#40752,#40753,#40754,#40755,#40756,#40757,#40758,#40759,#40760,#40761,
#40762,#40763,#40764,#40765,#40766,#40767,#40768,#40769,#40770),
 .UNSPECIFIED.,.F.,.F.,(4,3,3,3,3,3,3,3,4),(32.5386683423588,32.7855058115831,
33.7790059876917,34.7725061638003,35.7660063399088,36.7595065160174,37.753006692126,
38.7465068682346,38.8218536495384),.UNSPECIFIED.);
#2746=B_SPLINE_CURVE_WITH_KNOTS('',3,(#40775,#40776,#40777,#40778,#40779,
#40780,#40781,#40782,#40783,#40784,#40785,#40786,#40787,#40788,#40789,#40790,
#40791,#40792,#40793,#40794,#40795,#40796),.UNSPECIFIED.,.F.,.F.,(4,3,3,
3,3,3,3,4),(-48.0743206707057,-47.6529553056447,-46.6601854034437,-45.6674155012428,
-44.6746455990419,-43.6818756968409,-42.68910579464,-41.7911353635261),
 .UNSPECIFIED.);
#2747=B_SPLINE_CURVE_WITH_KNOTS('',3,(#40797,#40798,#40799,#40800,#40801,
#40802,#40803,#40804,#40805,#40806,#40807,#40808,#40809,#40810,#40811,#40812,
#40813,#40814,#40815,#40816,#40817,#40818),.UNSPECIFIED.,.F.,.F.,(4,3,3,
3,3,3,3,4),(38.8218536495384,39.7400070443432,40.7335072204517,41.7270073965603,
42.7205075726689,43.7140077487775,44.7075079248861,45.105038956718),
 .UNSPECIFIED.);
#2748=B_SPLINE_CURVE_WITH_KNOTS('',3,(#40823,#40824,#40825,#40826,#40827,
#40828,#40829,#40830,#40831,#40832,#40833,#40834,#40835,#40836,#40837,#40838,
#40839,#40840,#40841,#40842,#40843,#40844),.UNSPECIFIED.,.F.,.F.,(4,3,3,
3,3,3,3,4),(-54.3575059778853,-53.6095747188503,-52.6168048166493,-51.6240349144484,
-50.6312650122475,-49.6384951100465,-48.6457252078456,-48.0743206707057),
 .UNSPECIFIED.);
#2749=B_SPLINE_CURVE_WITH_KNOTS('',3,(#40845,#40846,#40847,#40848,#40849,
#40850,#40851,#40852,#40853,#40854,#40855,#40856,#40857,#40858,#40859,#40860,
#40861,#40862,#40863,#40864,#40865,#40866),.UNSPECIFIED.,.F.,.F.,(4,3,3,
3,3,3,3,4),(45.105038956718,45.7010081009946,46.6945082771032,47.6880084532118,
48.6815086293204,49.675008805429,50.6685089815375,51.3882242638976),
 .UNSPECIFIED.);
#2750=B_SPLINE_CURVE_WITH_KNOTS('',3,(#40871,#40872,#40873,#40874,#40875,
#40876,#40877,#40878,#40879,#40880,#40881,#40882,#40883,#40884,#40885,#40886,
#40887,#40888,#40889,#40890,#40891,#40892,#40893,#40894,#40895),
 .UNSPECIFIED.,.F.,.F.,(4,3,3,3,3,3,3,3,4),(-60.6406912850649,-60.5589640342568,
-59.5661941320559,-58.5734242298549,-57.580654327654,-56.5878844254531,
-55.5951145232521,-54.6023446210512,-54.3575059778853),.UNSPECIFIED.);
#2751=B_SPLINE_CURVE_WITH_KNOTS('',3,(#40896,#40897,#40898,#40899,#40900,
#40901,#40902,#40903,#40904,#40905,#40906,#40907,#40908,#40909,#40910,#40911,
#40912,#40913,#40914,#40915,#40916,#40917,#40918,#40919,#40920),
 .UNSPECIFIED.,.F.,.F.,(4,3,3,3,3,3,3,3,4),(51.3882242638976,51.6620091576461,
52.6555093337547,53.6490095098633,54.6425096859719,55.6360098620804,56.629510038189,
57.6230102142976,57.6714095710772),.UNSPECIFIED.);
#2752=B_SPLINE_CURVE_WITH_KNOTS('',3,(#40925,#40926,#40927,#40928,#40929,
#40930,#40931,#40932,#40933,#40934,#40935,#40936,#40937,#40938,#40939,#40940,
#40941,#40942,#40943,#40944,#40945,#40946),.UNSPECIFIED.,.F.,.F.,(4,3,3,
3,3,3,3,4),(-66.9238765922445,-66.5155834474624,-65.5228135452614,-64.5300436430605,
-63.5372737408596,-62.5445038386586,-61.5517339364577,-60.6406912850649),
 .UNSPECIFIED.);
#2753=B_SPLINE_CURVE_WITH_KNOTS('',3,(#40947,#40948,#40949,#40950,#40951,
#40952,#40953,#40954,#40955,#40956,#40957,#40958,#40959,#40960,#40961,#40962,
#40963,#40964,#40965,#40966,#40967,#40968),.UNSPECIFIED.,.F.,.F.,(4,3,3,
3,3,3,3,4),(57.6714095710772,58.6165103904062,59.6100105665148,60.6035107426233,
61.5970109187319,62.5905110948405,63.5840112709491,63.9545948782568),
 .UNSPECIFIED.);
#2754=B_SPLINE_CURVE_WITH_KNOTS('',3,(#40973,#40974,#40975,#40976,#40977,
#40978,#40979,#40980,#40981,#40982,#40983,#40984,#40985,#40986,#40987,#40988,
#40989,#40990,#40991,#40992,#40993,#40994),.UNSPECIFIED.,.F.,.F.,(4,3,3,
3,3,3,3,4),(-73.207061899424,-72.4722028606679,-71.479432958467,-70.4866630562661,
-69.4938931540652,-68.5011232518642,-67.5083533496633,-66.9238765922445),
 .UNSPECIFIED.);
#2755=B_SPLINE_CURVE_WITH_KNOTS('',3,(#40995,#40996,#40997,#40998,#40999,
#41000,#41001,#41002,#41003,#41004,#41005,#41006,#41007,#41008,#41009,#41010,
#41011,#41012,#41013,#41014,#41015,#41016),.UNSPECIFIED.,.F.,.F.,(4,3,3,
3,3,3,3,4),(63.9545948782568,64.5775114470576,65.5710116231662,66.5645117992748,
67.5580119753834,68.551512151492,69.5450123276005,70.2377801854364),
 .UNSPECIFIED.);
#2756=B_SPLINE_CURVE_WITH_KNOTS('',3,(#41021,#41022,#41023,#41024,#41025,
#41026,#41027,#41028,#41029,#41030,#41031,#41032,#41033,#41034,#41035,#41036,
#41037,#41038,#41039,#41040,#41041,#41042,#41043,#41044,#41045),
 .UNSPECIFIED.,.F.,.F.,(4,3,3,3,3,3,3,3,4),(-79.4902472066036,-79.4215921760745,
-78.4288222738735,-77.4360523716726,-76.4432824694717,-75.4505125672707,
-74.4577426650698,-73.4649727628689,-73.207061899424),.UNSPECIFIED.);
#2757=B_SPLINE_CURVE_WITH_KNOTS('',3,(#41046,#41047,#41048,#41049,#41050,
#41051,#41052,#41053,#41054,#41055,#41056,#41057,#41058,#41059,#41060,#41061,
#41062,#41063,#41064,#41065,#41066,#41067,#41068,#41069,#41070),
 .UNSPECIFIED.,.F.,.F.,(4,3,3,3,3,3,3,3,4),(70.2377801854364,70.5385125037091,
71.5320126798177,72.5255128559263,73.5190130320348,74.5125132081434,75.506013384252,
76.4995135603606,76.520965492616),.UNSPECIFIED.);
#2758=B_SPLINE_CURVE_WITH_KNOTS('',3,(#41075,#41076,#41077,#41078,#41079,
#41080,#41081,#41082,#41083,#41084,#41085,#41086,#41087,#41088,#41089,#41090,
#41091,#41092,#41093,#41094,#41095,#41096),.UNSPECIFIED.,.F.,.F.,(4,3,3,
3,3,3,3,4),(-85.7734325137832,-85.3782115892801,-84.3854416870791,-83.3926717848782,
-82.3999018826773,-81.4071319804763,-80.4143620782754,-79.4902472066036),
 .UNSPECIFIED.);
#2759=B_SPLINE_CURVE_WITH_KNOTS('',3,(#41097,#41098,#41099,#41100,#41101,
#41102,#41103,#41104,#41105,#41106,#41107,#41108,#41109,#41110,#41111,#41112,
#41113,#41114,#41115,#41116,#41117,#41118),.UNSPECIFIED.,.F.,.F.,(4,3,3,
3,3,3,3,4),(76.520965492616,77.4930137364692,78.4865139125777,79.4800140886863,
80.4735142647949,81.4670144409035,82.4605146170121,82.8041507997956),
 .UNSPECIFIED.);
#2760=B_SPLINE_CURVE_WITH_KNOTS('',3,(#41123,#41124,#41125,#41126,#41127,
#41128,#41129,#41130,#41131,#41132,#41133,#41134,#41135,#41136,#41137,#41138,
#41139,#41140,#41141,#41142,#41143,#41144),.UNSPECIFIED.,.F.,.F.,(4,3,3,
3,3,3,3,4),(-92.0566178209628,-91.3348310024856,-90.3420611002847,-89.3492911980838,
-88.3565212958828,-87.3637513936819,-86.370981491481,-85.7734325137832),
 .UNSPECIFIED.);
#2761=B_SPLINE_CURVE_WITH_KNOTS('',3,(#41145,#41146,#41147,#41148,#41149,
#41150,#41151,#41152,#41153,#41154,#41155,#41156,#41157,#41158,#41159,#41160,
#41161,#41162,#41163,#41164,#41165,#41166),.UNSPECIFIED.,.F.,.F.,(4,3,3,
3,3,3,3,4),(82.8041507997956,83.4540147931206,84.4475149692292,85.4410151453378,
86.4345153214464,87.428015497555,88.4215156736635,89.0873361069751),
 .UNSPECIFIED.);
#2762=B_SPLINE_CURVE_WITH_KNOTS('',3,(#41171,#41172,#41173,#41174,#41175,
#41176,#41177,#41178,#41179,#41180,#41181,#41182,#41183,#41184,#41185,#41186,
#41187,#41188,#41189,#41190,#41191,#41192,#41193,#41194,#41195),
 .UNSPECIFIED.,.F.,.F.,(4,3,3,3,3,3,3,3,4),(-98.3398031281424,-98.2842203178921,
-97.2914504156912,-96.2986805134903,-95.3059106112893,-94.3131407090884,
-93.3203708068875,-92.3276009046866,-92.0566178209628),.UNSPECIFIED.);
#2763=B_SPLINE_CURVE_WITH_KNOTS('',3,(#41196,#41197,#41198,#41199,#41200,
#41201,#41202,#41203,#41204,#41205,#41206,#41207,#41208,#41209,#41210,#41211,
#41212,#41213,#41214,#41215,#41216,#41217),.UNSPECIFIED.,.F.,.F.,(4,3,3,
3,3,3,3,4),(89.0873361069751,89.4150158497721,90.4085160258807,91.4020162019893,
92.3955163780979,93.3890165542064,94.382516730315,95.3705214141547),
 .UNSPECIFIED.);
#2764=B_SPLINE_CURVE_WITH_KNOTS('',3,(#41222,#41223,#41224,#41225,#41226,
#41227,#41228,#41229,#41230,#41231,#41232,#41233,#41234,#41235,#41236,#41237,
#41238,#41239,#41240,#41241,#41242,#41243),.UNSPECIFIED.,.F.,.F.,(4,3,3,
3,3,3,3,4),(-104.622988435322,-104.240839731098,-103.248069828897,-102.255299926696,
-101.262530024495,-100.269760122294,-99.2769902200931,-98.3398031281424),
 .UNSPECIFIED.);
#2765=B_SPLINE_CURVE_WITH_KNOTS('',3,(#41244,#41245,#41246,#41247,#41248,
#41249,#41250,#41251,#41252,#41253,#41254,#41255,#41256,#41257,#41258,#41259,
#41260,#41261,#41262,#41263,#41264,#41265),.UNSPECIFIED.,.F.,.F.,(4,3,3,
3,3,3,3,4),(95.3705214141547,96.3695170825322,97.3630172586407,98.3565174347493,
99.3500176108579,100.343517786966,101.337017963075,101.653706721334),
 .UNSPECIFIED.);
#2766=B_SPLINE_CURVE_WITH_KNOTS('',3,(#41270,#41271,#41272,#41273,#41274,
#41275,#41276,#41277,#41278,#41279,#41280,#41281,#41282,#41283,#41284,#41285,
#41286,#41287,#41288,#41289,#41290,#41291),.UNSPECIFIED.,.F.,.F.,(4,3,3,
3,3,3,3,4),(-110.906173742502,-110.197459144303,-109.204689242102,-108.211919339901,
-107.219149437701,-106.2263795355,-105.233609633299,-104.622988435322),
 .UNSPECIFIED.);
#2767=B_SPLINE_CURVE_WITH_KNOTS('',3,(#41292,#41293,#41294,#41295,#41296,
#41297,#41298,#41299,#41300,#41301,#41302,#41303,#41304,#41305,#41306,#41307,
#41308,#41309,#41310,#41311,#41312,#41313),.UNSPECIFIED.,.F.,.F.,(4,3,3,
3,3,3,3,4),(101.653706721334,102.330518139184,103.324018315292,104.317518491401,
105.311018667509,106.304518843618,107.298019019727,107.936892028514),
 .UNSPECIFIED.);
#2768=B_SPLINE_CURVE_WITH_KNOTS('',3,(#41319,#41320,#41321,#41322,#41323,
#41324,#41325,#41326,#41327,#41328),.UNSPECIFIED.,.F.,.F.,(4,1,1,1,1,1,
1,4),(122.522113490002,122.806168794005,123.798938696205,124.791708598406,
125.784478500607,126.777248402808,127.770018305009,128.76278820721),
 .UNSPECIFIED.);
#2769=B_SPLINE_CURVE_WITH_KNOTS('',3,(#41331,#41332,#41333,#41334,#41335,
#41336,#41337,#41338,#41339),.UNSPECIFIED.,.F.,.F.,(4,1,1,1,1,1,4),(122.522113490002,
122.554556406795,123.548056582903,124.541556759012,125.535056935121,126.528557111229,
127.522057287338),.UNSPECIFIED.);
#2770=B_SPLINE_CURVE_WITH_KNOTS('',3,(#41344,#41345,#41346,#41347,#41348,
#41349,#41350,#41351,#41352,#41353),.UNSPECIFIED.,.F.,.F.,(4,1,1,1,1,1,
1,4),(116.238928182822,116.849549380799,117.842319283,118.835089185201,
119.827859087402,120.820628989603,121.813398891804,122.522113490002),
 .UNSPECIFIED.);
#2771=B_SPLINE_CURVE_WITH_KNOTS('',3,(#41354,#41355,#41356,#41357,#41358,
#41359,#41360,#41361,#41362,#41363),.UNSPECIFIED.,.F.,.F.,(4,1,1,1,1,1,
1,4),(116.238928182822,116.593555350143,117.587055526252,118.580555702361,
119.574055878469,120.567556054578,121.561056230686,122.522113490002),
 .UNSPECIFIED.);
#2772=B_SPLINE_CURVE_WITH_KNOTS('',3,(#41368,#41369,#41370,#41371,#41372,
#41373,#41374,#41375,#41376,#41377),.UNSPECIFIED.,.F.,.F.,(4,1,1,1,1,1,
1,4),(109.955742875643,110.892929967593,111.885699869794,112.878469771995,
113.871239674196,114.864009576397,115.856779478598,116.238928182822),
 .UNSPECIFIED.);
#2773=B_SPLINE_CURVE_WITH_KNOTS('',3,(#41378,#41379,#41380,#41381,#41382,
#41383,#41384,#41385,#41386,#41387),.UNSPECIFIED.,.F.,.F.,(4,1,1,1,1,1,
1,4),(109.955742875643,110.632554293492,111.626054469601,112.619554645709,
113.613054821818,114.606554997926,115.600055174035,116.238928182822),
 .UNSPECIFIED.);
#2774=B_SPLINE_CURVE_WITH_KNOTS('',3,(#41392,#41393,#41394,#41395,#41396,
#41397,#41398,#41399,#41400,#41401,#41402),.UNSPECIFIED.,.F.,.F.,(4,1,1,
1,1,1,1,1,4),(103.672557568463,103.943540652187,104.936310554388,105.929080456589,
106.92185035879,107.914620260991,108.907390163192,109.900160065392,109.955742875643),
 .UNSPECIFIED.);
#2775=B_SPLINE_CURVE_WITH_KNOTS('',3,(#41403,#41404,#41405,#41406,#41407,
#41408,#41409,#41410,#41411,#41412,#41413),.UNSPECIFIED.,.F.,.F.,(4,1,1,
1,1,1,1,1,4),(103.672557568463,103.678053060732,104.67155323684,105.665053412949,
106.658553589058,107.652053765166,108.645553941275,109.639054117383,109.955742875643),
 .UNSPECIFIED.);
#2776=B_SPLINE_CURVE_WITH_KNOTS('',3,(#41418,#41419,#41420,#41421,#41422,
#41423,#41424,#41425,#41426,#41427),.UNSPECIFIED.,.F.,.F.,(4,1,1,1,1,1,
1,4),(97.3893722612836,97.9869212389813,98.9796911411822,99.9724610433832,
100.965230945584,101.958000847785,102.950770749986,103.672557568463),
 .UNSPECIFIED.);
#2777=B_SPLINE_CURVE_WITH_KNOTS('',3,(#41428,#41429,#41430,#41431,#41432,
#41433,#41434,#41435,#41436,#41437),.UNSPECIFIED.,.F.,.F.,(4,1,1,1,1,1,
1,4),(97.3893722612835,97.7170520040804,98.710552180189,99.7040523562976,
100.697552532406,101.691052708515,102.684552884623,103.672557568463),
 .UNSPECIFIED.);
#2778=B_SPLINE_CURVE_WITH_KNOTS('',3,(#41442,#41443,#41444,#41445,#41446,
#41447,#41448,#41449,#41450,#41451),.UNSPECIFIED.,.F.,.F.,(4,1,1,1,1,1,
1,4),(91.106186954104,92.0303018257757,93.0230717279766,94.0158416301776,
95.0086115323785,96.0013814345794,96.9941513367804,97.3893722612836),
 .UNSPECIFIED.);
#2779=B_SPLINE_CURVE_WITH_KNOTS('',3,(#41452,#41453,#41454,#41455,#41456,
#41457,#41458,#41459,#41460,#41461),.UNSPECIFIED.,.F.,.F.,(4,1,1,1,1,1,
1,4),(91.106186954104,91.756050947429,92.7495511235375,93.7430512996461,
94.7365514757547,95.7300516518633,96.7235518279718,97.3893722612835),
 .UNSPECIFIED.);
#2780=B_SPLINE_CURVE_WITH_KNOTS('',3,(#41466,#41467,#41468,#41469,#41470,
#41471,#41472,#41473,#41474,#41475,#41476),.UNSPECIFIED.,.F.,.F.,(4,1,1,
1,1,1,1,1,4),(84.8230016469244,85.0809125103692,86.0736824125701,87.0664523147711,
88.059222216972,89.0519921191729,90.0447620213739,91.0375319235748,91.106186954104),
 .UNSPECIFIED.);
#2781=B_SPLINE_CURVE_WITH_KNOTS('',3,(#41477,#41478,#41479,#41480,#41481,
#41482,#41483,#41484,#41485,#41486),.UNSPECIFIED.,.F.,.F.,(4,1,1,1,1,1,
1,4),(84.8230016469244,85.7950498907775,86.7885500668861,87.7820502429946,
88.7755504191032,89.7690505952118,90.7625507713204,91.106186954104),
 .UNSPECIFIED.);
#2782=B_SPLINE_CURVE_WITH_KNOTS('',3,(#41491,#41492,#41493,#41494,#41495,
#41496,#41497,#41498,#41499,#41500),.UNSPECIFIED.,.F.,.F.,(4,1,1,1,1,1,
1,4),(78.5398163397448,79.1242930971636,80.1170629993645,81.1098329015655,
82.1026028037664,83.0953727059673,84.0881426081683,84.8230016469244),
 .UNSPECIFIED.);
#2783=B_SPLINE_CURVE_WITH_KNOTS('',3,(#41501,#41502,#41503,#41504,#41505,
#41506,#41507,#41508,#41509,#41510,#41511),.UNSPECIFIED.,.F.,.F.,(4,1,1,
1,1,1,1,1,4),(78.5398163397448,78.8405486580174,79.834048834126,80.8275490102346,
81.8210491863432,82.8145493624517,83.8080495385603,84.8015497146689,84.8230016469244),
 .UNSPECIFIED.);
#2784=B_SPLINE_CURVE_WITH_KNOTS('',3,(#41516,#41517,#41518,#41519,#41520,
#41521,#41522,#41523,#41524,#41525),.UNSPECIFIED.,.F.,.F.,(4,1,1,1,1,1,
1,4),(72.2566310325652,73.167673683958,74.160443586159,75.1532134883599,
76.1459833905608,77.1387532927618,78.1315231949627,78.5398163397448),
 .UNSPECIFIED.);
#2785=B_SPLINE_CURVE_WITH_KNOTS('',3,(#41526,#41527,#41528,#41529,#41530,
#41531,#41532,#41533,#41534,#41535),.UNSPECIFIED.,.F.,.F.,(4,1,1,1,1,1,
1,4),(72.2566310325652,72.879547601366,73.8730477774745,74.8665479535831,
75.8600481296917,76.8535483058003,77.8470484819088,78.5398163397448),
 .UNSPECIFIED.);
#2786=B_SPLINE_CURVE_WITH_KNOTS('',3,(#41540,#41541,#41542,#41543,#41544,
#41545,#41546,#41547,#41548,#41549,#41550),.UNSPECIFIED.,.F.,.F.,(4,1,1,
1,1,1,1,1,4),(65.9734457253856,66.2182843685515,67.2110542707524,68.2038241729534,
69.1965940751543,70.1893639773552,71.1821338795562,72.1749037817571,72.2566310325652),
 .UNSPECIFIED.);
#2787=B_SPLINE_CURVE_WITH_KNOTS('',3,(#41551,#41552,#41553,#41554,#41555,
#41556,#41557,#41558,#41559,#41560),.UNSPECIFIED.,.F.,.F.,(4,1,1,1,1,1,
1,4),(65.9734457253856,66.9185465447145,67.9120467208231,68.9055468969316,
69.8990470730402,70.8925472491488,71.8860474252574,72.2566310325652),
 .UNSPECIFIED.);
#2788=B_SPLINE_CURVE_WITH_KNOTS('',3,(#41565,#41566,#41567,#41568,#41569,
#41570,#41571,#41572,#41573,#41574),.UNSPECIFIED.,.F.,.F.,(4,1,1,1,1,1,
1,4),(59.690260418206,60.2616649553459,61.2544348575469,62.2472047597478,
63.2399746619487,64.2327445641497,65.2255144663506,65.9734457253856),
 .UNSPECIFIED.);
#2789=B_SPLINE_CURVE_WITH_KNOTS('',3,(#41575,#41576,#41577,#41578,#41579,
#41580,#41581,#41582,#41583,#41584,#41585),.UNSPECIFIED.,.F.,.F.,(4,1,1,
1,1,1,1,1,4),(59.690260418206,59.9640453119544,60.957545488063,61.9510456641716,
62.9445458402802,63.9380460163887,64.9315461924973,65.9250463686059,65.9734457253856),
 .UNSPECIFIED.);
#2790=B_SPLINE_CURVE_WITH_KNOTS('',3,(#41590,#41591,#41592,#41593,#41594,
#41595,#41596,#41597,#41598,#41599),.UNSPECIFIED.,.F.,.F.,(4,1,1,1,1,1,
1,4),(53.4070751110264,54.3050455421403,55.2978154443413,56.2905853465422,
57.2833552487431,58.2761251509441,59.268895053145,59.690260418206),
 .UNSPECIFIED.);
#2791=B_SPLINE_CURVE_WITH_KNOTS('',3,(#41600,#41601,#41602,#41603,#41604,
#41605,#41606,#41607,#41608,#41609),.UNSPECIFIED.,.F.,.F.,(4,1,1,1,1,1,
1,4),(53.4070751110264,54.003044255303,54.9965444314115,55.9900446075201,
56.9835447836287,57.9770449597373,58.9705451358458,59.690260418206),
 .UNSPECIFIED.);
#2792=B_SPLINE_CURVE_WITH_KNOTS('',3,(#41614,#41615,#41616,#41617,#41618,
#41619,#41620,#41621,#41622,#41623,#41624),.UNSPECIFIED.,.F.,.F.,(4,1,1,
1,1,1,1,1,4),(47.1238898038468,47.3556562267338,48.3484261289348,49.3411960311357,
50.3339659333366,51.3267358355376,52.3195057377385,53.3122756399394,53.4070751110264),
 .UNSPECIFIED.);
#2793=B_SPLINE_CURVE_WITH_KNOTS('',3,(#41625,#41626,#41627,#41628,#41629,
#41630,#41631,#41632,#41633,#41634),.UNSPECIFIED.,.F.,.F.,(4,1,1,1,1,1,
1,4),(47.1238898038468,48.0420431986515,49.0355433747601,50.0290435508686,
51.0225437269772,52.0160439030858,53.0095440791944,53.4070751110264),
 .UNSPECIFIED.);
#2794=B_SPLINE_CURVE_WITH_KNOTS('',3,(#41639,#41640,#41641,#41642,#41643,
#41644,#41645,#41646,#41647,#41648),.UNSPECIFIED.,.F.,.F.,(4,1,1,1,1,1,
1,4),(40.8407044966672,41.3990368135282,42.3918067157292,43.3845766179301,
44.377346520131,45.370116422332,46.3628863245329,47.1238898038468),
 .UNSPECIFIED.);
#2795=B_SPLINE_CURVE_WITH_KNOTS('',3,(#41649,#41650,#41651,#41652,#41653,
#41654,#41655,#41656,#41657,#41658,#41659),.UNSPECIFIED.,.F.,.F.,(4,1,1,
1,1,1,1,1,4),(40.8407044966672,41.0875419658914,42.081042142,43.0745423181086,
44.0680424942172,45.0615426703257,46.0550428464343,47.0485430225429,47.1238898038468),
 .UNSPECIFIED.);
#2796=B_SPLINE_CURVE_WITH_KNOTS('',3,(#41664,#41665,#41666,#41667,#41668,
#41669,#41670,#41671,#41672,#41673),.UNSPECIFIED.,.F.,.F.,(4,1,1,1,1,1,
1,4),(34.5575191894876,35.4424174003227,36.4351873025236,37.4279572047245,
38.4207271069255,39.4134970091264,40.4062669113273,40.8407044966672),
 .UNSPECIFIED.);
#2797=B_SPLINE_CURVE_WITH_KNOTS('',3,(#41674,#41675,#41676,#41677,#41678,
#41679,#41680,#41681,#41682,#41683),.UNSPECIFIED.,.F.,.F.,(4,1,1,1,1,1,
1,4),(34.5575191894876,35.1265409092399,36.1200410853485,37.1135412614571,
38.1070414375657,39.1005416136743,40.0940417897828,40.8407044966672),
 .UNSPECIFIED.);
#2798=B_SPLINE_CURVE_WITH_KNOTS('',3,(#41688,#41689,#41690,#41691,#41692,
#41693,#41694,#41695,#41696,#41697,#41698),.UNSPECIFIED.,.F.,.F.,(4,1,1,
1,1,1,1,1,4),(28.2743338823081,28.4930280849161,29.4857979871171,30.478567889318,
31.4713377915189,32.4641076937199,33.4568775959208,34.4496474981217,34.5575191894876),
 .UNSPECIFIED.);
#2799=B_SPLINE_CURVE_WITH_KNOTS('',3,(#41699,#41700,#41701,#41702,#41703,
#41704,#41705,#41706,#41707,#41708),.UNSPECIFIED.,.F.,.F.,(4,1,1,1,1,1,
1,4),(28.274333882308,29.1655398525885,30.1590400286971,31.1525402048056,
32.1460403809142,33.1395405570228,34.1330407331314,34.5575191894876),
 .UNSPECIFIED.);
#2800=B_SPLINE_CURVE_WITH_KNOTS('',3,(#41713,#41714,#41715,#41716,#41717,
#41718,#41719,#41720,#41721,#41722),.UNSPECIFIED.,.F.,.F.,(4,1,1,1,1,1,
1,4),(21.9911485751285,22.5364086717106,23.5291785739115,24.5219484761124,
25.5147183783134,26.5074882805143,27.5002581827152,28.2743338823081),
 .UNSPECIFIED.);
#2801=B_SPLINE_CURVE_WITH_KNOTS('',3,(#41723,#41724,#41725,#41726,#41727,
#41728,#41729,#41730,#41731,#41732,#41733),.UNSPECIFIED.,.F.,.F.,(4,1,1,
1,1,1,1,1,4),(21.9911485751284,22.2110386198284,23.204538795937,24.1980389720456,
25.1915391481542,26.1850393242627,27.1785395003713,28.1720396764799,28.274333882308),
 .UNSPECIFIED.);
#2802=B_SPLINE_CURVE_WITH_KNOTS('',3,(#41738,#41739,#41740,#41741,#41742,
#41743,#41744,#41745,#41746,#41747),.UNSPECIFIED.,.F.,.F.,(4,1,1,1,1,1,
1,4),(15.7079632679489,16.579789258505,17.5725591607059,18.5653290629068,
19.5580989651078,20.5508688673087,21.5436387695096,21.9911485751285),
 .UNSPECIFIED.);
#2803=B_SPLINE_CURVE_WITH_KNOTS('',3,(#41748,#41749,#41750,#41751,#41752,
#41753,#41754,#41755,#41756,#41757),.UNSPECIFIED.,.F.,.F.,(4,1,1,1,1,1,
1,4),(15.7079632679489,16.2500375631769,17.2435377392855,18.2370379153941,
19.2305380915027,20.2240382676113,21.2175384437198,21.9911485751284),
 .UNSPECIFIED.);
#2804=B_SPLINE_CURVE_WITH_KNOTS('',3,(#41760,#41761,#41762,#41763,#41764,
#41765,#41766,#41767,#41768,#41769,#41770,#41771,#41772,#41773,#41774,#41775,
#41776,#41777,#41778,#41779,#41780,#41781,#41782,#41783,#41784,#41785,#41786,
#41787,#41788,#41789,#41790,#41791,#41792,#41793,#41794,#41795,#41796,#41797,
#41798,#41799,#41800,#41801,#41802,#41803,#41804,#41805,#41806,#41807,#41808,
#41809,#41810,#41811,#41812,#41813,#41814,#41815,#41816,#41817,#41818,#41819,
#41820,#41821,#41822,#41823,#41824,#41825,#41826,#41827,#41828,#41829,#41830,
#41831,#41832,#41833,#41834,#41835,#41836,#41837,#41838,#41839,#41840,#41841,
#41842,#41843,#41844,#41845,#41846,#41847,#41848,#41849,#41850,#41851,#41852,
#41853,#41854,#41855,#41856,#41857,#41858,#41859,#41860,#41861,#41862,#41863,
#41864,#41865,#41866,#41867,#41868,#41869,#41870,#41871,#41872,#41873,#41874,
#41875,#41876,#41877,#41878,#41879,#41880),.UNSPECIFIED.,.F.,.F.,(4,3,3,
3,3,3,3,3,3,3,3,3,3,3,3,3,3,3,3,3,3,3,3,3,3,3,3,3,3,3,3,3,3,3,3,3,3,3,3,
3,4),(-0.753008129282273,-0.726411087083563,-0.715881786499564,-0.695023186638146,
-0.683336694953651,-0.673827840112005,-0.646303346018245,-0.632512441881234,
-0.6236006747729,-0.596001444533992,-0.585111150938268,-0.576118283133321,
-0.547602758918121,-0.536376015702489,-0.528202226180116,-0.507015336770619,
-0.486225152468931,-0.477897600046977,-0.452583818906367,-0.439178352550759,
-0.427196798483684,-0.40191963698411,-0.385160728199621,-0.376642475484535,
-0.347726720901875,-0.333286923643958,-0.323497787746622,-0.293375916145958,
-0.277554167376485,-0.267492310267894,-0.241337846280271,-0.224844604159538,
-0.216317003933383,-0.18753716728625,-0.170582917097926,-0.162078349438165,
-0.131638003391508,-0.115498895283149,-0.106874758104641,-0.101197657344851,
-0.0965360155478817),.UNSPECIFIED.);
#2805=B_SPLINE_CURVE_WITH_KNOTS('',3,(#41882,#41883,#41884,#41885,#41886,
#41887,#41888,#41889,#41890,#41891,#41892,#41893,#41894,#41895,#41896,#41897,
#41898,#41899,#41900,#41901,#41902,#41903,#41904,#41905,#41906,#41907,#41908,
#41909,#41910,#41911,#41912,#41913,#41914,#41915),.UNSPECIFIED.,.F.,.F.,
(4,3,3,3,3,3,3,3,3,3,3,4),(-0.204609524178367,-0.173916487069214,-0.152160152794692,
-0.142779925772755,-0.129154387771013,-0.104956417030493,-0.0922484622970884,
-0.0691863467228163,-0.0542893062834328,-0.041770965424307,-0.0153008738219011,
0.),.UNSPECIFIED.);
#2806=B_SPLINE_CURVE_WITH_KNOTS('',3,(#41918,#41919,#41920,#41921,#41922,
#41923,#41924,#41925,#41926,#41927,#41928,#41929,#41930,#41931,#41932,#41933),
 .UNSPECIFIED.,.F.,.F.,(4,3,3,3,3,4),(-0.0965360155478817,-0.0724020116609113,
-0.0590192863946756,-0.0503863222172558,-0.0186895043865902,0.),
 .UNSPECIFIED.);
#2807=B_SPLINE_CURVE_WITH_KNOTS('',3,(#42422,#42423,#42424,#42425,#42426,
#42427,#42428,#42429),.UNSPECIFIED.,.F.,.F.,(4,1,1,1,1,4),(11.6159397475003,
12.6087096497013,13.6014795519022,14.5942494541031,15.5870193563041,15.7079632679489),
 .UNSPECIFIED.);
#2808=B_SPLINE_CURVE_WITH_KNOTS('',3,(#42430,#42431,#42432,#42433,#42434,
#42435,#42436,#42437,#42438,#42439,#42440,#42441,#42442,#42443,#42444,#42445,
#42446,#42447,#42448,#42449,#42450,#42451,#42452,#42453,#42454,#42455,#42456,
#42457,#42458,#42459,#42460,#42461,#42462,#42463,#42464,#42465,#42466,#42467,
#42468,#42469,#42470,#42471,#42472,#42473,#42474,#42475,#42476,#42477,#42478,
#42479,#42480,#42481,#42482,#42483,#42484),.UNSPECIFIED.,.F.,.F.,(4,3,3,
3,3,3,3,3,3,3,3,3,3,3,3,3,3,3,4),(-0.275362278356885,-0.262570109468003,
-0.240166040204702,-0.228737803218204,-0.209304350143588,-0.199561001302199,
-0.189130684518224,-0.159734566166372,-0.148075950500899,-0.139790942517999,
-0.124720142759856,-0.107306928893897,-0.096279762610833,-0.086780292972213,
-0.0650852197291597,-0.0467838010330817,-0.0380963509139461,-0.011916188874275,
0.),.UNSPECIFIED.);
#2809=B_SPLINE_CURVE_WITH_KNOTS('',3,(#42485,#42486,#42487,#42488,#42489,
#42490,#42491,#42492,#42493,#42494,#42495,#42496,#42497,#42498,#42499,#42500,
#42501,#42502,#42503),.UNSPECIFIED.,.F.,.F.,(4,3,3,3,3,3,4),(-115.629180729976,
-115.161308655308,-114.168538753107,-113.175768850906,-112.182998948705,
-111.190229046504,-110.906173742502),.UNSPECIFIED.);
#2810=B_SPLINE_CURVE_WITH_KNOTS('',3,(#42506,#42507,#42508,#42509,#42510,
#42511,#42512,#42513,#42514),.UNSPECIFIED.,.F.,.F.,(4,1,1,1,1,1,4),(10.375208827628,
11.282536682634,12.2760368587426,13.2695370348512,14.2630372109598,15.2565373870684,
15.7079632679489),.UNSPECIFIED.);
#2811=B_SPLINE_CURVE_WITH_KNOTS('',3,(#43008,#43009,#43010,#43011,#43012,
#43013,#43014,#43015,#43016,#43017,#43018,#43019,#43020,#43021,#43022,#43023,
#43024,#43025,#43026,#43027,#43028,#43029),.UNSPECIFIED.,.F.,.F.,(4,3,3,
3,3,3,3,4),(107.936892028514,108.291519195835,109.285019371944,110.278519548052,
111.272019724161,112.265519900269,113.259020076378,113.556008056657),
 .UNSPECIFIED.);
#2812=B_SPLINE_CURVE_WITH_KNOTS('',3,(#43030,#43031,#43032,#43033,#43034,
#43035,#43036,#43037,#43038,#43039,#43040,#43041,#43042,#43043,#43044,#43045,
#43046,#43047,#43048,#43049,#43050,#43051,#43052,#43053,#43054,#43055,#43056,
#43057,#43058,#43059,#43060,#43061,#43062,#43063,#43064,#43065,#43066,#43067,
#43068,#43069,#43070,#43071,#43072,#43073,#43074,#43075,#43076,#43077,#43078,
#43079,#43080,#43081),.UNSPECIFIED.,.F.,.F.,(4,3,3,3,3,3,3,3,3,3,3,3,3,
3,3,3,3,4),(-0.276631791712727,-0.266310431017225,-0.251016700765444,-0.236970857216412,
-0.216553357237997,-0.204277578780747,-0.175779167785564,-0.164239042752865,
-0.155154932673123,-0.139868422463251,-0.120223860282124,-0.110723029685393,
-0.100734922391118,-0.0755511917933386,-0.0588149891352748,-0.049317539854096,
-0.0183008691858031,0.),.UNSPECIFIED.);
#3382=LINE('',#40450,#4014);
#3383=LINE('',#40474,#4015);
#3384=LINE('',#40522,#4016);
#3385=LINE('',#40570,#4017);
#3386=LINE('',#40624,#4018);
#3387=LINE('',#40672,#4019);
#3388=LINE('',#40720,#4020);
#3389=LINE('',#40774,#4021);
#3390=LINE('',#40822,#4022);
#3391=LINE('',#40870,#4023);
#3392=LINE('',#40924,#4024);
#3393=LINE('',#40972,#4025);
#3394=LINE('',#41020,#4026);
#3395=LINE('',#41074,#4027);
#3396=LINE('',#41122,#4028);
#3397=LINE('',#41170,#4029);
#3398=LINE('',#41221,#4030);
#3399=LINE('',#41269,#4031);
#3400=LINE('',#41317,#4032);
#3401=LINE('',#41343,#4033);
#3402=LINE('',#41367,#4034);
#3403=LINE('',#41391,#4035);
#3404=LINE('',#41417,#4036);
#3405=LINE('',#41441,#4037);
#3406=LINE('',#41465,#4038);
#3407=LINE('',#41490,#4039);
#3408=LINE('',#41515,#4040);
#3409=LINE('',#41539,#4041);
#3410=LINE('',#41564,#4042);
#3411=LINE('',#41589,#4043);
#3412=LINE('',#41613,#4044);
#3413=LINE('',#41638,#4045);
#3414=LINE('',#41663,#4046);
#3415=LINE('',#41687,#4047);
#3416=LINE('',#41712,#4048);
#3417=LINE('',#41737,#4049);
#3418=LINE('',#41935,#4050);
#3419=LINE('',#43086,#4051);
#3420=LINE('',#43088,#4052);
#3421=LINE('',#43090,#4053);
#3422=LINE('',#43091,#4054);
#3423=LINE('',#43094,#4055);
#3424=LINE('',#43096,#4056);
#3425=LINE('',#43097,#4057);
#3426=LINE('',#43100,#4058);
#3427=LINE('',#43102,#4059);
#3428=LINE('',#43103,#4060);
#3429=LINE('',#43106,#4061);
#3430=LINE('',#43108,#4062);
#3431=LINE('',#43109,#4063);
#3432=LINE('',#43112,#4064);
#3433=LINE('',#43114,#4065);
#3434=LINE('',#43115,#4066);
#3435=LINE('',#43117,#4067);
#3436=LINE('',#43118,#4068);
#3437=LINE('',#43125,#4069);
#4014=VECTOR('',#14249,0.15);
#4015=VECTOR('',#14254,0.15);
#4016=VECTOR('',#14257,0.15);
#4017=VECTOR('',#14260,0.15);
#4018=VECTOR('',#14263,0.15);
#4019=VECTOR('',#14266,0.15);
#4020=VECTOR('',#14269,0.15);
#4021=VECTOR('',#14272,0.15);
#4022=VECTOR('',#14275,0.15);
#4023=VECTOR('',#14278,0.15);
#4024=VECTOR('',#14281,0.15);
#4025=VECTOR('',#14284,0.15);
#4026=VECTOR('',#14287,0.15);
#4027=VECTOR('',#14290,0.15);
#4028=VECTOR('',#14293,0.15);
#4029=VECTOR('',#14296,0.15);
#4030=VECTOR('',#14299,0.15);
#4031=VECTOR('',#14302,0.15);
#4032=VECTOR('',#14305,0.117775);
#4033=VECTOR('',#14310,0.117775);
#4034=VECTOR('',#14313,0.117775);
#4035=VECTOR('',#14316,0.117775);
#4036=VECTOR('',#14319,0.117775);
#4037=VECTOR('',#14322,0.117775);
#4038=VECTOR('',#14325,0.117775);
#4039=VECTOR('',#14328,0.117775);
#4040=VECTOR('',#14331,0.117775);
#4041=VECTOR('',#14334,0.117775);
#4042=VECTOR('',#14337,0.117775);
#4043=VECTOR('',#14340,0.117775);
#4044=VECTOR('',#14343,0.117775);
#4045=VECTOR('',#14346,0.117775);
#4046=VECTOR('',#14349,0.117775);
#4047=VECTOR('',#14352,0.117775);
#4048=VECTOR('',#14355,0.117775);
#4049=VECTOR('',#14358,0.117775);
#4050=VECTOR('',#14363,0.1);
#4051=VECTOR('',#14374,1.);
#4052=VECTOR('',#14375,1.);
#4053=VECTOR('',#14376,1.);
#4054=VECTOR('',#14377,1.);
#4055=VECTOR('',#14380,1.);
#4056=VECTOR('',#14381,1.);
#4057=VECTOR('',#14382,1.);
#4058=VECTOR('',#14385,1.);
#4059=VECTOR('',#14386,1.);
#4060=VECTOR('',#14387,1.);
#4061=VECTOR('',#14390,1.);
#4062=VECTOR('',#14391,1.);
#4063=VECTOR('',#14392,1.);
#4064=VECTOR('',#14395,1.);
#4065=VECTOR('',#14396,1.);
#4066=VECTOR('',#14397,1.);
#4067=VECTOR('',#14400,1.);
#4068=VECTOR('',#14401,1.);
#4069=VECTOR('',#14410,0.3);
#5072=VERTEX_POINT('',#40448);
#5073=VERTEX_POINT('',#40449);
#5074=VERTEX_POINT('',#40451);
#5075=VERTEX_POINT('',#40462);
#5076=VERTEX_POINT('',#40472);
#5077=VERTEX_POINT('',#40473);
#5078=VERTEX_POINT('',#40520);
#5079=VERTEX_POINT('',#40521);
#5080=VERTEX_POINT('',#40568);
#5081=VERTEX_POINT('',#40569);
#5082=VERTEX_POINT('',#40622);
#5083=VERTEX_POINT('',#40623);
#5084=VERTEX_POINT('',#40670);
#5085=VERTEX_POINT('',#40671);
#5086=VERTEX_POINT('',#40718);
#5087=VERTEX_POINT('',#40719);
#5088=VERTEX_POINT('',#40772);
#5089=VERTEX_POINT('',#40773);
#5090=VERTEX_POINT('',#40820);
#5091=VERTEX_POINT('',#40821);
#5092=VERTEX_POINT('',#40868);
#5093=VERTEX_POINT('',#40869);
#5094=VERTEX_POINT('',#40922);
#5095=VERTEX_POINT('',#40923);
#5096=VERTEX_POINT('',#40970);
#5097=VERTEX_POINT('',#40971);
#5098=VERTEX_POINT('',#41018);
#5099=VERTEX_POINT('',#41019);
#5100=VERTEX_POINT('',#41072);
#5101=VERTEX_POINT('',#41073);
#5102=VERTEX_POINT('',#41120);
#5103=VERTEX_POINT('',#41121);
#5104=VERTEX_POINT('',#41168);
#5105=VERTEX_POINT('',#41169);
#5106=VERTEX_POINT('',#41219);
#5107=VERTEX_POINT('',#41220);
#5108=VERTEX_POINT('',#41267);
#5109=VERTEX_POINT('',#41268);
#5110=VERTEX_POINT('',#41315);
#5111=VERTEX_POINT('',#41316);
#5112=VERTEX_POINT('',#41318);
#5113=VERTEX_POINT('',#41329);
#5114=VERTEX_POINT('',#41341);
#5115=VERTEX_POINT('',#41342);
#5116=VERTEX_POINT('',#41365);
#5117=VERTEX_POINT('',#41366);
#5118=VERTEX_POINT('',#41389);
#5119=VERTEX_POINT('',#41390);
#5120=VERTEX_POINT('',#41415);
#5121=VERTEX_POINT('',#41416);
#5122=VERTEX_POINT('',#41439);
#5123=VERTEX_POINT('',#41440);
#5124=VERTEX_POINT('',#41463);
#5125=VERTEX_POINT('',#41464);
#5126=VERTEX_POINT('',#41488);
#5127=VERTEX_POINT('',#41489);
#5128=VERTEX_POINT('',#41513);
#5129=VERTEX_POINT('',#41514);
#5130=VERTEX_POINT('',#41537);
#5131=VERTEX_POINT('',#41538);
#5132=VERTEX_POINT('',#41562);
#5133=VERTEX_POINT('',#41563);
#5134=VERTEX_POINT('',#41587);
#5135=VERTEX_POINT('',#41588);
#5136=VERTEX_POINT('',#41611);
#5137=VERTEX_POINT('',#41612);
#5138=VERTEX_POINT('',#41636);
#5139=VERTEX_POINT('',#41637);
#5140=VERTEX_POINT('',#41661);
#5141=VERTEX_POINT('',#41662);
#5142=VERTEX_POINT('',#41685);
#5143=VERTEX_POINT('',#41686);
#5144=VERTEX_POINT('',#41710);
#5145=VERTEX_POINT('',#41711);
#5146=VERTEX_POINT('',#41735);
#5147=VERTEX_POINT('',#41736);
#5148=VERTEX_POINT('',#41759);
#5149=VERTEX_POINT('',#41881);
#5150=VERTEX_POINT('',#41916);
#5151=VERTEX_POINT('',#41934);
#5152=VERTEX_POINT('',#42421);
#5153=VERTEX_POINT('',#42505);
#5154=VERTEX_POINT('',#43084);
#5155=VERTEX_POINT('',#43085);
#5156=VERTEX_POINT('',#43087);
#5157=VERTEX_POINT('',#43089);
#5158=VERTEX_POINT('',#43093);
#5159=VERTEX_POINT('',#43095);
#5160=VERTEX_POINT('',#43099);
#5161=VERTEX_POINT('',#43101);
#5162=VERTEX_POINT('',#43105);
#5163=VERTEX_POINT('',#43107);
#5164=VERTEX_POINT('',#43111);
#5165=VERTEX_POINT('',#43113);
#5166=VERTEX_POINT('',#43121);
#5167=VERTEX_POINT('',#43124);
#6669=EDGE_CURVE('',#5072,#5073,#3382,.T.);
#6670=EDGE_CURVE('',#5072,#5074,#2732,.T.);
#6671=EDGE_CURVE('',#5074,#5075,#1978,.F.);
#6672=EDGE_CURVE('',#5075,#5073,#2733,.T.);
#6673=EDGE_CURVE('',#5076,#5077,#3383,.T.);
#6674=EDGE_CURVE('',#5076,#5072,#2734,.T.);
#6675=EDGE_CURVE('',#5073,#5077,#2735,.T.);
#6676=EDGE_CURVE('',#5078,#5079,#3384,.T.);
#6677=EDGE_CURVE('',#5078,#5076,#2736,.T.);
#6678=EDGE_CURVE('',#5077,#5079,#2737,.T.);
#6679=EDGE_CURVE('',#5080,#5081,#3385,.T.);
#6680=EDGE_CURVE('',#5080,#5078,#2738,.T.);
#6681=EDGE_CURVE('',#5079,#5081,#2739,.T.);
#6682=EDGE_CURVE('',#5082,#5083,#3386,.T.);
#6683=EDGE_CURVE('',#5082,#5080,#2740,.T.);
#6684=EDGE_CURVE('',#5081,#5083,#2741,.T.);
#6685=EDGE_CURVE('',#5084,#5085,#3387,.T.);
#6686=EDGE_CURVE('',#5084,#5082,#2742,.T.);
#6687=EDGE_CURVE('',#5083,#5085,#2743,.T.);
#6688=EDGE_CURVE('',#5086,#5087,#3388,.T.);
#6689=EDGE_CURVE('',#5086,#5084,#2744,.T.);
#6690=EDGE_CURVE('',#5085,#5087,#2745,.T.);
#6691=EDGE_CURVE('',#5088,#5089,#3389,.T.);
#6692=EDGE_CURVE('',#5088,#5086,#2746,.T.);
#6693=EDGE_CURVE('',#5087,#5089,#2747,.T.);
#6694=EDGE_CURVE('',#5090,#5091,#3390,.T.);
#6695=EDGE_CURVE('',#5090,#5088,#2748,.T.);
#6696=EDGE_CURVE('',#5089,#5091,#2749,.T.);
#6697=EDGE_CURVE('',#5092,#5093,#3391,.T.);
#6698=EDGE_CURVE('',#5092,#5090,#2750,.T.);
#6699=EDGE_CURVE('',#5091,#5093,#2751,.T.);
#6700=EDGE_CURVE('',#5094,#5095,#3392,.T.);
#6701=EDGE_CURVE('',#5094,#5092,#2752,.T.);
#6702=EDGE_CURVE('',#5093,#5095,#2753,.T.);
#6703=EDGE_CURVE('',#5096,#5097,#3393,.T.);
#6704=EDGE_CURVE('',#5096,#5094,#2754,.T.);
#6705=EDGE_CURVE('',#5095,#5097,#2755,.T.);
#6706=EDGE_CURVE('',#5098,#5099,#3394,.T.);
#6707=EDGE_CURVE('',#5098,#5096,#2756,.T.);
#6708=EDGE_CURVE('',#5097,#5099,#2757,.T.);
#6709=EDGE_CURVE('',#5100,#5101,#3395,.T.);
#6710=EDGE_CURVE('',#5100,#5098,#2758,.T.);
#6711=EDGE_CURVE('',#5099,#5101,#2759,.T.);
#6712=EDGE_CURVE('',#5102,#5103,#3396,.T.);
#6713=EDGE_CURVE('',#5102,#5100,#2760,.T.);
#6714=EDGE_CURVE('',#5101,#5103,#2761,.T.);
#6715=EDGE_CURVE('',#5104,#5105,#3397,.T.);
#6716=EDGE_CURVE('',#5104,#5102,#2762,.T.);
#6717=EDGE_CURVE('',#5103,#5105,#2763,.T.);
#6718=EDGE_CURVE('',#5106,#5107,#3398,.T.);
#6719=EDGE_CURVE('',#5106,#5104,#2764,.T.);
#6720=EDGE_CURVE('',#5105,#5107,#2765,.T.);
#6721=EDGE_CURVE('',#5108,#5109,#3399,.T.);
#6722=EDGE_CURVE('',#5108,#5106,#2766,.T.);
#6723=EDGE_CURVE('',#5107,#5109,#2767,.T.);
#6724=EDGE_CURVE('',#5110,#5111,#3400,.T.);
#6725=EDGE_CURVE('',#5110,#5112,#2768,.T.);
#6726=EDGE_CURVE('',#5112,#5113,#1979,.T.);
#6727=EDGE_CURVE('',#5111,#5113,#2769,.T.);
#6728=EDGE_CURVE('',#5114,#5115,#3401,.T.);
#6729=EDGE_CURVE('',#5114,#5110,#2770,.T.);
#6730=EDGE_CURVE('',#5115,#5111,#2771,.T.);
#6731=EDGE_CURVE('',#5116,#5117,#3402,.T.);
#6732=EDGE_CURVE('',#5116,#5114,#2772,.T.);
#6733=EDGE_CURVE('',#5117,#5115,#2773,.T.);
#6734=EDGE_CURVE('',#5118,#5119,#3403,.T.);
#6735=EDGE_CURVE('',#5118,#5116,#2774,.T.);
#6736=EDGE_CURVE('',#5119,#5117,#2775,.T.);
#6737=EDGE_CURVE('',#5120,#5121,#3404,.T.);
#6738=EDGE_CURVE('',#5120,#5118,#2776,.T.);
#6739=EDGE_CURVE('',#5121,#5119,#2777,.T.);
#6740=EDGE_CURVE('',#5122,#5123,#3405,.T.);
#6741=EDGE_CURVE('',#5122,#5120,#2778,.T.);
#6742=EDGE_CURVE('',#5123,#5121,#2779,.T.);
#6743=EDGE_CURVE('',#5124,#5125,#3406,.T.);
#6744=EDGE_CURVE('',#5124,#5122,#2780,.T.);
#6745=EDGE_CURVE('',#5125,#5123,#2781,.T.);
#6746=EDGE_CURVE('',#5126,#5127,#3407,.T.);
#6747=EDGE_CURVE('',#5126,#5124,#2782,.T.);
#6748=EDGE_CURVE('',#5127,#5125,#2783,.T.);
#6749=EDGE_CURVE('',#5128,#5129,#3408,.T.);
#6750=EDGE_CURVE('',#5128,#5126,#2784,.T.);
#6751=EDGE_CURVE('',#5129,#5127,#2785,.T.);
#6752=EDGE_CURVE('',#5130,#5131,#3409,.T.);
#6753=EDGE_CURVE('',#5130,#5128,#2786,.T.);
#6754=EDGE_CURVE('',#5131,#5129,#2787,.T.);
#6755=EDGE_CURVE('',#5132,#5133,#3410,.T.);
#6756=EDGE_CURVE('',#5132,#5130,#2788,.T.);
#6757=EDGE_CURVE('',#5133,#5131,#2789,.T.);
#6758=EDGE_CURVE('',#5134,#5135,#3411,.T.);
#6759=EDGE_CURVE('',#5134,#5132,#2790,.T.);
#6760=EDGE_CURVE('',#5135,#5133,#2791,.T.);
#6761=EDGE_CURVE('',#5136,#5137,#3412,.T.);
#6762=EDGE_CURVE('',#5136,#5134,#2792,.T.);
#6763=EDGE_CURVE('',#5137,#5135,#2793,.T.);
#6764=EDGE_CURVE('',#5138,#5139,#3413,.T.);
#6765=EDGE_CURVE('',#5138,#5136,#2794,.T.);
#6766=EDGE_CURVE('',#5139,#5137,#2795,.T.);
#6767=EDGE_CURVE('',#5140,#5141,#3414,.T.);
#6768=EDGE_CURVE('',#5140,#5138,#2796,.T.);
#6769=EDGE_CURVE('',#5141,#5139,#2797,.T.);
#6770=EDGE_CURVE('',#5142,#5143,#3415,.T.);
#6771=EDGE_CURVE('',#5142,#5140,#2798,.T.);
#6772=EDGE_CURVE('',#5143,#5141,#2799,.T.);
#6773=EDGE_CURVE('',#5144,#5145,#3416,.T.);
#6774=EDGE_CURVE('',#5144,#5142,#2800,.T.);
#6775=EDGE_CURVE('',#5145,#5143,#2801,.T.);
#6776=EDGE_CURVE('',#5146,#5147,#3417,.T.);
#6777=EDGE_CURVE('',#5146,#5144,#2802,.T.);
#6778=EDGE_CURVE('',#5147,#5145,#2803,.T.);
#6779=EDGE_CURVE('',#5113,#5148,#2804,.T.);
#6780=EDGE_CURVE('',#5149,#5112,#2805,.T.);
#6781=EDGE_CURVE('',#5150,#5149,#1980,.T.);
#6782=EDGE_CURVE('',#5148,#5150,#2806,.T.);
#6783=EDGE_CURVE('',#5148,#5151,#3418,.T.);
#6784=EDGE_CURVE('',#5151,#5151,#1981,.T.);
#6785=EDGE_CURVE('',#5152,#5146,#2807,.T.);
#6786=EDGE_CURVE('',#5074,#5152,#2808,.T.);
#6787=EDGE_CURVE('',#5149,#5108,#2809,.T.);
#6788=EDGE_CURVE('',#5153,#5147,#2810,.T.);
#6789=EDGE_CURVE('',#5152,#5153,#1982,.T.);
#6790=EDGE_CURVE('',#5109,#5150,#2811,.T.);
#6791=EDGE_CURVE('',#5153,#5075,#2812,.T.);
#6792=EDGE_CURVE('',#5154,#5155,#3419,.T.);
#6793=EDGE_CURVE('',#5154,#5156,#3420,.T.);
#6794=EDGE_CURVE('',#5156,#5157,#3421,.T.);
#6795=EDGE_CURVE('',#5155,#5157,#3422,.T.);
#6796=EDGE_CURVE('',#5158,#5154,#3423,.T.);
#6797=EDGE_CURVE('',#5158,#5159,#3424,.T.);
#6798=EDGE_CURVE('',#5159,#5156,#3425,.T.);
#6799=EDGE_CURVE('',#5160,#5158,#3426,.T.);
#6800=EDGE_CURVE('',#5160,#5161,#3427,.T.);
#6801=EDGE_CURVE('',#5161,#5159,#3428,.T.);
#6802=EDGE_CURVE('',#5162,#5160,#3429,.T.);
#6803=EDGE_CURVE('',#5162,#5163,#3430,.T.);
#6804=EDGE_CURVE('',#5163,#5161,#3431,.T.);
#6805=EDGE_CURVE('',#5164,#5162,#3432,.T.);
#6806=EDGE_CURVE('',#5164,#5165,#3433,.T.);
#6807=EDGE_CURVE('',#5165,#5163,#3434,.T.);
#6808=EDGE_CURVE('',#5155,#5164,#3435,.T.);
#6809=EDGE_CURVE('',#5157,#5165,#3436,.T.);
#6810=EDGE_CURVE('',#5166,#5166,#1983,.T.);
#6811=EDGE_CURVE('',#5166,#5167,#3437,.T.);
#6812=EDGE_CURVE('',#5167,#5167,#1984,.T.);
#9799=ORIENTED_EDGE('',*,*,#6669,.F.);
#9800=ORIENTED_EDGE('',*,*,#6670,.T.);
#9801=ORIENTED_EDGE('',*,*,#6671,.T.);
#9802=ORIENTED_EDGE('',*,*,#6672,.T.);
#9803=ORIENTED_EDGE('',*,*,#6673,.F.);
#9804=ORIENTED_EDGE('',*,*,#6674,.T.);
#9805=ORIENTED_EDGE('',*,*,#6669,.T.);
#9806=ORIENTED_EDGE('',*,*,#6675,.T.);
#9807=ORIENTED_EDGE('',*,*,#6676,.F.);
#9808=ORIENTED_EDGE('',*,*,#6677,.T.);
#9809=ORIENTED_EDGE('',*,*,#6673,.T.);
#9810=ORIENTED_EDGE('',*,*,#6678,.T.);
#9811=ORIENTED_EDGE('',*,*,#6679,.F.);
#9812=ORIENTED_EDGE('',*,*,#6680,.T.);
#9813=ORIENTED_EDGE('',*,*,#6676,.T.);
#9814=ORIENTED_EDGE('',*,*,#6681,.T.);
#9815=ORIENTED_EDGE('',*,*,#6682,.F.);
#9816=ORIENTED_EDGE('',*,*,#6683,.T.);
#9817=ORIENTED_EDGE('',*,*,#6679,.T.);
#9818=ORIENTED_EDGE('',*,*,#6684,.T.);
#9819=ORIENTED_EDGE('',*,*,#6685,.F.);
#9820=ORIENTED_EDGE('',*,*,#6686,.T.);
#9821=ORIENTED_EDGE('',*,*,#6682,.T.);
#9822=ORIENTED_EDGE('',*,*,#6687,.T.);
#9823=ORIENTED_EDGE('',*,*,#6688,.F.);
#9824=ORIENTED_EDGE('',*,*,#6689,.T.);
#9825=ORIENTED_EDGE('',*,*,#6685,.T.);
#9826=ORIENTED_EDGE('',*,*,#6690,.T.);
#9827=ORIENTED_EDGE('',*,*,#6691,.F.);
#9828=ORIENTED_EDGE('',*,*,#6692,.T.);
#9829=ORIENTED_EDGE('',*,*,#6688,.T.);
#9830=ORIENTED_EDGE('',*,*,#6693,.T.);
#9831=ORIENTED_EDGE('',*,*,#6694,.F.);
#9832=ORIENTED_EDGE('',*,*,#6695,.T.);
#9833=ORIENTED_EDGE('',*,*,#6691,.T.);
#9834=ORIENTED_EDGE('',*,*,#6696,.T.);
#9835=ORIENTED_EDGE('',*,*,#6697,.F.);
#9836=ORIENTED_EDGE('',*,*,#6698,.T.);
#9837=ORIENTED_EDGE('',*,*,#6694,.T.);
#9838=ORIENTED_EDGE('',*,*,#6699,.T.);
#9839=ORIENTED_EDGE('',*,*,#6700,.F.);
#9840=ORIENTED_EDGE('',*,*,#6701,.T.);
#9841=ORIENTED_EDGE('',*,*,#6697,.T.);
#9842=ORIENTED_EDGE('',*,*,#6702,.T.);
#9843=ORIENTED_EDGE('',*,*,#6703,.F.);
#9844=ORIENTED_EDGE('',*,*,#6704,.T.);
#9845=ORIENTED_EDGE('',*,*,#6700,.T.);
#9846=ORIENTED_EDGE('',*,*,#6705,.T.);
#9847=ORIENTED_EDGE('',*,*,#6706,.F.);
#9848=ORIENTED_EDGE('',*,*,#6707,.T.);
#9849=ORIENTED_EDGE('',*,*,#6703,.T.);
#9850=ORIENTED_EDGE('',*,*,#6708,.T.);
#9851=ORIENTED_EDGE('',*,*,#6709,.F.);
#9852=ORIENTED_EDGE('',*,*,#6710,.T.);
#9853=ORIENTED_EDGE('',*,*,#6706,.T.);
#9854=ORIENTED_EDGE('',*,*,#6711,.T.);
#9855=ORIENTED_EDGE('',*,*,#6712,.F.);
#9856=ORIENTED_EDGE('',*,*,#6713,.T.);
#9857=ORIENTED_EDGE('',*,*,#6709,.T.);
#9858=ORIENTED_EDGE('',*,*,#6714,.T.);
#9859=ORIENTED_EDGE('',*,*,#6715,.F.);
#9860=ORIENTED_EDGE('',*,*,#6716,.T.);
#9861=ORIENTED_EDGE('',*,*,#6712,.T.);
#9862=ORIENTED_EDGE('',*,*,#6717,.T.);
#9863=ORIENTED_EDGE('',*,*,#6718,.F.);
#9864=ORIENTED_EDGE('',*,*,#6719,.T.);
#9865=ORIENTED_EDGE('',*,*,#6715,.T.);
#9866=ORIENTED_EDGE('',*,*,#6720,.T.);
#9867=ORIENTED_EDGE('',*,*,#6721,.F.);
#9868=ORIENTED_EDGE('',*,*,#6722,.T.);
#9869=ORIENTED_EDGE('',*,*,#6718,.T.);
#9870=ORIENTED_EDGE('',*,*,#6723,.T.);
#9871=ORIENTED_EDGE('',*,*,#6724,.F.);
#9872=ORIENTED_EDGE('',*,*,#6725,.T.);
#9873=ORIENTED_EDGE('',*,*,#6726,.T.);
#9874=ORIENTED_EDGE('',*,*,#6727,.F.);
#9875=ORIENTED_EDGE('',*,*,#6728,.F.);
#9876=ORIENTED_EDGE('',*,*,#6729,.T.);
#9877=ORIENTED_EDGE('',*,*,#6724,.T.);
#9878=ORIENTED_EDGE('',*,*,#6730,.F.);
#9879=ORIENTED_EDGE('',*,*,#6731,.F.);
#9880=ORIENTED_EDGE('',*,*,#6732,.T.);
#9881=ORIENTED_EDGE('',*,*,#6728,.T.);
#9882=ORIENTED_EDGE('',*,*,#6733,.F.);
#9883=ORIENTED_EDGE('',*,*,#6734,.F.);
#9884=ORIENTED_EDGE('',*,*,#6735,.T.);
#9885=ORIENTED_EDGE('',*,*,#6731,.T.);
#9886=ORIENTED_EDGE('',*,*,#6736,.F.);
#9887=ORIENTED_EDGE('',*,*,#6737,.F.);
#9888=ORIENTED_EDGE('',*,*,#6738,.T.);
#9889=ORIENTED_EDGE('',*,*,#6734,.T.);
#9890=ORIENTED_EDGE('',*,*,#6739,.F.);
#9891=ORIENTED_EDGE('',*,*,#6740,.F.);
#9892=ORIENTED_EDGE('',*,*,#6741,.T.);
#9893=ORIENTED_EDGE('',*,*,#6737,.T.);
#9894=ORIENTED_EDGE('',*,*,#6742,.F.);
#9895=ORIENTED_EDGE('',*,*,#6743,.F.);
#9896=ORIENTED_EDGE('',*,*,#6744,.T.);
#9897=ORIENTED_EDGE('',*,*,#6740,.T.);
#9898=ORIENTED_EDGE('',*,*,#6745,.F.);
#9899=ORIENTED_EDGE('',*,*,#6746,.F.);
#9900=ORIENTED_EDGE('',*,*,#6747,.T.);
#9901=ORIENTED_EDGE('',*,*,#6743,.T.);
#9902=ORIENTED_EDGE('',*,*,#6748,.F.);
#9903=ORIENTED_EDGE('',*,*,#6749,.F.);
#9904=ORIENTED_EDGE('',*,*,#6750,.T.);
#9905=ORIENTED_EDGE('',*,*,#6746,.T.);
#9906=ORIENTED_EDGE('',*,*,#6751,.F.);
#9907=ORIENTED_EDGE('',*,*,#6752,.F.);
#9908=ORIENTED_EDGE('',*,*,#6753,.T.);
#9909=ORIENTED_EDGE('',*,*,#6749,.T.);
#9910=ORIENTED_EDGE('',*,*,#6754,.F.);
#9911=ORIENTED_EDGE('',*,*,#6755,.F.);
#9912=ORIENTED_EDGE('',*,*,#6756,.T.);
#9913=ORIENTED_EDGE('',*,*,#6752,.T.);
#9914=ORIENTED_EDGE('',*,*,#6757,.F.);
#9915=ORIENTED_EDGE('',*,*,#6758,.F.);
#9916=ORIENTED_EDGE('',*,*,#6759,.T.);
#9917=ORIENTED_EDGE('',*,*,#6755,.T.);
#9918=ORIENTED_EDGE('',*,*,#6760,.F.);
#9919=ORIENTED_EDGE('',*,*,#6761,.F.);
#9920=ORIENTED_EDGE('',*,*,#6762,.T.);
#9921=ORIENTED_EDGE('',*,*,#6758,.T.);
#9922=ORIENTED_EDGE('',*,*,#6763,.F.);
#9923=ORIENTED_EDGE('',*,*,#6764,.F.);
#9924=ORIENTED_EDGE('',*,*,#6765,.T.);
#9925=ORIENTED_EDGE('',*,*,#6761,.T.);
#9926=ORIENTED_EDGE('',*,*,#6766,.F.);
#9927=ORIENTED_EDGE('',*,*,#6767,.F.);
#9928=ORIENTED_EDGE('',*,*,#6768,.T.);
#9929=ORIENTED_EDGE('',*,*,#6764,.T.);
#9930=ORIENTED_EDGE('',*,*,#6769,.F.);
#9931=ORIENTED_EDGE('',*,*,#6770,.F.);
#9932=ORIENTED_EDGE('',*,*,#6771,.T.);
#9933=ORIENTED_EDGE('',*,*,#6767,.T.);
#9934=ORIENTED_EDGE('',*,*,#6772,.F.);
#9935=ORIENTED_EDGE('',*,*,#6773,.F.);
#9936=ORIENTED_EDGE('',*,*,#6774,.T.);
#9937=ORIENTED_EDGE('',*,*,#6770,.T.);
#9938=ORIENTED_EDGE('',*,*,#6775,.F.);
#9939=ORIENTED_EDGE('',*,*,#6776,.F.);
#9940=ORIENTED_EDGE('',*,*,#6777,.T.);
#9941=ORIENTED_EDGE('',*,*,#6773,.T.);
#9942=ORIENTED_EDGE('',*,*,#6778,.F.);
#9943=ORIENTED_EDGE('',*,*,#6779,.F.);
#9944=ORIENTED_EDGE('',*,*,#6726,.F.);
#9945=ORIENTED_EDGE('',*,*,#6780,.F.);
#9946=ORIENTED_EDGE('',*,*,#6781,.F.);
#9947=ORIENTED_EDGE('',*,*,#6782,.F.);
#9948=ORIENTED_EDGE('',*,*,#6783,.T.);
#9949=ORIENTED_EDGE('',*,*,#6784,.F.);
#9950=ORIENTED_EDGE('',*,*,#6783,.F.);
#9951=ORIENTED_EDGE('',*,*,#6780,.T.);
#9952=ORIENTED_EDGE('',*,*,#6725,.F.);
#9953=ORIENTED_EDGE('',*,*,#6729,.F.);
#9954=ORIENTED_EDGE('',*,*,#6732,.F.);
#9955=ORIENTED_EDGE('',*,*,#6735,.F.);
#9956=ORIENTED_EDGE('',*,*,#6738,.F.);
#9957=ORIENTED_EDGE('',*,*,#6741,.F.);
#9958=ORIENTED_EDGE('',*,*,#6744,.F.);
#9959=ORIENTED_EDGE('',*,*,#6747,.F.);
#9960=ORIENTED_EDGE('',*,*,#6750,.F.);
#9961=ORIENTED_EDGE('',*,*,#6753,.F.);
#9962=ORIENTED_EDGE('',*,*,#6756,.F.);
#9963=ORIENTED_EDGE('',*,*,#6759,.F.);
#9964=ORIENTED_EDGE('',*,*,#6762,.F.);
#9965=ORIENTED_EDGE('',*,*,#6765,.F.);
#9966=ORIENTED_EDGE('',*,*,#6768,.F.);
#9967=ORIENTED_EDGE('',*,*,#6771,.F.);
#9968=ORIENTED_EDGE('',*,*,#6774,.F.);
#9969=ORIENTED_EDGE('',*,*,#6777,.F.);
#9970=ORIENTED_EDGE('',*,*,#6785,.F.);
#9971=ORIENTED_EDGE('',*,*,#6786,.F.);
#9972=ORIENTED_EDGE('',*,*,#6670,.F.);
#9973=ORIENTED_EDGE('',*,*,#6674,.F.);
#9974=ORIENTED_EDGE('',*,*,#6677,.F.);
#9975=ORIENTED_EDGE('',*,*,#6680,.F.);
#9976=ORIENTED_EDGE('',*,*,#6683,.F.);
#9977=ORIENTED_EDGE('',*,*,#6686,.F.);
#9978=ORIENTED_EDGE('',*,*,#6689,.F.);
#9979=ORIENTED_EDGE('',*,*,#6692,.F.);
#9980=ORIENTED_EDGE('',*,*,#6695,.F.);
#9981=ORIENTED_EDGE('',*,*,#6698,.F.);
#9982=ORIENTED_EDGE('',*,*,#6701,.F.);
#9983=ORIENTED_EDGE('',*,*,#6704,.F.);
#9984=ORIENTED_EDGE('',*,*,#6707,.F.);
#9985=ORIENTED_EDGE('',*,*,#6710,.F.);
#9986=ORIENTED_EDGE('',*,*,#6713,.F.);
#9987=ORIENTED_EDGE('',*,*,#6716,.F.);
#9988=ORIENTED_EDGE('',*,*,#6719,.F.);
#9989=ORIENTED_EDGE('',*,*,#6722,.F.);
#9990=ORIENTED_EDGE('',*,*,#6787,.F.);
#9991=ORIENTED_EDGE('',*,*,#6776,.T.);
#9992=ORIENTED_EDGE('',*,*,#6788,.F.);
#9993=ORIENTED_EDGE('',*,*,#6789,.F.);
#9994=ORIENTED_EDGE('',*,*,#6785,.T.);
#9995=ORIENTED_EDGE('',*,*,#6779,.T.);
#9996=ORIENTED_EDGE('',*,*,#6782,.T.);
#9997=ORIENTED_EDGE('',*,*,#6790,.F.);
#9998=ORIENTED_EDGE('',*,*,#6723,.F.);
#9999=ORIENTED_EDGE('',*,*,#6720,.F.);
#10000=ORIENTED_EDGE('',*,*,#6717,.F.);
#10001=ORIENTED_EDGE('',*,*,#6714,.F.);
#10002=ORIENTED_EDGE('',*,*,#6711,.F.);
#10003=ORIENTED_EDGE('',*,*,#6708,.F.);
#10004=ORIENTED_EDGE('',*,*,#6705,.F.);
#10005=ORIENTED_EDGE('',*,*,#6702,.F.);
#10006=ORIENTED_EDGE('',*,*,#6699,.F.);
#10007=ORIENTED_EDGE('',*,*,#6696,.F.);
#10008=ORIENTED_EDGE('',*,*,#6693,.F.);
#10009=ORIENTED_EDGE('',*,*,#6690,.F.);
#10010=ORIENTED_EDGE('',*,*,#6687,.F.);
#10011=ORIENTED_EDGE('',*,*,#6684,.F.);
#10012=ORIENTED_EDGE('',*,*,#6681,.F.);
#10013=ORIENTED_EDGE('',*,*,#6678,.F.);
#10014=ORIENTED_EDGE('',*,*,#6675,.F.);
#10015=ORIENTED_EDGE('',*,*,#6672,.F.);
#10016=ORIENTED_EDGE('',*,*,#6791,.F.);
#10017=ORIENTED_EDGE('',*,*,#6788,.T.);
#10018=ORIENTED_EDGE('',*,*,#6778,.T.);
#10019=ORIENTED_EDGE('',*,*,#6775,.T.);
#10020=ORIENTED_EDGE('',*,*,#6772,.T.);
#10021=ORIENTED_EDGE('',*,*,#6769,.T.);
#10022=ORIENTED_EDGE('',*,*,#6766,.T.);
#10023=ORIENTED_EDGE('',*,*,#6763,.T.);
#10024=ORIENTED_EDGE('',*,*,#6760,.T.);
#10025=ORIENTED_EDGE('',*,*,#6757,.T.);
#10026=ORIENTED_EDGE('',*,*,#6754,.T.);
#10027=ORIENTED_EDGE('',*,*,#6751,.T.);
#10028=ORIENTED_EDGE('',*,*,#6748,.T.);
#10029=ORIENTED_EDGE('',*,*,#6745,.T.);
#10030=ORIENTED_EDGE('',*,*,#6742,.T.);
#10031=ORIENTED_EDGE('',*,*,#6739,.T.);
#10032=ORIENTED_EDGE('',*,*,#6736,.T.);
#10033=ORIENTED_EDGE('',*,*,#6733,.T.);
#10034=ORIENTED_EDGE('',*,*,#6730,.T.);
#10035=ORIENTED_EDGE('',*,*,#6727,.T.);
#10036=ORIENTED_EDGE('',*,*,#6721,.T.);
#10037=ORIENTED_EDGE('',*,*,#6790,.T.);
#10038=ORIENTED_EDGE('',*,*,#6781,.T.);
#10039=ORIENTED_EDGE('',*,*,#6787,.T.);
#10040=ORIENTED_EDGE('',*,*,#6792,.F.);
#10041=ORIENTED_EDGE('',*,*,#6793,.T.);
#10042=ORIENTED_EDGE('',*,*,#6794,.T.);
#10043=ORIENTED_EDGE('',*,*,#6795,.F.);
#10044=ORIENTED_EDGE('',*,*,#6796,.F.);
#10045=ORIENTED_EDGE('',*,*,#6797,.T.);
#10046=ORIENTED_EDGE('',*,*,#6798,.T.);
#10047=ORIENTED_EDGE('',*,*,#6793,.F.);
#10048=ORIENTED_EDGE('',*,*,#6799,.F.);
#10049=ORIENTED_EDGE('',*,*,#6800,.T.);
#10050=ORIENTED_EDGE('',*,*,#6801,.T.);
#10051=ORIENTED_EDGE('',*,*,#6797,.F.);
#10052=ORIENTED_EDGE('',*,*,#6802,.F.);
#10053=ORIENTED_EDGE('',*,*,#6803,.T.);
#10054=ORIENTED_EDGE('',*,*,#6804,.T.);
#10055=ORIENTED_EDGE('',*,*,#6800,.F.);
#10056=ORIENTED_EDGE('',*,*,#6805,.F.);
#10057=ORIENTED_EDGE('',*,*,#6806,.T.);
#10058=ORIENTED_EDGE('',*,*,#6807,.T.);
#10059=ORIENTED_EDGE('',*,*,#6803,.F.);
#10060=ORIENTED_EDGE('',*,*,#6808,.F.);
#10061=ORIENTED_EDGE('',*,*,#6795,.T.);
#10062=ORIENTED_EDGE('',*,*,#6809,.T.);
#10063=ORIENTED_EDGE('',*,*,#6806,.F.);
#10064=ORIENTED_EDGE('',*,*,#6809,.F.);
#10065=ORIENTED_EDGE('',*,*,#6794,.F.);
#10066=ORIENTED_EDGE('',*,*,#6798,.F.);
#10067=ORIENTED_EDGE('',*,*,#6801,.F.);
#10068=ORIENTED_EDGE('',*,*,#6804,.F.);
#10069=ORIENTED_EDGE('',*,*,#6807,.F.);
#10070=ORIENTED_EDGE('',*,*,#6810,.T.);
#10071=ORIENTED_EDGE('',*,*,#6786,.T.);
#10072=ORIENTED_EDGE('',*,*,#6789,.T.);
#10073=ORIENTED_EDGE('',*,*,#6791,.T.);
#10074=ORIENTED_EDGE('',*,*,#6671,.F.);
#10075=ORIENTED_EDGE('',*,*,#6810,.F.);
#10076=ORIENTED_EDGE('',*,*,#6811,.T.);
#10077=ORIENTED_EDGE('',*,*,#6812,.T.);
#10078=ORIENTED_EDGE('',*,*,#6811,.F.);
#10079=ORIENTED_EDGE('',*,*,#6812,.F.);
#10080=ORIENTED_EDGE('',*,*,#6792,.T.);
#10081=ORIENTED_EDGE('',*,*,#6808,.T.);
#10082=ORIENTED_EDGE('',*,*,#6805,.T.);
#10083=ORIENTED_EDGE('',*,*,#6802,.T.);
#10084=ORIENTED_EDGE('',*,*,#6799,.T.);
#10085=ORIENTED_EDGE('',*,*,#6796,.T.);
#10086=ORIENTED_EDGE('',*,*,#6784,.T.);
#10563=CYLINDRICAL_SURFACE('',#12150,0.14635);
#10564=CYLINDRICAL_SURFACE('',#12152,0.14635);
#10565=CYLINDRICAL_SURFACE('',#12153,0.14635);
#10566=CYLINDRICAL_SURFACE('',#12154,0.14635);
#10567=CYLINDRICAL_SURFACE('',#12155,0.14635);
#10568=CYLINDRICAL_SURFACE('',#12156,0.14635);
#10569=CYLINDRICAL_SURFACE('',#12157,0.14635);
#10570=CYLINDRICAL_SURFACE('',#12158,0.14635);
#10571=CYLINDRICAL_SURFACE('',#12159,0.14635);
#10572=CYLINDRICAL_SURFACE('',#12160,0.14635);
#10573=CYLINDRICAL_SURFACE('',#12161,0.14635);
#10574=CYLINDRICAL_SURFACE('',#12162,0.14635);
#10575=CYLINDRICAL_SURFACE('',#12163,0.14635);
#10576=CYLINDRICAL_SURFACE('',#12164,0.14635);
#10577=CYLINDRICAL_SURFACE('',#12165,0.14635);
#10578=CYLINDRICAL_SURFACE('',#12166,0.14635);
#10579=CYLINDRICAL_SURFACE('',#12167,0.14635);
#10580=CYLINDRICAL_SURFACE('',#12168,0.14635);
#10581=CYLINDRICAL_SURFACE('',#12169,0.117775);
#10582=CYLINDRICAL_SURFACE('',#12171,0.117775);
#10583=CYLINDRICAL_SURFACE('',#12172,0.117775);
#10584=CYLINDRICAL_SURFACE('',#12173,0.117775);
#10585=CYLINDRICAL_SURFACE('',#12174,0.117775);
#10586=CYLINDRICAL_SURFACE('',#12175,0.117775);
#10587=CYLINDRICAL_SURFACE('',#12176,0.117775);
#10588=CYLINDRICAL_SURFACE('',#12177,0.117775);
#10589=CYLINDRICAL_SURFACE('',#12178,0.117775);
#10590=CYLINDRICAL_SURFACE('',#12179,0.117775);
#10591=CYLINDRICAL_SURFACE('',#12180,0.117775);
#10592=CYLINDRICAL_SURFACE('',#12181,0.117775);
#10593=CYLINDRICAL_SURFACE('',#12182,0.117775);
#10594=CYLINDRICAL_SURFACE('',#12183,0.117775);
#10595=CYLINDRICAL_SURFACE('',#12184,0.117775);
#10596=CYLINDRICAL_SURFACE('',#12185,0.117775);
#10597=CYLINDRICAL_SURFACE('',#12186,0.117775);
#10598=CYLINDRICAL_SURFACE('',#12187,0.117775);
#10599=CYLINDRICAL_SURFACE('',#12191,0.117775);
#10600=CYLINDRICAL_SURFACE('',#12193,0.14635);
#10601=CYLINDRICAL_SURFACE('',#12203,0.3);
#11159=ADVANCED_FACE('',(#1034),#10563,.T.);
#11160=ADVANCED_FACE('',(#1035),#10564,.T.);
#11161=ADVANCED_FACE('',(#1036),#10565,.T.);
#11162=ADVANCED_FACE('',(#1037),#10566,.T.);
#11163=ADVANCED_FACE('',(#1038),#10567,.T.);
#11164=ADVANCED_FACE('',(#1039),#10568,.T.);
#11165=ADVANCED_FACE('',(#1040),#10569,.T.);
#11166=ADVANCED_FACE('',(#1041),#10570,.T.);
#11167=ADVANCED_FACE('',(#1042),#10571,.T.);
#11168=ADVANCED_FACE('',(#1043),#10572,.T.);
#11169=ADVANCED_FACE('',(#1044),#10573,.T.);
#11170=ADVANCED_FACE('',(#1045),#10574,.T.);
#11171=ADVANCED_FACE('',(#1046),#10575,.T.);
#11172=ADVANCED_FACE('',(#1047),#10576,.T.);
#11173=ADVANCED_FACE('',(#1048),#10577,.T.);
#11174=ADVANCED_FACE('',(#1049),#10578,.T.);
#11175=ADVANCED_FACE('',(#1050),#10579,.T.);
#11176=ADVANCED_FACE('',(#1051),#10580,.T.);
#11177=ADVANCED_FACE('',(#1052),#10581,.T.);
#11178=ADVANCED_FACE('',(#1053),#10582,.T.);
#11179=ADVANCED_FACE('',(#1054),#10583,.T.);
#11180=ADVANCED_FACE('',(#1055),#10584,.T.);
#11181=ADVANCED_FACE('',(#1056),#10585,.T.);
#11182=ADVANCED_FACE('',(#1057),#10586,.T.);
#11183=ADVANCED_FACE('',(#1058),#10587,.T.);
#11184=ADVANCED_FACE('',(#1059),#10588,.T.);
#11185=ADVANCED_FACE('',(#1060),#10589,.T.);
#11186=ADVANCED_FACE('',(#1061),#10590,.T.);
#11187=ADVANCED_FACE('',(#1062),#10591,.T.);
#11188=ADVANCED_FACE('',(#1063),#10592,.T.);
#11189=ADVANCED_FACE('',(#1064),#10593,.T.);
#11190=ADVANCED_FACE('',(#1065),#10594,.T.);
#11191=ADVANCED_FACE('',(#1066),#10595,.T.);
#11192=ADVANCED_FACE('',(#1067),#10596,.T.);
#11193=ADVANCED_FACE('',(#1068),#10597,.T.);
#11194=ADVANCED_FACE('',(#1069),#10598,.T.);
#11195=ADVANCED_FACE('',(#1070),#149,.T.);
#11196=ADVANCED_FACE('',(#1071),#254,.F.);
#11197=ADVANCED_FACE('',(#1072),#10599,.T.);
#11198=ADVANCED_FACE('',(#1073),#255,.F.);
#11199=ADVANCED_FACE('',(#1074),#10600,.T.);
#11200=ADVANCED_FACE('',(#1075),#464,.F.);
#11201=ADVANCED_FACE('',(#1076),#465,.F.);
#11202=ADVANCED_FACE('',(#1077),#466,.F.);
#11203=ADVANCED_FACE('',(#1078),#467,.F.);
#11204=ADVANCED_FACE('',(#1079),#468,.F.);
#11205=ADVANCED_FACE('',(#1080),#469,.F.);
#11206=ADVANCED_FACE('',(#1081),#470,.F.);
#11207=ADVANCED_FACE('',(#1082,#327),#471,.T.);
#11208=ADVANCED_FACE('',(#1083),#10601,.T.);
#11209=ADVANCED_FACE('',(#1084,#328),#472,.F.);
#11210=ADVANCED_FACE('',(#1085),#473,.T.);
#11246=CLOSED_SHELL('',(#11159,#11160,#11161,#11162,#11163,#11164,#11165,
#11166,#11167,#11168,#11169,#11170,#11171,#11172,#11173,#11174,#11175,#11176,
#11177,#11178,#11179,#11180,#11181,#11182,#11183,#11184,#11185,#11186,#11187,
#11188,#11189,#11190,#11191,#11192,#11193,#11194,#11195,#11196,#11197,#11198,
#11199,#11200,#11201,#11202,#11203,#11204,#11205,#11206,#11207,#11208,#11209,
#11210));
#12149=AXIS2_PLACEMENT_3D('',#40446,#14245,#14246);
#12150=AXIS2_PLACEMENT_3D('',#40447,#14247,#14248);
#12151=AXIS2_PLACEMENT_3D('',#40463,#14250,#14251);
#12152=AXIS2_PLACEMENT_3D('',#40471,#14252,#14253);
#12153=AXIS2_PLACEMENT_3D('',#40519,#14255,#14256);
#12154=AXIS2_PLACEMENT_3D('',#40567,#14258,#14259);
#12155=AXIS2_PLACEMENT_3D('',#40621,#14261,#14262);
#12156=AXIS2_PLACEMENT_3D('',#40669,#14264,#14265);
#12157=AXIS2_PLACEMENT_3D('',#40717,#14267,#14268);
#12158=AXIS2_PLACEMENT_3D('',#40771,#14270,#14271);
#12159=AXIS2_PLACEMENT_3D('',#40819,#14273,#14274);
#12160=AXIS2_PLACEMENT_3D('',#40867,#14276,#14277);
#12161=AXIS2_PLACEMENT_3D('',#40921,#14279,#14280);
#12162=AXIS2_PLACEMENT_3D('',#40969,#14282,#14283);
#12163=AXIS2_PLACEMENT_3D('',#41017,#14285,#14286);
#12164=AXIS2_PLACEMENT_3D('',#41071,#14288,#14289);
#12165=AXIS2_PLACEMENT_3D('',#41119,#14291,#14292);
#12166=AXIS2_PLACEMENT_3D('',#41167,#14294,#14295);
#12167=AXIS2_PLACEMENT_3D('',#41218,#14297,#14298);
#12168=AXIS2_PLACEMENT_3D('',#41266,#14300,#14301);
#12169=AXIS2_PLACEMENT_3D('',#41314,#14303,#14304);
#12170=AXIS2_PLACEMENT_3D('',#41330,#14306,#14307);
#12171=AXIS2_PLACEMENT_3D('',#41340,#14308,#14309);
#12172=AXIS2_PLACEMENT_3D('',#41364,#14311,#14312);
#12173=AXIS2_PLACEMENT_3D('',#41388,#14314,#14315);
#12174=AXIS2_PLACEMENT_3D('',#41414,#14317,#14318);
#12175=AXIS2_PLACEMENT_3D('',#41438,#14320,#14321);
#12176=AXIS2_PLACEMENT_3D('',#41462,#14323,#14324);
#12177=AXIS2_PLACEMENT_3D('',#41487,#14326,#14327);
#12178=AXIS2_PLACEMENT_3D('',#41512,#14329,#14330);
#12179=AXIS2_PLACEMENT_3D('',#41536,#14332,#14333);
#12180=AXIS2_PLACEMENT_3D('',#41561,#14335,#14336);
#12181=AXIS2_PLACEMENT_3D('',#41586,#14338,#14339);
#12182=AXIS2_PLACEMENT_3D('',#41610,#14341,#14342);
#12183=AXIS2_PLACEMENT_3D('',#41635,#14344,#14345);
#12184=AXIS2_PLACEMENT_3D('',#41660,#14347,#14348);
#12185=AXIS2_PLACEMENT_3D('',#41684,#14350,#14351);
#12186=AXIS2_PLACEMENT_3D('',#41709,#14353,#14354);
#12187=AXIS2_PLACEMENT_3D('',#41734,#14356,#14357);
#12188=AXIS2_PLACEMENT_3D('',#41758,#14359,#14360);
#12189=AXIS2_PLACEMENT_3D('',#41917,#14361,#14362);
#12190=AXIS2_PLACEMENT_3D('',#41936,#14364,#14365);
#12191=AXIS2_PLACEMENT_3D('',#42504,#14366,#14367);
#12192=AXIS2_PLACEMENT_3D('',#42515,#14368,#14369);
#12193=AXIS2_PLACEMENT_3D('',#43082,#14370,#14371);
#12194=AXIS2_PLACEMENT_3D('',#43083,#14372,#14373);
#12195=AXIS2_PLACEMENT_3D('',#43092,#14378,#14379);
#12196=AXIS2_PLACEMENT_3D('',#43098,#14383,#14384);
#12197=AXIS2_PLACEMENT_3D('',#43104,#14388,#14389);
#12198=AXIS2_PLACEMENT_3D('',#43110,#14393,#14394);
#12199=AXIS2_PLACEMENT_3D('',#43116,#14398,#14399);
#12200=AXIS2_PLACEMENT_3D('',#43119,#14402,#14403);
#12201=AXIS2_PLACEMENT_3D('',#43120,#14404,#14405);
#12202=AXIS2_PLACEMENT_3D('',#43122,#14406,#14407);
#12203=AXIS2_PLACEMENT_3D('',#43123,#14408,#14409);
#12204=AXIS2_PLACEMENT_3D('',#43126,#14411,#14412);
#12205=AXIS2_PLACEMENT_3D('',#43127,#14413,#14414);
#12206=AXIS2_PLACEMENT_3D('',#43128,#14415,#14416);
#14245=DIRECTION('axis',(0.,0.,1.));
#14246=DIRECTION('refdir',(1.,0.,0.));
#14247=DIRECTION('center_axis',(0.,0.,1.));
#14248=DIRECTION('ref_axis',(1.,0.,0.));
#14249=DIRECTION('',(0.,0.,-1.));
#14250=DIRECTION('center_axis',(0.,0.,-1.));
#14251=DIRECTION('ref_axis',(1.,0.,0.));
#14252=DIRECTION('center_axis',(0.,0.,1.));
#14253=DIRECTION('ref_axis',(1.,0.,0.));
#14254=DIRECTION('',(0.,0.,-1.));
#14255=DIRECTION('center_axis',(0.,0.,1.));
#14256=DIRECTION('ref_axis',(1.,0.,0.));
#14257=DIRECTION('',(0.,0.,-1.));
#14258=DIRECTION('center_axis',(0.,0.,1.));
#14259=DIRECTION('ref_axis',(1.,0.,0.));
#14260=DIRECTION('',(0.,0.,-1.));
#14261=DIRECTION('center_axis',(0.,0.,1.));
#14262=DIRECTION('ref_axis',(1.,0.,0.));
#14263=DIRECTION('',(0.,0.,-1.));
#14264=DIRECTION('center_axis',(0.,0.,1.));
#14265=DIRECTION('ref_axis',(1.,0.,0.));
#14266=DIRECTION('',(0.,0.,-1.));
#14267=DIRECTION('center_axis',(0.,0.,1.));
#14268=DIRECTION('ref_axis',(1.,0.,0.));
#14269=DIRECTION('',(0.,0.,-1.));
#14270=DIRECTION('center_axis',(0.,0.,1.));
#14271=DIRECTION('ref_axis',(1.,0.,0.));
#14272=DIRECTION('',(0.,0.,-1.));
#14273=DIRECTION('center_axis',(0.,0.,1.));
#14274=DIRECTION('ref_axis',(1.,0.,0.));
#14275=DIRECTION('',(0.,0.,-1.));
#14276=DIRECTION('center_axis',(0.,0.,1.));
#14277=DIRECTION('ref_axis',(1.,0.,0.));
#14278=DIRECTION('',(0.,0.,-1.));
#14279=DIRECTION('center_axis',(0.,0.,1.));
#14280=DIRECTION('ref_axis',(1.,0.,0.));
#14281=DIRECTION('',(0.,0.,-1.));
#14282=DIRECTION('center_axis',(0.,0.,1.));
#14283=DIRECTION('ref_axis',(1.,0.,0.));
#14284=DIRECTION('',(0.,0.,-1.));
#14285=DIRECTION('center_axis',(0.,0.,1.));
#14286=DIRECTION('ref_axis',(1.,0.,0.));
#14287=DIRECTION('',(0.,0.,-1.));
#14288=DIRECTION('center_axis',(0.,0.,1.));
#14289=DIRECTION('ref_axis',(1.,0.,0.));
#14290=DIRECTION('',(0.,0.,-1.));
#14291=DIRECTION('center_axis',(0.,0.,1.));
#14292=DIRECTION('ref_axis',(1.,0.,0.));
#14293=DIRECTION('',(0.,0.,-1.));
#14294=DIRECTION('center_axis',(0.,0.,1.));
#14295=DIRECTION('ref_axis',(1.,0.,0.));
#14296=DIRECTION('',(0.,0.,-1.));
#14297=DIRECTION('center_axis',(0.,0.,1.));
#14298=DIRECTION('ref_axis',(1.,0.,0.));
#14299=DIRECTION('',(0.,0.,-1.));
#14300=DIRECTION('center_axis',(0.,0.,1.));
#14301=DIRECTION('ref_axis',(1.,0.,0.));
#14302=DIRECTION('',(0.,0.,-1.));
#14303=DIRECTION('center_axis',(0.,0.,1.));
#14304=DIRECTION('ref_axis',(1.,1.10671505702589E-13,0.));
#14305=DIRECTION('',(0.,0.,1.));
#14306=DIRECTION('center_axis',(0.,0.,-1.));
#14307=DIRECTION('ref_axis',(1.,1.10671505702589E-13,0.));
#14308=DIRECTION('center_axis',(0.,0.,1.));
#14309=DIRECTION('ref_axis',(1.,1.10671505702589E-13,0.));
#14310=DIRECTION('',(0.,0.,1.));
#14311=DIRECTION('center_axis',(0.,0.,1.));
#14312=DIRECTION('ref_axis',(1.,1.10671505702589E-13,0.));
#14313=DIRECTION('',(0.,0.,1.));
#14314=DIRECTION('center_axis',(0.,0.,1.));
#14315=DIRECTION('ref_axis',(1.,1.10671505702589E-13,0.));
#14316=DIRECTION('',(0.,0.,1.));
#14317=DIRECTION('center_axis',(0.,0.,1.));
#14318=DIRECTION('ref_axis',(1.,1.10671505702589E-13,0.));
#14319=DIRECTION('',(0.,0.,1.));
#14320=DIRECTION('center_axis',(0.,0.,1.));
#14321=DIRECTION('ref_axis',(1.,1.10671505702589E-13,0.));
#14322=DIRECTION('',(0.,0.,1.));
#14323=DIRECTION('center_axis',(0.,0.,1.));
#14324=DIRECTION('ref_axis',(1.,1.10671505702589E-13,0.));
#14325=DIRECTION('',(0.,0.,1.));
#14326=DIRECTION('center_axis',(0.,0.,1.));
#14327=DIRECTION('ref_axis',(1.,1.10671505702589E-13,0.));
#14328=DIRECTION('',(0.,0.,1.));
#14329=DIRECTION('center_axis',(0.,0.,1.));
#14330=DIRECTION('ref_axis',(1.,1.10671505702589E-13,0.));
#14331=DIRECTION('',(0.,0.,1.));
#14332=DIRECTION('center_axis',(0.,0.,1.));
#14333=DIRECTION('ref_axis',(1.,1.10671505702589E-13,0.));
#14334=DIRECTION('',(0.,0.,1.));
#14335=DIRECTION('center_axis',(0.,0.,1.));
#14336=DIRECTION('ref_axis',(1.,1.10671505702589E-13,0.));
#14337=DIRECTION('',(0.,0.,1.));
#14338=DIRECTION('center_axis',(0.,0.,1.));
#14339=DIRECTION('ref_axis',(1.,1.10671505702589E-13,0.));
#14340=DIRECTION('',(0.,0.,1.));
#14341=DIRECTION('center_axis',(0.,0.,1.));
#14342=DIRECTION('ref_axis',(1.,1.10671505702589E-13,0.));
#14343=DIRECTION('',(0.,0.,1.));
#14344=DIRECTION('center_axis',(0.,0.,1.));
#14345=DIRECTION('ref_axis',(1.,1.10671505702589E-13,0.));
#14346=DIRECTION('',(0.,0.,1.));
#14347=DIRECTION('center_axis',(0.,0.,1.));
#14348=DIRECTION('ref_axis',(1.,1.10671505702589E-13,0.));
#14349=DIRECTION('',(0.,0.,1.));
#14350=DIRECTION('center_axis',(0.,0.,1.));
#14351=DIRECTION('ref_axis',(1.,1.10671505702589E-13,0.));
#14352=DIRECTION('',(0.,0.,1.));
#14353=DIRECTION('center_axis',(0.,0.,1.));
#14354=DIRECTION('ref_axis',(1.,1.10671505702589E-13,0.));
#14355=DIRECTION('',(0.,0.,1.));
#14356=DIRECTION('center_axis',(0.,0.,1.));
#14357=DIRECTION('ref_axis',(1.,1.10671505702589E-13,0.));
#14358=DIRECTION('',(0.,0.,1.));
#14359=DIRECTION('center_axis',(0.,0.,-1.));
#14360=DIRECTION('ref_axis',(1.,0.,0.));
#14361=DIRECTION('center_axis',(0.,0.,-1.));
#14362=DIRECTION('ref_axis',(1.,0.,0.));
#14363=DIRECTION('',(0.707106781186548,8.65956056235493E-17,0.707106781186547));
#14364=DIRECTION('center_axis',(0.,0.,1.));
#14365=DIRECTION('ref_axis',(1.,0.,0.));
#14366=DIRECTION('center_axis',(0.,0.,1.));
#14367=DIRECTION('ref_axis',(1.,1.10671505702589E-13,0.));
#14368=DIRECTION('center_axis',(0.,0.,-1.));
#14369=DIRECTION('ref_axis',(1.,1.10671505702589E-13,0.));
#14370=DIRECTION('center_axis',(0.,0.,1.));
#14371=DIRECTION('ref_axis',(1.,0.,0.));
#14372=DIRECTION('center_axis',(-2.40370335797945E-16,-1.,0.));
#14373=DIRECTION('ref_axis',(1.,-2.40370335797945E-16,0.));
#14374=DIRECTION('',(1.,-2.40370335797945E-16,0.));
#14375=DIRECTION('',(0.,0.,1.));
#14376=DIRECTION('',(1.,-2.40370335797945E-16,0.));
#14377=DIRECTION('',(0.,0.,1.));
#14378=DIRECTION('center_axis',(-0.866025403784439,-0.5,0.));
#14379=DIRECTION('ref_axis',(0.5,-0.866025403784439,0.));
#14380=DIRECTION('',(0.5,-0.866025403784439,0.));
#14381=DIRECTION('',(0.,0.,1.));
#14382=DIRECTION('',(0.5,-0.866025403784439,0.));
#14383=DIRECTION('center_axis',(-0.866025403784439,0.5,0.));
#14384=DIRECTION('ref_axis',(-0.5,-0.866025403784439,0.));
#14385=DIRECTION('',(-0.5,-0.866025403784439,0.));
#14386=DIRECTION('',(0.,0.,1.));
#14387=DIRECTION('',(-0.5,-0.866025403784439,0.));
#14388=DIRECTION('center_axis',(1.20185167898973E-16,1.,0.));
#14389=DIRECTION('ref_axis',(-1.,1.20185167898973E-16,0.));
#14390=DIRECTION('',(-1.,1.20185167898973E-16,0.));
#14391=DIRECTION('',(0.,0.,1.));
#14392=DIRECTION('',(-1.,1.20185167898973E-16,0.));
#14393=DIRECTION('center_axis',(0.866025403784439,0.5,0.));
#14394=DIRECTION('ref_axis',(-0.5,0.866025403784439,0.));
#14395=DIRECTION('',(-0.5,0.866025403784439,0.));
#14396=DIRECTION('',(0.,0.,1.));
#14397=DIRECTION('',(-0.5,0.866025403784439,0.));
#14398=DIRECTION('center_axis',(0.866025403784439,-0.5,0.));
#14399=DIRECTION('ref_axis',(0.5,0.866025403784439,0.));
#14400=DIRECTION('',(0.5,0.866025403784439,0.));
#14401=DIRECTION('',(0.5,0.866025403784439,0.));
#14402=DIRECTION('center_axis',(0.,0.,1.));
#14403=DIRECTION('ref_axis',(1.,0.,0.));
#14404=DIRECTION('center_axis',(0.,0.,1.));
#14405=DIRECTION('ref_axis',(1.,0.,0.));
#14406=DIRECTION('center_axis',(0.,0.,1.));
#14407=DIRECTION('ref_axis',(1.,0.,0.));
#14408=DIRECTION('center_axis',(0.,0.,1.));
#14409=DIRECTION('ref_axis',(1.,0.,0.));
#14410=DIRECTION('',(0.,0.,-1.));
#14411=DIRECTION('center_axis',(0.,0.,1.));
#14412=DIRECTION('ref_axis',(1.,0.,0.));
#14413=DIRECTION('center_axis',(0.,0.,1.));
#14414=DIRECTION('ref_axis',(1.,0.,0.));
#14415=DIRECTION('center_axis',(0.,0.,1.));
#14416=DIRECTION('ref_axis',(1.,0.,0.));
#40446=CARTESIAN_POINT('',(0.,0.,0.));
#40447=CARTESIAN_POINT('Origin',(0.,0.,0.));
#40448=CARTESIAN_POINT('',(-0.146500586129689,0.000104807665585484,0.0160655045842905));
#40449=CARTESIAN_POINT('',(-0.146471000393815,0.000161627070721384,0.00893449541570859));
#40450=CARTESIAN_POINT('',(-0.14635,-1.79227059055215E-17,0.));
#40451=CARTESIAN_POINT('',(0.0634007094575212,0.131904027763685,0.));
#40452=CARTESIAN_POINT('Ctrl Pts',(-0.146500586129689,0.000104807665585484,
0.0160655045842905));
#40453=CARTESIAN_POINT('Ctrl Pts',(-0.14654494062996,0.00598698351314685,
0.0157446908947048));
#40454=CARTESIAN_POINT('Ctrl Pts',(-0.146221105349753,0.0118639507829193,
0.0154238772051191));
#40455=CARTESIAN_POINT('Ctrl Pts',(-0.145512600887712,0.0176938044004412,
0.0151030635155334));
#40456=CARTESIAN_POINT('Ctrl Pts',(-0.139696831446137,0.0655482447521769,
0.0124696595607311));
#40457=CARTESIAN_POINT('Ctrl Pts',(-0.107962161373412,0.110228180545907,
0.00983625560592885));
#40458=CARTESIAN_POINT('Ctrl Pts',(-0.06469522132477,0.13152107817143,0.0072028516511266));
#40459=CARTESIAN_POINT('Ctrl Pts',(-0.0252475006917791,0.150934428781716,
0.00480190110075107));
#40460=CARTESIAN_POINT('Ctrl Pts',(0.0237864150713563,0.150907312609249,
0.00240095055037554));
#40461=CARTESIAN_POINT('Ctrl Pts',(0.0635538308725811,0.132076982143462,
1.66967134562768E-17));
#40462=CARTESIAN_POINT('',(-0.063400709457524,0.131904027763684,0.));
#40463=CARTESIAN_POINT('Origin',(0.,0.,0.));
#40464=CARTESIAN_POINT('Ctrl Pts',(-0.0634007094575239,0.131904027763684,
1.49186218934005E-16));
#40465=CARTESIAN_POINT('Ctrl Pts',(-0.107082934395073,0.110907822426531,
0.00263534106650592));
#40466=CARTESIAN_POINT('Ctrl Pts',(-0.139152358317953,0.0667027373135744,
0.00527068213301169));
#40467=CARTESIAN_POINT('Ctrl Pts',(-0.145347393378452,0.0189333151714045,
0.00790602319951745));
#40468=CARTESIAN_POINT('Ctrl Pts',(-0.146153287982764,0.0127191260377668,
0.00824884727158116));
#40469=CARTESIAN_POINT('Ctrl Pts',(-0.14652131876894,0.00644461879462582,
0.00859167134364488));
#40470=CARTESIAN_POINT('Ctrl Pts',(-0.146471000393815,0.000161627070721384,
0.00893449541570859));
#40471=CARTESIAN_POINT('Origin',(0.,0.,0.));
#40472=CARTESIAN_POINT('',(-0.146124286466753,3.81045546672121E-5,0.0660655045842905));
#40473=CARTESIAN_POINT('',(-0.146121893894205,3.63833482308178E-5,0.0589344954157087));
#40474=CARTESIAN_POINT('',(-0.14635,-1.79227059055215E-17,0.));
#40475=CARTESIAN_POINT('Ctrl Pts',(-0.146124286466753,3.81045546672121E-5,
0.0660655045842905));
#40476=CARTESIAN_POINT('Ctrl Pts',(-0.146175624225919,0.0219480700681356,
0.0648784479568517));
#40477=CARTESIAN_POINT('Ctrl Pts',(-0.141554683648142,0.0438374299905643,
0.0636913913294129));
#40478=CARTESIAN_POINT('Ctrl Pts',(-0.132150173022132,0.0634306246655632,
0.062504334701974));
#40479=CARTESIAN_POINT('Ctrl Pts',(-0.111286909296501,0.106896787232447,
0.0598709307471717));
#40480=CARTESIAN_POINT('Ctrl Pts',(-0.0668815981213141,0.139062512957816,
0.0572375267923695));
#40481=CARTESIAN_POINT('Ctrl Pts',(-0.0190775358903001,0.145337701034954,
0.0546041228375673));
#40482=CARTESIAN_POINT('Ctrl Pts',(0.028726526340714,0.151612889112092,
0.051970718882765));
#40483=CARTESIAN_POINT('Ctrl Pts',(0.0799293396275551,0.131997539540999,
0.0493373149279628));
#40484=CARTESIAN_POINT('Ctrl Pts',(0.111303508306999,0.0953874982726326,
0.0467039109731605));
#40485=CARTESIAN_POINT('Ctrl Pts',(0.142677676986443,0.0587774570042668,
0.0440705070183582));
#40486=CARTESIAN_POINT('Ctrl Pts',(0.154223201058489,0.00517272403862895,
0.041437103063556));
#40487=CARTESIAN_POINT('Ctrl Pts',(0.14070340769012,-0.0411058697401277,
0.0388036991087537));
#40488=CARTESIAN_POINT('Ctrl Pts',(0.12718361432175,-0.0873844635188848,
0.0361702951539514));
#40489=CARTESIAN_POINT('Ctrl Pts',(0.0885985035129631,-0.12633691811076,
0.0335368911991492));
#40490=CARTESIAN_POINT('Ctrl Pts',(0.0424500313328507,-0.140301337584722,
0.030903487244347));
#40491=CARTESIAN_POINT('Ctrl Pts',(-0.00369844084726173,-0.154265757058684,
0.0282700832895447));
#40492=CARTESIAN_POINT('Ctrl Pts',(-0.0574102743986997,-0.143242141414731,
0.0256366793347424));
#40493=CARTESIAN_POINT('Ctrl Pts',(-0.0943177567692062,-0.112215861137884,
0.0230032753799401));
#40494=CARTESIAN_POINT('Ctrl Pts',(-0.126728995572139,-0.0849693486522956,
0.0206906851147236));
#40495=CARTESIAN_POINT('Ctrl Pts',(-0.146180856053097,-0.0422969446440751,
0.0183780948495071));
#40496=CARTESIAN_POINT('Ctrl Pts',(-0.146500586129689,0.000104807665585484,
0.0160655045842905));
#40497=CARTESIAN_POINT('Ctrl Pts',(-0.146471000393815,0.000161627070721384,
0.00893449541570859));
#40498=CARTESIAN_POINT('Ctrl Pts',(-0.146134513724681,-0.0418536993801969,
0.0112270124101507));
#40499=CARTESIAN_POINT('Ctrl Pts',(-0.127090283331881,-0.0842484349621326,
0.0135195294045928));
#40500=CARTESIAN_POINT('Ctrl Pts',(-0.0951738980203006,-0.111522448354846,
0.0158120463990349));
#40501=CARTESIAN_POINT('Ctrl Pts',(-0.0584847214035319,-0.142875030567541,
0.0184473874655407));
#40502=CARTESIAN_POINT('Ctrl Pts',(-0.00478572197187679,-0.154246435821546,
0.0210827285320465));
#40503=CARTESIAN_POINT('Ctrl Pts',(0.0414949714453012,-0.140576153089947,
0.0237180695985523));
#40504=CARTESIAN_POINT('Ctrl Pts',(0.0877756648624791,-0.126905870358348,
0.0263534106650582));
#40505=CARTESIAN_POINT('Ctrl Pts',(0.12663805226518,-0.0881938996411451,
0.028988751731564));
#40506=CARTESIAN_POINT('Ctrl Pts',(0.140447863117085,-0.0419714582064656,
0.0316240927980698));
#40507=CARTESIAN_POINT('Ctrl Pts',(0.154257673968991,0.00425098322821388,
0.0342594338645756));
#40508=CARTESIAN_POINT('Ctrl Pts',(0.143014908270101,0.0579838953803693,
0.0368947749310814));
#40509=CARTESIAN_POINT('Ctrl Pts',(0.111816739036639,0.0947918176848183,
0.0395301159975872));
#40510=CARTESIAN_POINT('Ctrl Pts',(0.0806185698031766,0.131599739989267,
0.042165457064093));
#40511=CARTESIAN_POINT('Ctrl Pts',(0.0294649970351413,0.15148267244601,
0.0448007981305989));
#40512=CARTESIAN_POINT('Ctrl Pts',(-0.0184028717348104,0.145423626667293,
0.0474361391971047));
#40513=CARTESIAN_POINT('Ctrl Pts',(-0.0662707405047621,0.139364580888577,
0.0500714802636105));
#40514=CARTESIAN_POINT('Ctrl Pts',(-0.11085290527663,0.107363556874401,
0.0527068213301163));
#40515=CARTESIAN_POINT('Ctrl Pts',(-0.131901071754926,0.0639489919997987,
0.0553421623966221));
#40516=CARTESIAN_POINT('Ctrl Pts',(-0.141464922191872,0.0442223138744639,
0.0565396067363176));
#40517=CARTESIAN_POINT('Ctrl Pts',(-0.146169931163403,0.0221391901971212,
0.0577370510760131));
#40518=CARTESIAN_POINT('Ctrl Pts',(-0.146121893894205,3.63833482308178E-5,
0.0589344954157087));
#40519=CARTESIAN_POINT('Origin',(0.,0.,0.));
#40520=CARTESIAN_POINT('',(-0.146368002745976,-0.000129372869328834,0.116065504584291));
#40521=CARTESIAN_POINT('',(-0.146366557616609,-0.000129983413451606,0.108934495415709));
#40522=CARTESIAN_POINT('',(-0.14635,-1.79227059055215E-17,0.));
#40523=CARTESIAN_POINT('Ctrl Pts',(-0.146368002745976,-0.000129372869328834,
0.116065504584291));
#40524=CARTESIAN_POINT('Ctrl Pts',(-0.146025111950034,0.0376095209348488,
0.114012205018999));
#40525=CARTESIAN_POINT('Ctrl Pts',(-0.131097704503774,0.0755892522017571,
0.111958905453707));
#40526=CARTESIAN_POINT('Ctrl Pts',(-0.104818007194008,0.1024708903805,0.109905605888415));
#40527=CARTESIAN_POINT('Ctrl Pts',(-0.0711136904949951,0.136947210099294,
0.107272201933612));
#40528=CARTESIAN_POINT('Ctrl Pts',(-0.0187363862257596,0.153168661700715,
0.10463879797881));
#40529=CARTESIAN_POINT('Ctrl Pts',(0.0285541005041433,0.143776766284718,
0.102005394024008));
#40530=CARTESIAN_POINT('Ctrl Pts',(0.0758445872340461,0.134384870868722,
0.0993719900692057));
#40531=CARTESIAN_POINT('Ctrl Pts',(0.118048256424616,0.0993796284353078,
0.0967385861144034));
#40532=CARTESIAN_POINT('Ctrl Pts',(0.136020336225278,0.0546403479960236,
0.0941051821596012));
#40533=CARTESIAN_POINT('Ctrl Pts',(0.153992416025939,0.00990106755673973,
0.0914717782047989));
#40534=CARTESIAN_POINT('Ctrl Pts',(0.147732906436694,-0.0445722508884142,
0.0888383742499967));
#40535=CARTESIAN_POINT('Ctrl Pts',(0.120081310876684,-0.0840688974447852,
0.0862049702951944));
#40536=CARTESIAN_POINT('Ctrl Pts',(0.092429715316675,-0.123565544001157,
0.0835715663403921));
#40537=CARTESIAN_POINT('Ctrl Pts',(0.0433860337859016,-0.148085518668745,
0.0809381623855898));
#40538=CARTESIAN_POINT('Ctrl Pts',(-0.00480217723865872,-0.146506046566169,
0.0783047584307875));
#40539=CARTESIAN_POINT('Ctrl Pts',(-0.0529903882632186,-0.144926574463593,
0.0756713544759853));
#40540=CARTESIAN_POINT('Ctrl Pts',(-0.100323128781565,-0.117247655590855,
0.0730379505211831));
#40541=CARTESIAN_POINT('Ctrl Pts',(-0.125328890902702,-0.0760248964502869,
0.0704045465663809));
#40542=CARTESIAN_POINT('Ctrl Pts',(-0.139062832915904,-0.053384075469981,
0.0689581992390174));
#40543=CARTESIAN_POINT('Ctrl Pts',(-0.146061734917782,-0.0266576901787336,
0.067511851911654));
#40544=CARTESIAN_POINT('Ctrl Pts',(-0.146124286466753,3.81045546672121E-5,
0.0660655045842905));
#40545=CARTESIAN_POINT('Ctrl Pts',(-0.146121893894205,3.63833482308178E-5,
0.0589344954157087));
#40546=CARTESIAN_POINT('Ctrl Pts',(-0.146064210518155,-0.026504769812526,
0.060372392142519));
#40547=CARTESIAN_POINT('Ctrl Pts',(-0.139152958627323,-0.0530743047642348,
0.0618102888693293));
#40548=CARTESIAN_POINT('Ctrl Pts',(-0.125571320368441,-0.0756261679111494,
0.0632481855961396));
#40549=CARTESIAN_POINT('Ctrl Pts',(-0.100679234318938,-0.116958657212465,
0.0658835266626455));
#40550=CARTESIAN_POINT('Ctrl Pts',(-0.0533808940352117,-0.144795530080065,
0.0685188677291512));
#40551=CARTESIAN_POINT('Ctrl Pts',(-0.00516183231960515,-0.146494306755382,
0.071154208795657));
#40552=CARTESIAN_POINT('Ctrl Pts',(0.0430572293960016,-0.148193083430699,
0.0737895498621628));
#40553=CARTESIAN_POINT('Ctrl Pts',(0.0921970125434883,-0.123753763913733,
0.0764248909286687));
#40554=CARTESIAN_POINT('Ctrl Pts',(0.119936668638416,-0.0842765346784538,
0.0790602319951745));
#40555=CARTESIAN_POINT('Ctrl Pts',(0.147676324733344,-0.0447993054431753,
0.0816955730616803));
#40556=CARTESIAN_POINT('Ctrl Pts',(0.154015853775713,0.00971583351041531,
0.0843309141281861));
#40557=CARTESIAN_POINT('Ctrl Pts',(0.136075382627054,0.0545053485317346,
0.0869662551946919));
#40558=CARTESIAN_POINT('Ctrl Pts',(0.118134911478395,0.0992948635530542,
0.0896015962611977));
#40559=CARTESIAN_POINT('Ctrl Pts',(0.0759144401387073,0.134358754642102,
0.0922369373277035));
#40560=CARTESIAN_POINT('Ctrl Pts',(0.0285922932904845,0.143769920707126,
0.0948722783942094));
#40561=CARTESIAN_POINT('Ctrl Pts',(-0.0187298535577381,0.15318108677215,
0.0975076194607152));
#40562=CARTESIAN_POINT('Ctrl Pts',(-0.0711536759144954,0.13693952781315,
0.100142960527221));
#40563=CARTESIAN_POINT('Ctrl Pts',(-0.104866248150923,0.102422641268563,
0.102778301593727));
#40564=CARTESIAN_POINT('Ctrl Pts',(-0.131117262559492,0.0755453303453163,
0.104830366201054));
#40565=CARTESIAN_POINT('Ctrl Pts',(-0.146023101823344,0.0375871567885092,
0.106882430808381));
#40566=CARTESIAN_POINT('Ctrl Pts',(-0.146366557616609,-0.000129983413451606,
0.108934495415709));
#40567=CARTESIAN_POINT('Origin',(0.,0.,0.));
#40568=CARTESIAN_POINT('',(-0.14651736545536,8.65668654492988E-5,0.166065504584291));
#40569=CARTESIAN_POINT('',(-0.146524127737672,8.31850724179233E-5,0.158934495415709));
#40570=CARTESIAN_POINT('',(-0.14635,-1.79227059055215E-17,0.));
#40571=CARTESIAN_POINT('Ctrl Pts',(-0.14651736545536,8.65668654492988E-5,
0.166065504584291));
#40572=CARTESIAN_POINT('Ctrl Pts',(-0.146554285531508,0.00533178393548585,
0.165779366035948));
#40573=CARTESIAN_POINT('Ctrl Pts',(-0.146296777197391,0.0105733383781062,
0.165493227487605));
#40574=CARTESIAN_POINT('Ctrl Pts',(-0.145732753046151,0.0157816995937671,
0.165207088939262));
#40575=CARTESIAN_POINT('Ctrl Pts',(-0.140541899038255,0.0637155382981208,
0.16257368498446));
#40576=CARTESIAN_POINT('Ctrl Pts',(-0.109389226009343,0.108837918334108,
0.159940281029658));
#40577=CARTESIAN_POINT('Ctrl Pts',(-0.0664064572564633,0.130680066597967,
0.157306877074855));
#40578=CARTESIAN_POINT('Ctrl Pts',(-0.0234236885035836,0.152522214861825,
0.154673473120053));
#40579=CARTESIAN_POINT('Ctrl Pts',(0.031389175973264,0.151084131353554,
0.152040069165251));
#40580=CARTESIAN_POINT('Ctrl Pts',(0.073167488832194,0.12701817148098,0.149406665210449));
#40581=CARTESIAN_POINT('Ctrl Pts',(0.114945801691124,0.102952211608407,
0.146773261255646));
#40582=CARTESIAN_POINT('Ctrl Pts',(0.143689562932137,0.0562583753715299,
0.144139857300844));
#40583=CARTESIAN_POINT('Ctrl Pts',(0.146359798857064,0.00811829104130666,
0.141506453346042));
#40584=CARTESIAN_POINT('Ctrl Pts',(0.149030034781992,-0.0400217932889162,
0.13887304939124));
#40585=CARTESIAN_POINT('Ctrl Pts',(0.125626745390835,-0.0896081257124856,
0.136239645436437));
#40586=CARTESIAN_POINT('Ctrl Pts',(0.0867663172267087,-0.118146957909964,
0.133606241481635));
#40587=CARTESIAN_POINT('Ctrl Pts',(0.0479058890625822,-0.146685790107443,
0.130972837526833));
#40588=CARTESIAN_POINT('Ctrl Pts',(-0.00641167787451363,-0.154177122078832,
0.128339433572031));
#40589=CARTESIAN_POINT('Ctrl Pts',(-0.0515464175662268,-0.13722267989126,
0.125706029617228));
#40590=CARTESIAN_POINT('Ctrl Pts',(-0.0966811572579399,-0.120268237703689,
0.123072625662426));
#40591=CARTESIAN_POINT('Ctrl Pts',(-0.13263306970427,-0.0788680213571585,
0.120439221707624));
#40592=CARTESIAN_POINT('Ctrl Pts',(-0.143093361363041,-0.0318023192658095,
0.117805817752821));
#40593=CARTESIAN_POINT('Ctrl Pts',(-0.145397626569199,-0.0214343617297895,
0.117225713363311));
#40594=CARTESIAN_POINT('Ctrl Pts',(-0.146464877288401,-0.0107914790330514,
0.116645608973801));
#40595=CARTESIAN_POINT('Ctrl Pts',(-0.146368002745976,-0.000129372869328834,
0.116065504584291));
#40596=CARTESIAN_POINT('Ctrl Pts',(-0.146366557616609,-0.000129983413451606,
0.108934495415709));
#40597=CARTESIAN_POINT('Ctrl Pts',(-0.146464181092139,-0.0108506595114597,
0.109517771874887));
#40598=CARTESIAN_POINT('Ctrl Pts',(-0.145385284604313,-0.0215518621108894,
0.110101048334066));
#40599=CARTESIAN_POINT('Ctrl Pts',(-0.143055987718722,-0.0319735935649507,
0.110684324793244));
#40600=CARTESIAN_POINT('Ctrl Pts',(-0.132531832933994,-0.0790607277237021,
0.11331966585975));
#40601=CARTESIAN_POINT('Ctrl Pts',(-0.0964822012484396,-0.12044278191103,
0.115955006926256));
#40602=CARTESIAN_POINT('Ctrl Pts',(-0.0512822836387571,-0.13732242834474,
0.118590347992762));
#40603=CARTESIAN_POINT('Ctrl Pts',(-0.00608236602907434,-0.154202074778449,
0.121225689059267));
#40604=CARTESIAN_POINT('Ctrl Pts',(0.0482678375047366,-0.14657931345854,
0.123861030125773));
#40605=CARTESIAN_POINT('Ctrl Pts',(0.0870803134198012,-0.117916681520738,
0.126496371192279));
#40606=CARTESIAN_POINT('Ctrl Pts',(0.125892789334866,-0.089254049582936,
0.129131712258785));
#40607=CARTESIAN_POINT('Ctrl Pts',(0.149167537631184,-0.0395515470272406,
0.131767053325291));
#40608=CARTESIAN_POINT('Ctrl Pts',(0.146332238452734,0.00861396207485353,
0.134402394391797));
#40609=CARTESIAN_POINT('Ctrl Pts',(0.143496939274284,0.0567794711769477,
0.137037735458302));
#40610=CARTESIAN_POINT('Ctrl Pts',(0.114551592621066,0.103407986825441,
0.139673076524808));
#40611=CARTESIAN_POINT('Ctrl Pts',(0.0726443273415577,0.127318991170589,
0.142308417591314));
#40612=CARTESIAN_POINT('Ctrl Pts',(0.0307370620620493,0.151229995515737,
0.14494375865782));
#40613=CARTESIAN_POINT('Ctrl Pts',(-0.0241321218437492,0.152423488557541,
0.147579099724326));
#40614=CARTESIAN_POINT('Ctrl Pts',(-0.067039462170215,0.130357334843671,
0.150214440790831));
#40615=CARTESIAN_POINT('Ctrl Pts',(-0.109946802496681,0.108291181129802,
0.152849781857337));
#40616=CARTESIAN_POINT('Ctrl Pts',(-0.140892299243814,0.0629653806602592,
0.155485122923843));
#40617=CARTESIAN_POINT('Ctrl Pts',(-0.145819277598255,0.0149687147614827,
0.158120463990349));
#40618=CARTESIAN_POINT('Ctrl Pts',(-0.1463265762883,0.0100268124462353,
0.158391807798802));
#40619=CARTESIAN_POINT('Ctrl Pts',(-0.146558040382541,0.0050565950257616,
0.158663151607255));
#40620=CARTESIAN_POINT('Ctrl Pts',(-0.146524127737672,8.31850724179233E-5,
0.158934495415709));
#40621=CARTESIAN_POINT('Origin',(0.,0.,0.));
#40622=CARTESIAN_POINT('',(-0.146129957599089,4.76874783713124E-5,0.21606550458429));
#40623=CARTESIAN_POINT('',(-0.146134590291164,5.53529746073057E-5,0.208934495415709));
#40624=CARTESIAN_POINT('',(-0.14635,-1.79227059055215E-17,0.));
#40625=CARTESIAN_POINT('Ctrl Pts',(-0.146129957599089,4.76874783713124E-5,
0.21606550458429));
#40626=CARTESIAN_POINT('Ctrl Pts',(-0.146192738333019,0.0213155226117273,
0.214913123098095));
#40627=CARTESIAN_POINT('Ctrl Pts',(-0.14184845306411,0.0425589323614883,
0.213760741611899));
#40628=CARTESIAN_POINT('Ctrl Pts',(-0.132968065125987,0.0616975770053832,
0.212608360125703));
#40629=CARTESIAN_POINT('Ctrl Pts',(-0.11267474299563,0.105432905191852,
0.2099749561709));
#40630=CARTESIAN_POINT('Ctrl Pts',(-0.0686935897650435,0.13817700942041,
0.207341552216098));
#40631=CARTESIAN_POINT('Ctrl Pts',(-0.0209756858809845,0.145076248759314,
0.204708148261296));
#40632=CARTESIAN_POINT('Ctrl Pts',(0.0267422180030747,0.151975488098219,
0.202074744306494));
#40633=CARTESIAN_POINT('Ctrl Pts',(0.0781968725406062,0.13302986254747,
0.199441340351692));
#40634=CARTESIAN_POINT('Ctrl Pts',(0.110047008199114,0.0968336374273772,
0.196807936396889));
#40635=CARTESIAN_POINT('Ctrl Pts',(0.141897143857622,0.0606374123072843,
0.194174532442087));
#40636=CARTESIAN_POINT('Ctrl Pts',(0.154142760637107,0.00719058761784734,
0.191541128487285));
#40637=CARTESIAN_POINT('Ctrl Pts',(0.141228904479148,-0.0392618630629832,
0.188907724532483));
#40638=CARTESIAN_POINT('Ctrl Pts',(0.128315048321188,-0.0857143137438141,
0.18627432057768));
#40639=CARTESIAN_POINT('Ctrl Pts',(0.0902417192257834,-0.125172390416039,
0.183640916622878));
#40640=CARTESIAN_POINT('Ctrl Pts',(0.0442800434850501,-0.139736806546778,
0.181007512668076));
#40641=CARTESIAN_POINT('Ctrl Pts',(-0.00168163225568323,-0.154301222677517,
0.178374108713273));
#40642=CARTESIAN_POINT('Ctrl Pts',(-0.0555316546417454,-0.143971978266771,
0.175740704758471));
#40643=CARTESIAN_POINT('Ctrl Pts',(-0.0928421483413364,-0.113434707375038,
0.173107300803669));
#40644=CARTESIAN_POINT('Ctrl Pts',(-0.126098584749153,-0.0862155337115625,
0.17076003539721));
#40645=CARTESIAN_POINT('Ctrl Pts',(-0.146214500923306,-0.0429412483281845,
0.16841276999075));
#40646=CARTESIAN_POINT('Ctrl Pts',(-0.14651736545536,8.65668654492988E-5,
0.166065504584291));
#40647=CARTESIAN_POINT('Ctrl Pts',(-0.146524127737672,8.31850724179233E-5,
0.158934495415709));
#40648=CARTESIAN_POINT('Ctrl Pts',(-0.146228674526712,-0.043246078859919,
0.161298492673761));
#40649=CARTESIAN_POINT('Ctrl Pts',(-0.125790555024919,-0.0868176629158599,
0.163662489931814));
#40650=CARTESIAN_POINT('Ctrl Pts',(-0.0921252733308782,-0.11401867430555,
0.166026487189866));
#40651=CARTESIAN_POINT('Ctrl Pts',(-0.0545958307473115,-0.144341866145796,
0.168661828256372));
#40652=CARTESIAN_POINT('Ctrl Pts',(-0.000628485618429035,-0.154320718498276,
0.171297169322878));
#40653=CARTESIAN_POINT('Ctrl Pts',(0.0452626498105411,-0.139422439628514,
0.173932510389384));
#40654=CARTESIAN_POINT('Ctrl Pts',(0.0911537852395115,-0.124524160758753,
0.17656785145589));
#40655=CARTESIAN_POINT('Ctrl Pts',(0.128968710968569,-0.0847487506667484,
0.179203192522395));
#40656=CARTESIAN_POINT('Ctrl Pts',(0.141530385150016,-0.0381637812674535,
0.181838533588901));
#40657=CARTESIAN_POINT('Ctrl Pts',(0.154092059331463,0.00842118813184087,
0.184473874655407));
#40658=CARTESIAN_POINT('Ctrl Pts',(0.141400481965299,0.0618157168384256,
0.187109215721913));
#40659=CARTESIAN_POINT('Ctrl Pts',(0.109220671810841,0.0977658885483793,
0.189744556788419));
#40660=CARTESIAN_POINT('Ctrl Pts',(0.0770408616563825,0.133716060258333,
0.192379897854925));
#40661=CARTESIAN_POINT('Ctrl Pts',(0.025372818713629,0.152221874971656,
0.19501523892143));
#40662=CARTESIAN_POINT('Ctrl Pts',(-0.022313779030084,0.144877256285936,
0.197650579987936));
#40663=CARTESIAN_POINT('Ctrl Pts',(-0.0700003767737975,0.137532637600217,
0.200285921054442));
#40664=CARTESIAN_POINT('Ctrl Pts',(-0.113705529318471,0.104337585515455,
0.202921262120948));
#40665=CARTESIAN_POINT('Ctrl Pts',(-0.133576619842631,0.0603706116554267,
0.205556603187454));
#40666=CARTESIAN_POINT('Ctrl Pts',(-0.142066653397378,0.041585478402751,
0.206682567263539));
#40667=CARTESIAN_POINT('Ctrl Pts',(-0.146205843323087,0.0208339599326467,
0.207808531339624));
#40668=CARTESIAN_POINT('Ctrl Pts',(-0.146134590291164,5.53529746073057E-5,
0.208934495415709));
#40669=CARTESIAN_POINT('Origin',(0.,0.,0.));
#40670=CARTESIAN_POINT('',(-0.146348968946192,-0.000130334789587572,0.266065504584291));
#40671=CARTESIAN_POINT('',(-0.146327394052832,-0.000130859996972892,0.258934495415708));
#40672=CARTESIAN_POINT('',(-0.14635,-1.79227059055215E-17,0.));
#40673=CARTESIAN_POINT('Ctrl Pts',(-0.146348968946192,-0.000130334789587572,
0.266065504584291));
#40674=CARTESIAN_POINT('Ctrl Pts',(-0.146013620606683,0.0369836123692833,
0.264046880160242));
#40675=CARTESIAN_POINT('Ctrl Pts',(-0.131636768783893,0.074328824870482,
0.262028255736193));
#40676=CARTESIAN_POINT('Ctrl Pts',(-0.106148536005423,0.10109196632601,
0.260009631312144));
#40677=CARTESIAN_POINT('Ctrl Pts',(-0.072897767709896,0.136005921449249,
0.257376227357342));
#40678=CARTESIAN_POINT('Ctrl Pts',(-0.020736980756812,0.152910669462462,
0.254742823402539));
#40679=CARTESIAN_POINT('Ctrl Pts',(0.0266722339182632,0.144137744153214,
0.252109419447737));
#40680=CARTESIAN_POINT('Ctrl Pts',(0.0740814485933381,0.135364818843967,
0.249476015492935));
#40681=CARTESIAN_POINT('Ctrl Pts',(0.116739090990404,0.100914220212258,
0.246842611538132));
#40682=CARTESIAN_POINT('Ctrl Pts',(0.135294462171964,0.056413702744499,
0.24420920758333));
#40683=CARTESIAN_POINT('Ctrl Pts',(0.153849833353525,0.0119131852767396,
0.241575803628528));
#40684=CARTESIAN_POINT('Ctrl Pts',(0.148302933319579,-0.0426372510270706,
0.238942399673726));
#40685=CARTESIAN_POINT('Ctrl Pts',(0.121169990969772,-0.082492003492008,
0.236308995718923));
#40686=CARTESIAN_POINT('Ctrl Pts',(0.094037048619966,-0.122346755956945,
0.233675591764121));
#40687=CARTESIAN_POINT('Ctrl Pts',(0.0453180639542996,-0.14750582458301,
0.231042187809319));
#40688=CARTESIAN_POINT('Ctrl Pts',(-0.00288666981273841,-0.146556352606171,
0.228408783854516));
#40689=CARTESIAN_POINT('Ctrl Pts',(-0.0510914035797761,-0.145606880629331,
0.225775379899714));
#40690=CARTESIAN_POINT('Ctrl Pts',(-0.0987818864481854,-0.118548868049589,
0.223141975944912));
#40691=CARTESIAN_POINT('Ctrl Pts',(-0.124324382367327,-0.0776565856875276,
0.22050857199011));
#40692=CARTESIAN_POINT('Ctrl Pts',(-0.138689444093445,-0.0546588268893121,
0.219027549521503));
#40693=CARTESIAN_POINT('Ctrl Pts',(-0.146049272792313,-0.0272853980218952,
0.217546527052897));
#40694=CARTESIAN_POINT('Ctrl Pts',(-0.146129957599089,4.76874783713124E-5,
0.21606550458429));
#40695=CARTESIAN_POINT('Ctrl Pts',(-0.146134590291164,5.53529746073057E-5,
0.208934495415709));
#40696=CARTESIAN_POINT('Ctrl Pts',(-0.146039074200404,-0.0277987783441389,
0.210443872406129));
#40697=CARTESIAN_POINT('Ctrl Pts',(-0.138377421661147,-0.055701587485614,
0.21195324939655));
#40698=CARTESIAN_POINT('Ctrl Pts',(-0.123487844473835,-0.0789814939515912,
0.213462626386971));
#40699=CARTESIAN_POINT('Ctrl Pts',(-0.0974909500772326,-0.119627730063286,
0.216097967453477));
#40700=CARTESIAN_POINT('Ctrl Pts',(-0.0494601327803805,-0.146181306651382,
0.218733308519983));
#40701=CARTESIAN_POINT('Ctrl Pts',(-0.00121289818784218,-0.14658053417448,
0.221368649586488));
#40702=CARTESIAN_POINT('Ctrl Pts',(0.047034336404696,-0.146979761697578,
0.224003990652994));
#40703=CARTESIAN_POINT('Ctrl Pts',(0.0954979882929203,-0.121224640155678,
0.2266393317195));
#40704=CARTESIAN_POINT('Ctrl Pts',(0.122163941197393,-0.0810141690783142,
0.229274672786006));
#40705=CARTESIAN_POINT('Ctrl Pts',(0.148829894101866,-0.0408036980009502,
0.231910013852512));
#40706=CARTESIAN_POINT('Ctrl Pts',(0.153698148022588,0.0138621226118777,
0.234545354919018));
#40707=CARTESIAN_POINT('Ctrl Pts',(0.134557348601142,0.0581519050223658,
0.237180695985524));
#40708=CARTESIAN_POINT('Ctrl Pts',(0.115416549179696,0.102441687432854,
0.239816037052029));
#40709=CARTESIAN_POINT('Ctrl Pts',(0.0722666964160822,0.136355431641002,
0.242451378118535));
#40710=CARTESIAN_POINT('Ctrl Pts',(0.0247081678934101,0.144488167542617,
0.245086719185041));
#40711=CARTESIAN_POINT('Ctrl Pts',(-0.0228503606292616,0.152620903444231,
0.247722060251547));
#40712=CARTESIAN_POINT('Ctrl Pts',(-0.0748175649109913,0.134972631039312,
0.250357401318053));
#40713=CARTESIAN_POINT('Ctrl Pts',(-0.107587875971466,0.0995598968678148,
0.252992742384558));
#40714=CARTESIAN_POINT('Ctrl Pts',(-0.132216325719399,0.072945540282363,
0.254973326728275));
#40715=CARTESIAN_POINT('Ctrl Pts',(-0.146001912399175,0.0362973920726889,
0.256953911071992));
#40716=CARTESIAN_POINT('Ctrl Pts',(-0.146327394052832,-0.000130859996972892,
0.258934495415708));
#40717=CARTESIAN_POINT('Origin',(0.,0.,0.));
#40718=CARTESIAN_POINT('',(-0.146531331768327,7.78185235384022E-5,0.316065504584291));
#40719=CARTESIAN_POINT('',(-0.146550416329645,6.385150607816E-5,0.308934495415709));
#40720=CARTESIAN_POINT('',(-0.14635,-1.79227059055215E-17,0.));
#40721=CARTESIAN_POINT('Ctrl Pts',(-0.146531331768327,7.78185235384022E-5,
0.316065504584291));
#40722=CARTESIAN_POINT('Ctrl Pts',(-0.14656115307709,0.00468624689283061,
0.315814041177191));
#40723=CARTESIAN_POINT('Ctrl Pts',(-0.14636239679671,0.00929207042467623,
0.315562577770091));
#40724=CARTESIAN_POINT('Ctrl Pts',(-0.145926597573945,0.0138753548512781,
0.315311114362991));
#40725=CARTESIAN_POINT('Ctrl Pts',(-0.14136277093227,0.0618729520929492,
0.312677710408189));
#40726=CARTESIAN_POINT('Ctrl Pts',(-0.110802592512226,0.10739869970775,
0.310044306453387));
#40727=CARTESIAN_POINT('Ctrl Pts',(-0.0681090134487845,0.12980084606346,
0.307410902498584));
#40728=CARTESIAN_POINT('Ctrl Pts',(-0.0254154343853437,0.152202992419171,
0.304777498543782));
#40729=CARTESIAN_POINT('Ctrl Pts',(0.0294115453214934,0.151481537515791,
0.30214409458898));
#40730=CARTESIAN_POINT('Ctrl Pts',(0.0715008751789212,0.127963753463258,
0.299510690634177));
#40731=CARTESIAN_POINT('Ctrl Pts',(0.113590205036349,0.104445969410725,
0.296877286679375));
#40732=CARTESIAN_POINT('Ctrl Pts',(0.142941885044368,0.0581318562090376,
0.294243882724573));
#40733=CARTESIAN_POINT('Ctrl Pts',(0.146241172727074,0.0100307901566561,
0.291610478769771));
#40734=CARTESIAN_POINT('Ctrl Pts',(0.149540460409781,-0.038070275895725,
0.288977074814969));
#40735=CARTESIAN_POINT('Ctrl Pts',(0.126787355767176,-0.0879582947988004,
0.286343670860166));
#40736=CARTESIAN_POINT('Ctrl Pts',(0.0883033030491544,-0.117002666731855,
0.283710266905364));
#40737=CARTESIAN_POINT('Ctrl Pts',(0.0498192503311324,-0.14604703866491,
0.281076862950562));
#40738=CARTESIAN_POINT('Ctrl Pts',(-0.00439575046230666,-0.154247763627944,
0.27844345899576));
#40739=CARTESIAN_POINT('Ctrl Pts',(-0.0497482595792165,-0.137884763554925,
0.275810055040957));
#40740=CARTESIAN_POINT('Ctrl Pts',(-0.0951007686961262,-0.121521763481905,
0.273176651086155));
#40741=CARTESIAN_POINT('Ctrl Pts',(-0.131590786136507,-0.0805950383728307,
0.270543247131353));
#40742=CARTESIAN_POINT('Ctrl Pts',(-0.142665420037712,-0.0336700947016615,
0.26790984317655));
#40743=CARTESIAN_POINT('Ctrl Pts',(-0.145250841169412,-0.0227152638644948,
0.267295063645797));
#40744=CARTESIAN_POINT('Ctrl Pts',(-0.146451100522698,-0.0114335245988962,
0.266680284115044));
#40745=CARTESIAN_POINT('Ctrl Pts',(-0.146348968946192,-0.000130334789587572,
0.266065504584291));
#40746=CARTESIAN_POINT('Ctrl Pts',(-0.146327394052832,-0.000130859996972892,
0.258934495415708));
#40747=CARTESIAN_POINT('Ctrl Pts',(-0.146434994267663,-0.0121735902233998,
0.259589252138497));
#40748=CARTESIAN_POINT('Ctrl Pts',(-0.145071563913279,-0.0241922883978194,
0.260244008861286));
#40749=CARTESIAN_POINT('Ctrl Pts',(-0.142142543798705,-0.0358164956803284,
0.260898765584076));
#40750=CARTESIAN_POINT('Ctrl Pts',(-0.130353482726251,-0.0826029581188991,
0.263534106650581));
#40751=CARTESIAN_POINT('Ctrl Pts',(-0.0932019427421253,-0.122998687057965,
0.266169447717088));
#40752=CARTESIAN_POINT('Ctrl Pts',(-0.0475636294365445,-0.138654337383406,
0.268804788783593));
#40753=CARTESIAN_POINT('Ctrl Pts',(-0.00192531613096394,-0.154309987708848,
0.271440129850099));
#40754=CARTESIAN_POINT('Ctrl Pts',(0.0521997704960722,-0.145225559420664,
0.274075470916605));
#40755=CARTESIAN_POINT('Ctrl Pts',(0.090225865564854,-0.115527560795972,
0.27671081198311));
#40756=CARTESIAN_POINT('Ctrl Pts',(0.128251960633635,-0.0858295621712801,
0.279346153049616));
#40757=CARTESIAN_POINT('Ctrl Pts',(0.150179064144164,-0.0355179932100797,
0.281981494116122));
#40758=CARTESIAN_POINT('Ctrl Pts',(0.14604701445983,0.0125536324530514,
0.284616835182628));
#40759=CARTESIAN_POINT('Ctrl Pts',(0.141914964775496,0.0606252581161832,
0.287252176249134));
#40760=CARTESIAN_POINT('Ctrl Pts',(0.1117237618963,0.106456940481245,0.28988751731564));
#40761=CARTESIAN_POINT('Ctrl Pts',(0.0691874497467596,0.129230108403338,
0.292522858382145));
#40762=CARTESIAN_POINT('Ctrl Pts',(0.02665113759722,0.152003276325431,0.295158199448651));
#40763=CARTESIAN_POINT('Ctrl Pts',(-0.0282302838226635,0.151717929804555,
0.297793540515157));
#40764=CARTESIAN_POINT('Ctrl Pts',(-0.0705274923191129,0.128503684568086,
0.300428881581663));
#40765=CARTESIAN_POINT('Ctrl Pts',(-0.112824700815562,0.105289439331617,
0.303064222648169));
#40766=CARTESIAN_POINT('Ctrl Pts',(-0.142537696388578,0.0591462953795561,
0.305699563714675));
#40767=CARTESIAN_POINT('Ctrl Pts',(-0.146169655872548,0.0110343020847702,
0.30833490478118));
#40768=CARTESIAN_POINT('Ctrl Pts',(-0.146445102685266,0.00738550168790281,
0.308534768326023));
#40769=CARTESIAN_POINT('Ctrl Pts',(-0.146570540139926,0.00372537713102106,
0.308734631870866));
#40770=CARTESIAN_POINT('Ctrl Pts',(-0.146550416329645,6.385150607816E-5,
0.308934495415709));
#40771=CARTESIAN_POINT('Origin',(0.,0.,0.));
#40772=CARTESIAN_POINT('',(-0.146136883584905,5.71367125724795E-5,0.366065504584291));
#40773=CARTESIAN_POINT('',(-0.14615227160514,7.39083677616704E-5,0.358934495415709));
#40774=CARTESIAN_POINT('',(-0.14635,-1.79227059055215E-17,0.));
#40775=CARTESIAN_POINT('Ctrl Pts',(-0.146136883584905,5.71367125724795E-5,
0.366065504584291));
#40776=CARTESIAN_POINT('Ctrl Pts',(-0.14621004407594,0.0206825763459024,
0.364947798239338));
#40777=CARTESIAN_POINT('Ctrl Pts',(-0.142132997319362,0.0412803999606639,
0.363830091894385));
#40778=CARTESIAN_POINT('Ctrl Pts',(-0.133763205647759,0.0599541672162359,
0.362712385549432));
#40779=CARTESIAN_POINT('Ctrl Pts',(-0.114043318945497,0.10395102986619,
0.360078981594629));
#40780=CARTESIAN_POINT('Ctrl Pts',(-0.070493949429046,0.137267251375705,
0.357445577639827));
#40781=CARTESIAN_POINT('Ctrl Pts',(-0.0228703083824292,0.144789662428813,
0.354812173685025));
#40782=CARTESIAN_POINT('Ctrl Pts',(0.0247533326641879,0.15231207348192,
0.352178769730223));
#40783=CARTESIAN_POINT('Ctrl Pts',(0.0764512452409704,0.13404067407862,
0.34954536577542));
#40784=CARTESIAN_POINT('Ctrl Pts',(0.108771811167509,0.0982638817017563,
0.346911961820618));
#40785=CARTESIAN_POINT('Ctrl Pts',(0.141092377094047,0.0624870893248929,
0.344278557865816));
#40786=CARTESIAN_POINT('Ctrl Pts',(0.154035596370341,0.00920490397446603,
0.341645153911014));
#40787=CARTESIAN_POINT('Ctrl Pts',(0.141730062949927,-0.0374123857561472,
0.339011749956212));
#40788=CARTESIAN_POINT('Ctrl Pts',(0.129424529529512,-0.0840296754867619,
0.336378346001409));
#40789=CARTESIAN_POINT('Ctrl Pts',(0.0918702434123863,-0.123982069597563,
0.333744942046607));
#40790=CARTESIAN_POINT('Ctrl Pts',(0.0461028784809079,-0.139146045389481,
0.331111538091804));
#40791=CARTESIAN_POINT('Ctrl Pts',(0.000335513549430837,-0.154310021181399,
0.328478134137002));
#40792=CARTESIAN_POINT('Ctrl Pts',(-0.0536449301963988,-0.144685578654437,
0.3258447301822));
#40793=CARTESIAN_POINT('Ctrl Pts',(-0.0913514146376612,-0.114638633956686,
0.323211326227398));
#40794=CARTESIAN_POINT('Ctrl Pts',(-0.125457311698448,-0.0874608681681781,
0.320829385679696));
#40795=CARTESIAN_POINT('Ctrl Pts',(-0.146248854944573,-0.043574665631504,
0.318447445131993));
#40796=CARTESIAN_POINT('Ctrl Pts',(-0.146531331768327,7.78185235384022E-5,
0.316065504584291));
#40797=CARTESIAN_POINT('Ctrl Pts',(-0.146550416329645,6.385150607816E-5,
0.308934495415709));
#40798=CARTESIAN_POINT('Ctrl Pts',(-0.146305193582165,-0.0445544072241828,
0.311369972937372));
#40799=CARTESIAN_POINT('Ctrl Pts',(-0.1244453858937,-0.0893807124057277,
0.313805450459035));
#40800=CARTESIAN_POINT('Ctrl Pts',(-0.0890196886128741,-0.116459517256704,
0.316240927980698));
#40801=CARTESIAN_POINT('Ctrl Pts',(-0.0506868384743053,-0.145760500665881,
0.318876269047204));
#40802=CARTESIAN_POINT('Ctrl Pts',(0.00352978519775653,-0.154281624846726,
0.321511610113709));
#40803=CARTESIAN_POINT('Ctrl Pts',(0.0490028377607838,-0.138152256629371,
0.324146951180215));
#40804=CARTESIAN_POINT('Ctrl Pts',(0.0944758903238113,-0.122022888412016,
0.326782292246721));
#40805=CARTESIAN_POINT('Ctrl Pts',(0.131205371777804,-0.0812430277964604,
0.329417633313227));
#40806=CARTESIAN_POINT('Ctrl Pts',(0.142507292286359,-0.034336507766627,
0.332052974379733));
#40807=CARTESIAN_POINT('Ctrl Pts',(0.153809212794913,0.0125700122632054,
0.334688315446239));
#40808=CARTESIAN_POINT('Ctrl Pts',(0.139683572358031,0.0656031917073164,
0.337323656512744));
#40809=CARTESIAN_POINT('Ctrl Pts',(0.106546798111412,0.1006732533129,0.33995899757925));
#40810=CARTESIAN_POINT('Ctrl Pts',(0.0734100238647925,0.135743314918485,
0.342594338645756));
#40811=CARTESIAN_POINT('Ctrl Pts',(0.0212621158084357,0.152850258685541,
0.345229679712262));
#40812=CARTESIAN_POINT('Ctrl Pts',(-0.026209274243358,0.144223431050692,
0.347865020778768));
#40813=CARTESIAN_POINT('Ctrl Pts',(-0.0736806642951504,0.135596603415843,
0.350500361845274));
#40814=CARTESIAN_POINT('Ctrl Pts',(-0.11647553634238,0.10123600437909,0.353135702911779));
#40815=CARTESIAN_POINT('Ctrl Pts',(-0.135154759147093,0.056749583260925,
0.355771043978285));
#40816=CARTESIAN_POINT('Ctrl Pts',(-0.142628910530197,0.0389491506944377,
0.356825527790759));
#40817=CARTESIAN_POINT('Ctrl Pts',(-0.146242014510603,0.0195275186049996,
0.357880011603234));
#40818=CARTESIAN_POINT('Ctrl Pts',(-0.14615227160514,7.39083677616704E-5,
0.358934495415709));
#40819=CARTESIAN_POINT('Origin',(0.,0.,0.));
#40820=CARTESIAN_POINT('',(-0.146330070388523,-0.000130413829425732,0.416065504584291));
#40821=CARTESIAN_POINT('',(-0.146289342453438,-0.000128032530387096,0.408934495415709));
#40822=CARTESIAN_POINT('',(-0.14635,-1.79227059055215E-17,0.));
#40823=CARTESIAN_POINT('Ctrl Pts',(-0.146330070388523,-0.000130413829425732,
0.416065504584291));
#40824=CARTESIAN_POINT('Ctrl Pts',(-0.146004163689088,0.0363580550473478,
0.414081555301485));
#40825=CARTESIAN_POINT('Ctrl Pts',(-0.13216535679172,0.0730671490760677,
0.412097606018678));
#40826=CARTESIAN_POINT('Ctrl Pts',(-0.107460925463154,0.0996957714768259,
0.410113656735872));
#40827=CARTESIAN_POINT('Ctrl Pts',(-0.0746693880354573,0.135041392531165,
0.40748025278107));
#40828=CARTESIAN_POINT('Ctrl Pts',(-0.0227340340094623,0.152626534075836,
0.404846848826268));
#40829=CARTESIAN_POINT('Ctrl Pts',(0.0247858083562081,0.144474084374625,
0.402213444871466));
#40830=CARTESIAN_POINT('Ctrl Pts',(0.0723056507218785,0.136321634673413,
0.399580040916663));
#40831=CARTESIAN_POINT('Ctrl Pts',(0.115409981427224,0.102431593726319,
0.396946636961861));
#40832=CARTESIAN_POINT('Ctrl Pts',(0.134545471232452,0.0581774313853258,
0.394313233007059));
#40833=CARTESIAN_POINT('Ctrl Pts',(0.15368096103768,0.0139232690443328,
0.391679829052256));
#40834=CARTESIAN_POINT('Ctrl Pts',(0.14884760994279,-0.0406950146905586,
0.389046425097455));
#40835=CARTESIAN_POINT('Ctrl Pts',(0.122237961103967,-0.0809010396527884,
0.386413021142652));
#40836=CARTESIAN_POINT('Ctrl Pts',(0.0956283122651433,-0.121107064615018,
0.38377961718785));
#40837=CARTESIAN_POINT('Ctrl Pts',(0.0472423656823864,-0.146900830804586,
0.381146213233048));
#40838=CARTESIAN_POINT('Ctrl Pts',(-0.000970660813290544,-0.146581564902762,
0.378512809278245));
#40839=CARTESIAN_POINT('Ctrl Pts',(-0.0491836873089679,-0.146262299000937,
0.375879405323443));
#40840=CARTESIAN_POINT('Ctrl Pts',(-0.0972237937175652,-0.11983000100772,
0.373246001368641));
#40841=CARTESIAN_POINT('Ctrl Pts',(-0.123298644977828,-0.0792751001159155,
0.370612597413839));
#40842=CARTESIAN_POINT('Ctrl Pts',(-0.138306441127099,-0.0559330806595814,
0.369096899803989));
#40843=CARTESIAN_POINT('Ctrl Pts',(-0.146037672211633,-0.0279125797478292,
0.36758120219414));
#40844=CARTESIAN_POINT('Ctrl Pts',(-0.146136883584905,5.71367125724795E-5,
0.366065504584291));
#40845=CARTESIAN_POINT('Ctrl Pts',(-0.14615227160514,7.39083677616704E-5,
0.358934495415709));
#40846=CARTESIAN_POINT('Ctrl Pts',(-0.146017731158506,-0.0290904851457483,
0.36051535266974));
#40847=CARTESIAN_POINT('Ctrl Pts',(-0.137560931614845,-0.0583267505026361,
0.362096209923772));
#40848=CARTESIAN_POINT('Ctrl Pts',(-0.121314920725415,-0.0822800955868649,
0.363677067177803));
#40849=CARTESIAN_POINT('Ctrl Pts',(-0.0942322859368278,-0.122211110116912,
0.366312408244309));
#40850=CARTESIAN_POINT('Ctrl Pts',(-0.0455034427974572,-0.147460895977431,
0.368947749310814));
#40851=CARTESIAN_POINT('Ctrl Pts',(0.00273703201223555,-0.146559997189415,
0.37158309037732));
#40852=CARTESIAN_POINT('Ctrl Pts',(0.050977506821928,-0.145659098401399,
0.374218431443826));
#40853=CARTESIAN_POINT('Ctrl Pts',(0.0987296133019425,-0.11860751496485,
0.376853772510332));
#40854=CARTESIAN_POINT('Ctrl Pts',(0.124302447370845,-0.0776931509080149,
0.379489113576838));
#40855=CARTESIAN_POINT('Ctrl Pts',(0.149875281439748,-0.0367787868511801,
0.382124454643343));
#40856=CARTESIAN_POINT('Ctrl Pts',(0.153268843097537,0.0179983578259404,
0.384759795709849));
#40857=CARTESIAN_POINT('Ctrl Pts',(0.132941641804014,0.0617563275693305,
0.387395136776355));
#40858=CARTESIAN_POINT('Ctrl Pts',(0.112614440510491,0.10551429731272,0.39003047784286));
#40859=CARTESIAN_POINT('Ctrl Pts',(0.0685664762656556,0.13825309212238,
0.392665818909367));
#40860=CARTESIAN_POINT('Ctrl Pts',(0.0208060845723004,0.145101450596359,
0.395301159975872));
#40861=CARTESIAN_POINT('Ctrl Pts',(-0.0269543071210555,0.151949809070337,
0.397936501042378));
#40862=CARTESIAN_POINT('Ctrl Pts',(-0.0784271262629304,0.132907731208634,
0.400571842108884));
#40863=CARTESIAN_POINT('Ctrl Pts',(-0.110231373247062,0.0966248853684404,
0.40320718317539));
#40864=CARTESIAN_POINT('Ctrl Pts',(-0.133271130208243,0.0703407243117375,
0.405116287255496));
#40865=CARTESIAN_POINT('Ctrl Pts',(-0.145989017153952,0.0350087805988431,
0.407025391335602));
#40866=CARTESIAN_POINT('Ctrl Pts',(-0.146289342453438,-0.000128032530387096,
0.408934495415709));
#40867=CARTESIAN_POINT('Origin',(0.,0.,0.));
#40868=CARTESIAN_POINT('',(-0.146544022497492,6.84377374728824E-5,0.466065504584291));
#40869=CARTESIAN_POINT('',(-0.146570300119817,4.22437972465385E-5,0.458934495415709));
#40870=CARTESIAN_POINT('',(-0.14635,-1.79227059055215E-17,0.));
#40871=CARTESIAN_POINT('Ctrl Pts',(-0.146544022497492,6.84377374728824E-5,
0.466065504584291));
#40872=CARTESIAN_POINT('Ctrl Pts',(-0.146567170791634,0.00404048499144927,
0.465848716318434));
#40873=CARTESIAN_POINT('Ctrl Pts',(-0.146419528859516,0.00801078566506452,
0.465631928052577));
#40874=CARTESIAN_POINT('Ctrl Pts',(-0.146095506097533,0.0119666390378655,
0.46541513978672));
#40875=CARTESIAN_POINT('Ctrl Pts',(-0.142159486684863,0.0600197930006592,
0.462781735831918));
#40876=CARTESIAN_POINT('Ctrl Pts',(-0.112197024986195,0.105941128890497,
0.460148331877115));
#40877=CARTESIAN_POINT('Ctrl Pts',(-0.0697999311245908,0.128899445176305,
0.457514927922313));
#40878=CARTESIAN_POINT('Ctrl Pts',(-0.0274028372629858,0.151857761462114,
0.454881523967511));
#40879=CARTESIAN_POINT('Ctrl Pts',(0.0274288887615551,0.151853058143892,
0.452248120012709));
#40880=CARTESIAN_POINT('Ctrl Pts',(0.0698220433938502,0.12888746877825,
0.449614716057906));
#40881=CARTESIAN_POINT('Ctrl Pts',(0.112215198026145,0.105921879412608,
0.446981312103104));
#40882=CARTESIAN_POINT('Ctrl Pts',(0.142169781266193,0.0599954039995453,
0.444347908148302));
#40883=CARTESIAN_POINT('Ctrl Pts',(0.146097556879977,0.0119415755015296,
0.441714504193499));
#40884=CARTESIAN_POINT('Ctrl Pts',(0.150025332493762,-0.036112252996486,
0.439081100238697));
#40885=CARTESIAN_POINT('Ctrl Pts',(0.127926300481281,-0.0862934345794555,
0.436447696283895));
#40886=CARTESIAN_POINT('Ctrl Pts',(0.0898251994650805,-0.11583838264071,
0.433814292329093));
#40887=CARTESIAN_POINT('Ctrl Pts',(0.0517240984488793,-0.145383330701964,
0.431180888374291));
#40888=CARTESIAN_POINT('Ctrl Pts',(-0.00237907157104229,-0.154292045241502,
0.428547484419488));
#40889=CARTESIAN_POINT('Ctrl Pts',(-0.0479416004074503,-0.138523284332019,
0.425914080464686));
#40890=CARTESIAN_POINT('Ctrl Pts',(-0.0935041292438574,-0.122754523422536,
0.423280676509884));
#40891=CARTESIAN_POINT('Ctrl Pts',(-0.130526016896751,-0.0823082870640309,
0.420647272555081));
#40892=CARTESIAN_POINT('Ctrl Pts',(-0.142213100308499,-0.0355321186027758,
0.418013868600279));
#40893=CARTESIAN_POINT('Ctrl Pts',(-0.145095389184054,-0.0239960984301615,
0.417364413928283));
#40894=CARTESIAN_POINT('Ctrl Pts',(-0.146436757404375,-0.0120750773303437,
0.416714959256287));
#40895=CARTESIAN_POINT('Ctrl Pts',(-0.146330070388523,-0.000130413829425732,
0.416065504584291));
#40896=CARTESIAN_POINT('Ctrl Pts',(-0.146289342453438,-0.000128032530387096,
0.408934495415709));
#40897=CARTESIAN_POINT('Ctrl Pts',(-0.146403588367378,-0.0134943301275472,
0.409660732402108));
#40898=CARTESIAN_POINT('Ctrl Pts',(-0.144720893191604,-0.0268323904448261,
0.410386969388508));
#40899=CARTESIAN_POINT('Ctrl Pts',(-0.141125892037436,-0.0396334040556115,
0.411113206374907));
#40900=CARTESIAN_POINT('Ctrl Pts',(-0.128080489017291,-0.0860852338207874,
0.413748547441413));
#40901=CARTESIAN_POINT('Ctrl Pts',(-0.0898540081506159,-0.125465279532456,
0.416383888507919));
#40902=CARTESIAN_POINT('Ctrl Pts',(-0.0438104358868217,-0.139885559754408,
0.419019229574425));
#40903=CARTESIAN_POINT('Ctrl Pts',(0.00223313637697255,-0.15430583997636,
0.42165457064093));
#40904=CARTESIAN_POINT('Ctrl Pts',(0.0560938000378854,-0.143766354708596,
0.424289911707436));
#40905=CARTESIAN_POINT('Ctrl Pts',(0.0933059016336915,-0.11305455692152,
0.426925252773942));
#40906=CARTESIAN_POINT('Ctrl Pts',(0.130518003229497,-0.082342759134444,
0.429560593840448));
#40907=CARTESIAN_POINT('Ctrl Pts',(0.151081542760197,-0.0314586488280562,
0.432195934906954));
#40908=CARTESIAN_POINT('Ctrl Pts',(0.145655743526821,0.0164841893354265,
0.434831275973459));
#40909=CARTESIAN_POINT('Ctrl Pts',(0.140229944293446,0.06442702749891,0.437466617039965));
#40910=CARTESIAN_POINT('Ctrl Pts',(0.108814806295994,0.109428593519488,
0.440101958106471));
#40911=CARTESIAN_POINT('Ctrl Pts',(0.0656803334199076,0.131047388078691,
0.442737299172977));
#40912=CARTESIAN_POINT('Ctrl Pts',(0.022545860543821,0.152666182637894,
0.445372640239483));
#40913=CARTESIAN_POINT('Ctrl Pts',(-0.032307947210901,0.150902205735721,
0.448007981305989));
#40914=CARTESIAN_POINT('Ctrl Pts',(-0.0739643108743681,0.126556725768634,
0.450643322372494));
#40915=CARTESIAN_POINT('Ctrl Pts',(-0.115620674537836,0.102211245801546,
0.453278663439));
#40916=CARTESIAN_POINT('Ctrl Pts',(-0.144079594110048,0.0552842627695439,
0.455914004505506));
#40917=CARTESIAN_POINT('Ctrl Pts',(-0.14641389757273,0.0070918768996262,
0.458549345572012));
#40918=CARTESIAN_POINT('Ctrl Pts',(-0.146527615505388,0.00474413652285832,
0.458677728853244));
#40919=CARTESIAN_POINT('Ctrl Pts',(-0.146579333222338,0.00239339303023303,
0.458806112134477));
#40920=CARTESIAN_POINT('Ctrl Pts',(-0.146570300119817,4.22437972465385E-5,
0.458934495415709));
#40921=CARTESIAN_POINT('Origin',(0.,0.,0.));
#40922=CARTESIAN_POINT('',(-0.146145057762853,6.62388175271394E-5,0.516065504584291));
#40923=CARTESIAN_POINT('',(-0.146174937959923,9.05479403153491E-5,0.508934495415709));
#40924=CARTESIAN_POINT('',(-0.14635,-1.79227059055215E-17,0.));
#40925=CARTESIAN_POINT('Ctrl Pts',(-0.146145057762853,6.62388175271395E-5,
0.516065504584291));
#40926=CARTESIAN_POINT('Ctrl Pts',(-0.146227515408595,0.0200490060336265,
0.514982473380581));
#40927=CARTESIAN_POINT('Ctrl Pts',(-0.142408399519226,0.0400016020167204,
0.513899442176871));
#40928=CARTESIAN_POINT('Ctrl Pts',(-0.134535488644935,0.0582005124275171,
0.512816410973161));
#40929=CARTESIAN_POINT('Ctrl Pts',(-0.115392407114926,0.102451391335448,
0.510183007018359));
#40930=CARTESIAN_POINT('Ctrl Pts',(-0.0722822630505052,0.136334037036404,
0.507549603063556));
#40931=CARTESIAN_POINT('Ctrl Pts',(-0.0247610227936349,0.144478334368756,
0.504916199108754));
#40932=CARTESIAN_POINT('Ctrl Pts',(0.0227602174632348,0.152622631701108,
0.502282795153951));
#40933=CARTESIAN_POINT('Ctrl Pts',(0.0746925539125539,0.135028580664858,
0.49964939119915));
#40934=CARTESIAN_POINT('Ctrl Pts',(0.107478027152826,0.0996773345906346,
0.497015987244347));
#40935=CARTESIAN_POINT('Ctrl Pts',(0.140263500393099,0.06432608851641,0.494382583289545));
#40936=CARTESIAN_POINT('Ctrl Pts',(0.153902110424324,0.0112176474042102,
0.491749179334742));
#40937=CARTESIAN_POINT('Ctrl Pts',(0.142207002516364,-0.0355565153954619,
0.48911577537994));
#40938=CARTESIAN_POINT('Ctrl Pts',(0.130511894608405,-0.0823306781951331,
0.486482371425138));
#40939=CARTESIAN_POINT('Ctrl Pts',(0.0934830687612624,-0.122770562682277,
0.483848967470336));
#40940=CARTESIAN_POINT('Ctrl Pts',(0.0479178353914133,-0.138531506897017,
0.481215563515534));
#40941=CARTESIAN_POINT('Ctrl Pts',(0.00235260202156486,-0.154292451111757,
0.478582159560731));
#40942=CARTESIAN_POINT('Ctrl Pts',(-0.0517490388709899,-0.145374455054093,
0.475948755605929));
#40943=CARTESIAN_POINT('Ctrl Pts',(-0.0898450707539318,-0.115822971007387,
0.473315351651126));
#40944=CARTESIAN_POINT('Ctrl Pts',(-0.124804943950367,-0.0887042375336795,
0.470898735962181));
#40945=CARTESIAN_POINT('Ctrl Pts',(-0.146285980252562,-0.044209381789552,
0.468482120273236));
#40946=CARTESIAN_POINT('Ctrl Pts',(-0.146544022497492,6.84377374728824E-5,
0.466065504584291));
#40947=CARTESIAN_POINT('Ctrl Pts',(-0.146570300119817,4.22437972465385E-5,
0.458934495415709));
#40948=CARTESIAN_POINT('Ctrl Pts',(-0.14639390949893,-0.0458689668946884,
0.461441453200982));
#40949=CARTESIAN_POINT('Ctrl Pts',(-0.123052682342738,-0.0919348900534666,
0.463948410986256));
#40950=CARTESIAN_POINT('Ctrl Pts',(-0.0858494648887911,-0.118815796503266,
0.466455368771529));
#40951=CARTESIAN_POINT('Ctrl Pts',(-0.0467410413890165,-0.147073295328412,
0.469090709838035));
#40952=CARTESIAN_POINT('Ctrl Pts',(0.00768549296368549,-0.154130504270872,
0.471726050904541));
#40953=CARTESIAN_POINT('Ctrl Pts',(0.0527074437553312,-0.136781758627296,
0.474361391971047));
#40954=CARTESIAN_POINT('Ctrl Pts',(0.0977293945469769,-0.11943301298372,
0.476996733037553));
#40955=CARTESIAN_POINT('Ctrl Pts',(0.133346761777566,-0.0776783127541087,
0.479632074104058));
#40956=CARTESIAN_POINT('Ctrl Pts',(0.143380722078222,-0.0304843018080604,
0.482267415170564));
#40957=CARTESIAN_POINT('Ctrl Pts',(0.153414682378878,0.0167097091379873,
0.48490275623707));
#40958=CARTESIAN_POINT('Ctrl Pts',(0.137865235749601,0.0693430308004717,
0.487538097303576));
#40959=CARTESIAN_POINT('Ctrl Pts',(0.103795558670285,0.103507517218417,
0.490173438370082));
#40960=CARTESIAN_POINT('Ctrl Pts',(0.0697258815909678,0.137672003636362,
0.492808779436588));
#40961=CARTESIAN_POINT('Ctrl Pts',(0.0171359740616113,0.153367654809767,
0.495444120503093));
#40962=CARTESIAN_POINT('Ctrl Pts',(-0.0300857383810333,0.143464882345699,
0.498079461569599));
#40963=CARTESIAN_POINT('Ctrl Pts',(-0.0773074508236773,0.133562109881631,
0.500714802636104));
#40964=CARTESIAN_POINT('Ctrl Pts',(-0.11916096817961,0.09806091378009,0.503350143702611));
#40965=CARTESIAN_POINT('Ctrl Pts',(-0.136634759914189,0.0530873478673518,
0.505985484769117));
#40966=CARTESIAN_POINT('Ctrl Pts',(-0.143152625668081,0.0363118437555022,
0.506968488317981));
#40967=CARTESIAN_POINT('Ctrl Pts',(-0.146278417362408,0.0182184011065993,
0.507951491866845));
#40968=CARTESIAN_POINT('Ctrl Pts',(-0.146174937959923,9.05479403153491E-5,
0.508934495415709));
#40969=CARTESIAN_POINT('Origin',(0.,0.,0.));
#40970=CARTESIAN_POINT('',(-0.146311419053965,-0.000129619860865307,0.566065504584291));
#40971=CARTESIAN_POINT('',(-0.146253314944083,-0.00012165943743628,0.558934495415709));
#40972=CARTESIAN_POINT('',(-0.14635,-1.79227059055215E-17,0.));
#40973=CARTESIAN_POINT('Ctrl Pts',(-0.146311419053965,-0.000129619860865307,
0.566065504584291));
#40974=CARTESIAN_POINT('Ctrl Pts',(-0.145996667082224,0.0357327735863427,
0.564116230442728));
#40975=CARTESIAN_POINT('Ctrl Pts',(-0.132683527872108,0.0718042758553121,
0.562166956301165));
#40976=CARTESIAN_POINT('Ctrl Pts',(-0.10875495194318,0.0982825405633859,
0.560217682159602));
#40977=CARTESIAN_POINT('Ctrl Pts',(-0.0764282488179375,0.134053787671104,
0.557584278204799));
#40978=CARTESIAN_POINT('Ctrl Pts',(-0.0247272024587828,0.152316317789357,
0.554950874249997));
#40979=CARTESIAN_POINT('Ctrl Pts',(0.022895147382597,0.144785736790908,
0.552317470295194));
#40980=CARTESIAN_POINT('Ctrl Pts',(0.0705174972239762,0.13725515579246,
0.549684066340392));
#40981=CARTESIAN_POINT('Ctrl Pts',(0.11406115054758,0.103931463677311,0.54705066238559));
#40982=CARTESIAN_POINT('Ctrl Pts',(0.133773489094236,0.0599312186369601,
0.544417258430788));
#40983=CARTESIAN_POINT('Ctrl Pts',(0.153485827640893,0.0159309735966095,
0.541783854475986));
#40984=CARTESIAN_POINT('Ctrl Pts',(0.149366851410602,-0.038745824368944,
0.539150450521183));
#40985=CARTESIAN_POINT('Ctrl Pts',(0.123285043153097,-0.0792962514025479,
0.536517046566381));
#40986=CARTESIAN_POINT('Ctrl Pts',(0.097203234895591,-0.119846678436152,
0.533883642611579));
#40987=CARTESIAN_POINT('Ctrl Pts',(0.0491585946108714,-0.146270734537808,
0.531250238656777));
#40988=CARTESIAN_POINT('Ctrl Pts',(0.000945514053129371,-0.146581729267096,
0.528616834701974));
#40989=CARTESIAN_POINT('Ctrl Pts',(-0.0472675665046126,-0.146892723996384,
0.525983430747172));
#40990=CARTESIAN_POINT('Ctrl Pts',(-0.0956490873353763,-0.121090657353305,
0.523350026792369));
#40991=CARTESIAN_POINT('Ctrl Pts',(-0.122251838252959,-0.0808800679743115,
0.520716622837567));
#40992=CARTESIAN_POINT('Ctrl Pts',(-0.137913765110592,-0.057206752695483,
0.519166250086475));
#40993=CARTESIAN_POINT('Ctrl Pts',(-0.146027018608819,-0.0285393430688772,
0.517615877335383));
#40994=CARTESIAN_POINT('Ctrl Pts',(-0.146145057762853,6.62388175271395E-5,
0.516065504584291));
#40995=CARTESIAN_POINT('Ctrl Pts',(-0.146174937959923,9.05479403153491E-5,
0.508934495415709));
#40996=CARTESIAN_POINT('Ctrl Pts',(-0.146000998710948,-0.0303806868131737,
0.510586832933351));
#40997=CARTESIAN_POINT('Ctrl Pts',(-0.136702921110135,-0.060949146702594,
0.512239170450992));
#40998=CARTESIAN_POINT('Ctrl Pts',(-0.119053907816366,-0.0855189520167866,
0.513891507968634));
#40999=CARTESIAN_POINT('Ctrl Pts',(-0.0909051978707368,-0.124705750264253,
0.51652684903514));
#41000=CARTESIAN_POINT('Ctrl Pts',(-0.041513711866252,-0.148633411035251,
0.519162190101645));
#41001=CARTESIAN_POINT('Ctrl Pts',(0.00668497479873183,-0.146433040097983,
0.521797531168151));
#41002=CARTESIAN_POINT('Ctrl Pts',(0.0548836614637157,-0.144232669160716,
0.524432872234657));
#41003=CARTESIAN_POINT('Ctrl Pts',(0.101889548789197,-0.115904266515181,
0.527068213301163));
#41004=CARTESIAN_POINT('Ctrl Pts',(0.126350695083001,-0.0743157182057725,
0.529703554367669));
#41005=CARTESIAN_POINT('Ctrl Pts',(0.150811841376805,-0.0327271698963649,
0.532338895434175));
#41006=CARTESIAN_POINT('Ctrl Pts',(0.152728246638932,0.0221215240769157,
0.53497423650068));
#41007=CARTESIAN_POINT('Ctrl Pts',(0.131229403455446,0.0653159076268943,
0.537609577567186));
#41008=CARTESIAN_POINT('Ctrl Pts',(0.10973056027196,0.108510291176874,0.540244918633692));
#41009=CARTESIAN_POINT('Ctrl Pts',(0.0648164686428582,0.140050364303552,
0.542880259700198));
#41010=CARTESIAN_POINT('Ctrl Pts',(0.0168888935424139,0.145609372621787,
0.545515600766704));
#41011=CARTESIAN_POINT('Ctrl Pts',(-0.0310386815580289,0.151168380940021,
0.54815094183321));
#41012=CARTESIAN_POINT('Ctrl Pts',(-0.0819797401298146,0.130746324449814,
0.550786282899715));
#41013=CARTESIAN_POINT('Ctrl Pts',(-0.112794829345876,0.093619712631646,
0.553421623966221));
#41014=CARTESIAN_POINT('Ctrl Pts',(-0.134282196795419,0.0677313192961588,
0.555259247782717));
#41015=CARTESIAN_POINT('Ctrl Pts',(-0.145983763479016,0.0337207109540846,
0.557096871599213));
#41016=CARTESIAN_POINT('Ctrl Pts',(-0.146253314944083,-0.00012165943743628,
0.558934495415709));
#41017=CARTESIAN_POINT('Origin',(0.,0.,0.));
#41018=CARTESIAN_POINT('',(-0.146555285157174,5.84873774584615E-5,0.616065504584291));
#41019=CARTESIAN_POINT('',(-0.146582406651585,1.90495679610238E-5,0.608934495415709));
#41020=CARTESIAN_POINT('',(-0.14635,-1.79227059055215E-17,0.));
#41021=CARTESIAN_POINT('Ctrl Pts',(-0.146555285157174,5.84873774584615E-5,
0.616065504584291));
#41022=CARTESIAN_POINT('Ctrl Pts',(-0.146572323774182,0.00339452825839206,
0.615883391459677));
#41023=CARTESIAN_POINT('Ctrl Pts',(-0.146468182740347,0.00672948697362643,
0.615701278335063));
#41024=CARTESIAN_POINT('Ctrl Pts',(-0.146239449746585,0.0100558783590757,
0.615519165210449));
#41025=CARTESIAN_POINT('Ctrl Pts',(-0.142931910151921,0.0581563776955572,
0.612885761255647));
#41026=CARTESIAN_POINT('Ctrl Pts',(-0.113572285175357,0.10446545479915,
0.610252357300844));
#41027=CARTESIAN_POINT('Ctrl Pts',(-0.0714789213525946,0.127976017886268,
0.607618953346042));
#41028=CARTESIAN_POINT('Ctrl Pts',(-0.0293855575298321,0.151486580973386,
0.60498554939124));
#41029=CARTESIAN_POINT('Ctrl Pts',(0.0254415451391293,0.15219863004403,
0.602352145436437));
#41030=CARTESIAN_POINT('Ctrl Pts',(0.068131280382423,0.129789159736893,
0.599718741481635));
#41031=CARTESIAN_POINT('Ctrl Pts',(0.110821015625717,0.107379689429756,
0.597085337526833));
#41032=CARTESIAN_POINT('Ctrl Pts',(0.141373383443343,0.0618486997448399,
0.594451933572031));
#41033=CARTESIAN_POINT('Ctrl Pts',(0.145928975807906,0.0138503202638931,
0.591818529617228));
#41034=CARTESIAN_POINT('Ctrl Pts',(0.150484568172469,-0.0341480592170517,
0.589185125662426));
#41035=CARTESIAN_POINT('Ctrl Pts',(0.129043385083969,-0.0846138284940251,
0.586551721707624));
#41036=CARTESIAN_POINT('Ctrl Pts',(0.0913317465051492,-0.114654304027699,
0.583918317752822));
#41037=CARTESIAN_POINT('Ctrl Pts',(0.0536201079263286,-0.144694779561374,
0.58128491379802));
#41038=CARTESIAN_POINT('Ctrl Pts',(-0.000361986142813277,-0.154309961351749,
0.578651509843217));
#41039=CARTESIAN_POINT('Ctrl Pts',(-0.0461267489505717,-0.139138134179699,
0.576018105888415));
#41040=CARTESIAN_POINT('Ctrl Pts',(-0.0918915117583307,-0.123966307007649,
0.573384701933613));
#41041=CARTESIAN_POINT('Ctrl Pts',(-0.129438943304707,-0.0840074708731724,
0.57075129797881));
#41042=CARTESIAN_POINT('Ctrl Pts',(-0.141736479132229,-0.0373880707573429,
0.568117894024008));
#41043=CARTESIAN_POINT('Ctrl Pts',(-0.14493124569041,-0.0252768557512302,
0.567433764210769));
#41044=CARTESIAN_POINT('Ctrl Pts',(-0.146421886434131,-0.0127161165512012,
0.56674963439753));
#41045=CARTESIAN_POINT('Ctrl Pts',(-0.146311419053965,-0.000129619860865307,
0.566065504584291));
#41046=CARTESIAN_POINT('Ctrl Pts',(-0.146253314944083,-0.00012165943743628,
0.558934495415709));
#41047=CARTESIAN_POINT('Ctrl Pts',(-0.146370327932007,-0.0148127199255511,
0.559732212665719));
#41048=CARTESIAN_POINT('Ctrl Pts',(-0.144333034185812,-0.0294720768038573,
0.560529929915728));
#41049=CARTESIAN_POINT('Ctrl Pts',(-0.140006765979157,-0.0434215338335114,
0.561327647165738));
#41050=CARTESIAN_POINT('Ctrl Pts',(-0.125714493536039,-0.089505001334368,
0.563962988232244));
#41051=CARTESIAN_POINT('Ctrl Pts',(-0.0864408287894652,-0.127840769189951,
0.56659832929875));
#41052=CARTESIAN_POINT('Ctrl Pts',(-0.0400254307145004,-0.141015208458223,
0.569233670365256));
#41053=CARTESIAN_POINT('Ctrl Pts',(0.00638996736046498,-0.154189647726494,
0.571869011431762));
#41054=CARTESIAN_POINT('Ctrl Pts',(0.0599470987638218,-0.142202758407454,
0.574504352498268));
#41055=CARTESIAN_POINT('Ctrl Pts',(0.0963181864448715,-0.110499461900809,
0.577139693564773));
#41056=CARTESIAN_POINT('Ctrl Pts',(0.132689274125921,-0.0787961653941636,
0.579775034631279));
#41057=CARTESIAN_POINT('Ctrl Pts',(0.151874318084663,-0.0273764616999143,
0.582410375697785));
#41058=CARTESIAN_POINT('Ctrl Pts',(0.145158709082207,0.0204027767224063,
0.585045716764291));
#41059=CARTESIAN_POINT('Ctrl Pts',(0.138443100079752,0.0681820151447277,
0.587681057830797));
#41060=CARTESIAN_POINT('Ctrl Pts',(0.1058268381161,0.112320788295119,0.590316398897302));
#41061=CARTESIAN_POINT('Ctrl Pts',(0.0621255253059884,0.132769511657806,
0.592951739963808));
#41062=CARTESIAN_POINT('Ctrl Pts',(0.0184242124958778,0.153218235020492,
0.595587081030314));
#41063=CARTESIAN_POINT('Ctrl Pts',(-0.0363621511606923,0.149976908595474,
0.59822242209682));
#41064=CARTESIAN_POINT('Ctrl Pts',(-0.0773474224829438,0.124517871631514,
0.600857763163326));
#41065=CARTESIAN_POINT('Ctrl Pts',(-0.118332693805197,0.0990588346675542,
0.603493104229832));
#41066=CARTESIAN_POINT('Ctrl Pts',(-0.145516872793131,0.0513820871646532,
0.606128445296338));
#41067=CARTESIAN_POINT('Ctrl Pts',(-0.146551825250685,0.00314430216262847,
0.608763786362843));
#41068=CARTESIAN_POINT('Ctrl Pts',(-0.146574172232136,0.00210273848614761,
0.608820689380465));
#41069=CARTESIAN_POINT('Ctrl Pts',(-0.146584327751734,0.00106091323912811,
0.608877592398087));
#41070=CARTESIAN_POINT('Ctrl Pts',(-0.146582406651585,1.90495679610238E-5,
0.608934495415709));
#41071=CARTESIAN_POINT('Origin',(0.,0.,0.));
#41072=CARTESIAN_POINT('',(-0.146154441698478,7.49371236435786E-5,0.666065504584291));
#41073=CARTESIAN_POINT('',(-0.14620212788816,0.000104817362006062,0.658934495415709));
#41074=CARTESIAN_POINT('',(-0.14635,-1.79227059055215E-17,0.));
#41075=CARTESIAN_POINT('Ctrl Pts',(-0.146154441698478,7.49371236435786E-5,
0.666065504584291));
#41076=CARTESIAN_POINT('Ctrl Pts',(-0.146245091243546,0.019414808211501,
0.665017148521823));
#41077=CARTESIAN_POINT('Ctrl Pts',(-0.142674700046404,0.0387225584902945,
0.663968792459356));
#41078=CARTESIAN_POINT('Ctrl Pts',(-0.135284782149148,0.0564369123056677,
0.662920436396889));
#41079=CARTESIAN_POINT('Ctrl Pts',(-0.116721776970831,0.100934245858918,
0.660287032442087));
#41080=CARTESIAN_POINT('Ctrl Pts',(-0.074058225042023,0.13537752586737,
0.657653628487285));
#41081=CARTESIAN_POINT('Ctrl Pts',(-0.0266475060286977,0.144142317777245,
0.655020224532483));
#41082=CARTESIAN_POINT('Ctrl Pts',(0.020763212984627,0.15290710968712,0.652386820577681));
#41083=CARTESIAN_POINT('Ctrl Pts',(0.0729210990824686,0.13599341349842,
0.649753416622878));
#41084=CARTESIAN_POINT('Ctrl Pts',(0.106165877238123,0.101073754565802,
0.647120012668076));
#41085=CARTESIAN_POINT('Ctrl Pts',(0.139410655393777,0.0661540956331838,
0.644486608713273));
#41086=CARTESIAN_POINT('Ctrl Pts',(0.153742325607243,0.0132284739566488,
0.641853204758471));
#41087=CARTESIAN_POINT('Ctrl Pts',(0.142659641677727,-0.0336945691193152,
0.639219800803669));
#41088=CARTESIAN_POINT('Ctrl Pts',(0.13157695774821,-0.0806176121952798,
0.636586396848867));
#41089=CARTESIAN_POINT('Ctrl Pts',(0.09507991967571,-0.121538076670673,
0.633952992894065));
#41090=CARTESIAN_POINT('Ctrl Pts',(0.049724604077795,-0.137893296070049,
0.631319588939263));
#41091=CARTESIAN_POINT('Ctrl Pts',(0.00436928847988189,-0.154248515469425,
0.62868618498446));
#41092=CARTESIAN_POINT('Ctrl Pts',(-0.0498443046434454,-0.146038489792785,
0.626052781029658));
#41093=CARTESIAN_POINT('Ctrl Pts',(-0.0883233740987275,-0.116987516169781,
0.623419377074855));
#41094=CARTESIAN_POINT('Ctrl Pts',(-0.1241414224228,-0.0899455634453427,
0.620968086244667));
#41095=CARTESIAN_POINT('Ctrl Pts',(-0.146325940865162,-0.0448455053352938,
0.618516795414479));
#41096=CARTESIAN_POINT('Ctrl Pts',(-0.146555285157174,5.84873774584615E-5,
0.616065504584291));
#41097=CARTESIAN_POINT('Ctrl Pts',(-0.146582406651585,1.90495679610238E-5,
0.608934495415709));
#41098=CARTESIAN_POINT('Ctrl Pts',(-0.146495356123754,-0.0471907653725723,
0.611512933464593));
#41099=CARTESIAN_POINT('Ctrl Pts',(-0.121611930441545,-0.0944794748712001,
0.614091371513477));
#41100=CARTESIAN_POINT('Ctrl Pts',(-0.0826169041730041,-0.121085801253764,
0.616669809562361));
#41101=CARTESIAN_POINT('Ctrl Pts',(-0.042761304710591,-0.148279297166989,
0.619305150628866));
#41102=CARTESIAN_POINT('Ctrl Pts',(0.0118356201414113,-0.153867466492291,
0.621940491695373));
#41103=CARTESIAN_POINT('Ctrl Pts',(0.0563737778341691,-0.135311940689286,
0.624575832761878));
#41104=CARTESIAN_POINT('Ctrl Pts',(0.100911935526926,-0.116756414886282,
0.627211173828384));
#41105=CARTESIAN_POINT('Ctrl Pts',(0.135391326060439,-0.0740571939549723,
0.62984651489489));
#41106=CARTESIAN_POINT('Ctrl Pts',(0.144150040296483,-0.0266099605959858,
0.632481855961396));
#41107=CARTESIAN_POINT('Ctrl Pts',(0.152908754532526,0.0208372727630014,
0.635117197027901));
#41108=CARTESIAN_POINT('Ctrl Pts',(0.135946792471101,0.0730325185496646,
0.637752538094407));
#41109=CARTESIAN_POINT('Ctrl Pts',(0.100968951224381,0.106266622271745,
0.640387879160913));
#41110=CARTESIAN_POINT('Ctrl Pts',(0.0659911099776614,0.139500725993825,
0.643023220227419));
#41111=CARTESIAN_POINT('Ctrl Pts',(0.0129973895456473,0.153773687651321,
0.645658561293925));
#41112=CARTESIAN_POINT('Ctrl Pts',(-0.0339403566699702,0.14260216095667,
0.648293902360431));
#41113=CARTESIAN_POINT('Ctrl Pts',(-0.0808781028855877,0.131430634262018,
0.650929243426936));
#41114=CARTESIAN_POINT('Ctrl Pts',(-0.121759874884809,0.0948146192152183,
0.653564584493442));
#41115=CARTESIAN_POINT('Ctrl Pts',(-0.138015547484023,0.0493865647021963,
0.656199925559948));
#41116=CARTESIAN_POINT('Ctrl Pts',(-0.143638130564433,0.0336737106740469,
0.657111448845201));
#41117=CARTESIAN_POINT('Ctrl Pts',(-0.146314545676077,0.0169066195134479,
0.658022972130455));
#41118=CARTESIAN_POINT('Ctrl Pts',(-0.14620212788816,0.000104817362006062,
0.658934495415709));
#41119=CARTESIAN_POINT('Origin',(0.,0.,0.));
#41120=CARTESIAN_POINT('',(-0.146293122286189,-0.000127967976324597,0.716065504584291));
#41121=CARTESIAN_POINT('',(-0.146220133725287,-0.000111981377959844,0.708934495415709));
#41122=CARTESIAN_POINT('',(-0.14635,-1.79227059055215E-17,0.));
#41123=CARTESIAN_POINT('Ctrl Pts',(-0.146293122286189,-0.000127967976324597,
0.716065504584291));
#41124=CARTESIAN_POINT('Ctrl Pts',(-0.145991055868361,0.035107698155652,
0.714150905583971));
#41125=CARTESIAN_POINT('Ctrl Pts',(-0.133191339997662,0.0705402609933279,
0.71223630658365));
#41126=CARTESIAN_POINT('Ctrl Pts',(-0.110030394316881,0.0968525150836482,
0.71032170758333));
#41127=CARTESIAN_POINT('Ctrl Pts',(-0.0781740494934874,0.133043275639576,
0.707688303628528));
#41128=CARTESIAN_POINT('Ctrl Pts',(-0.0267161455114648,0.151980073612578,
0.705054899673726));
#41129=CARTESIAN_POINT('Ctrl Pts',(0.0210005740720494,0.145072648144428,
0.702421495718924));
#41130=CARTESIAN_POINT('Ctrl Pts',(0.0687172936555642,0.138165222676278,
0.699788091764121));
#41131=CARTESIAN_POINT('Ctrl Pts',(0.112692828840571,0.105413573766977,
0.697154687809319));
#41132=CARTESIAN_POINT('Ctrl Pts',(0.132978647675338,0.0616747648126076,
0.694521283854517));
#41133=CARTESIAN_POINT('Ctrl Pts',(0.153264466510106,0.0179359558582386,
0.691887879899714));
#41134=CARTESIAN_POINT('Ctrl Pts',(0.149860568994636,-0.0367900131411976,
0.689254475944912));
#41135=CARTESIAN_POINT('Ctrl Pts',(0.124311058190535,-0.0776779129690893,
0.68662107199011));
#41136=CARTESIAN_POINT('Ctrl Pts',(0.0987615473864338,-0.11856581279698,
0.683987668035308));
#41137=CARTESIAN_POINT('Ctrl Pts',(0.0510664232937013,-0.145615643453328,
0.681354264080505));
#41138=CARTESIAN_POINT('Ctrl Pts',(0.00286152734998743,-0.146556845670501,
0.678720860125703));
#41139=CARTESIAN_POINT('Ctrl Pts',(-0.0453433685937279,-0.147498047887674,
0.6760874561709));
#41140=CARTESIAN_POINT('Ctrl Pts',(-0.094058036388424,-0.122330621665673,
0.673454052216099));
#41141=CARTESIAN_POINT('Ctrl Pts',(-0.121184141071859,-0.082471215005648,
0.670820648261296));
#41142=CARTESIAN_POINT('Ctrl Pts',(-0.137511364617388,-0.0584798070786627,
0.669235600368961));
#41143=CARTESIAN_POINT('Ctrl Pts',(-0.146017385334238,-0.0291657216594994,
0.667650552476626));
#41144=CARTESIAN_POINT('Ctrl Pts',(-0.146154441698478,7.49371236435786E-5,
0.666065504584291));
#41145=CARTESIAN_POINT('Ctrl Pts',(-0.14620212788816,0.000104817362006062,
0.658934495415709));
#41146=CARTESIAN_POINT('Ctrl Pts',(-0.145989530157664,-0.0316697360413935,
0.660658313196961));
#41147=CARTESIAN_POINT('Ctrl Pts',(-0.135802925380645,-0.0635684301444077,
0.662382130978214));
#41148=CARTESIAN_POINT('Ctrl Pts',(-0.116706447513916,-0.088695711446933,
0.664105948759466));
#41149=CARTESIAN_POINT('Ctrl Pts',(-0.0875121017453893,-0.127109839103795,
0.666741289825971));
#41150=CARTESIAN_POINT('Ctrl Pts',(-0.0374938370091297,-0.149698000438276,
0.669376630892477));
#41151=CARTESIAN_POINT('Ctrl Pts',(0.0106280634930049,-0.146199755084551,
0.672011971958983));
#41152=CARTESIAN_POINT('Ctrl Pts',(0.0587499639951401,-0.142701509730827,
0.674647313025488));
#41153=CARTESIAN_POINT('Ctrl Pts',(0.104975500263151,-0.113116857688896,
0.677282654091995));
#41154=CARTESIAN_POINT('Ctrl Pts',(0.128307197060476,-0.0708843233930653,
0.679917995158501));
#41155=CARTESIAN_POINT('Ctrl Pts',(0.1516388938578,-0.0286517890972343,
0.682553336225006));
#41156=CARTESIAN_POINT('Ctrl Pts',(0.152076751184439,0.0262286274524959,
0.685188677291512));
#41157=CARTESIAN_POINT('Ctrl Pts',(0.129421876845612,0.06882806051419,0.687824018358017));
#41158=CARTESIAN_POINT('Ctrl Pts',(0.106767002506784,0.111427493575885,
0.690459359424523));
#41159=CARTESIAN_POINT('Ctrl Pts',(0.0610193965024891,0.141745943149541,
0.69309470049103));
#41160=CARTESIAN_POINT('Ctrl Pts',(0.0129594391535466,0.146011564806377,
0.695730041557535));
#41161=CARTESIAN_POINT('Ctrl Pts',(-0.0351005181953946,0.150277186463213,
0.698365382624041));
#41162=CARTESIAN_POINT('Ctrl Pts',(-0.0854728268889839,0.128489980203229,
0.701000723690547));
#41163=CARTESIAN_POINT('Ctrl Pts',(-0.115276382892,0.0905465607729482,0.703636064757053));
#41164=CARTESIAN_POINT('Ctrl Pts',(-0.135250024617843,0.0651177741718751,
0.705402208309938));
#41165=CARTESIAN_POINT('Ctrl Pts',(-0.145985488943994,0.0324326426859288,
0.707168351862824));
#41166=CARTESIAN_POINT('Ctrl Pts',(-0.146220133725287,-0.000111981377959844,
0.708934495415709));
#41167=CARTESIAN_POINT('Origin',(0.,0.,0.));
#41168=CARTESIAN_POINT('',(-0.146564965442509,4.80374956639621E-5,0.766065504584291));
#41169=CARTESIAN_POINT('',(-0.14658533994215,-4.90005960534454E-6,0.758934495415709));
#41170=CARTESIAN_POINT('',(-0.14635,-1.79227059055215E-17,0.));
#41171=CARTESIAN_POINT('Ctrl Pts',(-0.146564965442509,4.80374956639621E-5,
0.766065504584291));
#41172=CARTESIAN_POINT('Ctrl Pts',(-0.146576599691724,0.00274840678048242,
0.76591806660092));
#41173=CARTESIAN_POINT('Ctrl Pts',(-0.146508366823243,0.00544817658194007,
0.765770628617549));
#41174=CARTESIAN_POINT('Ctrl Pts',(-0.146358404344074,0.00814339894155673,
0.765623190634177));
#41175=CARTESIAN_POINT('Ctrl Pts',(-0.14367991012782,0.0562830238780745,
0.762989786679375));
#41176=CARTESIAN_POINT('Ctrl Pts',(-0.11492813804623,0.102971929623608,
0.760356382724573));
#41177=CARTESIAN_POINT('Ctrl Pts',(-0.0731456970048765,0.127030722191848,
0.757722978769771));
#41178=CARTESIAN_POINT('Ctrl Pts',(-0.031363255963523,0.151089514760089,
0.755089574814969));
#41179=CARTESIAN_POINT('Ctrl Pts',(0.023449854037593,0.152518194151036,
0.752456170860167));
#41180=CARTESIAN_POINT('Ctrl Pts',(0.0664288749466077,0.130668672151013,
0.749822766905364));
#41181=CARTESIAN_POINT('Ctrl Pts',(0.109407895855622,0.108819150150991,
0.747189362950562));
#41182=CARTESIAN_POINT('Ctrl Pts',(0.140552827672535,0.0636914267599971,
0.744555958995759));
#41183=CARTESIAN_POINT('Ctrl Pts',(0.145735458379408,0.0157566983326864,
0.741922555040957));
#41184=CARTESIAN_POINT('Ctrl Pts',(0.150918089086281,-0.0321780300946251,
0.739289151086155));
#41185=CARTESIAN_POINT('Ctrl Pts',(0.130138418683114,-0.0829197635582554,
0.736655747131352));
#41186=CARTESIAN_POINT('Ctrl Pts',(0.0928226866975336,-0.113450633258391,
0.73402234317655));
#41187=CARTESIAN_POINT('Ctrl Pts',(0.0555069547119538,-0.143981502958525,
0.731388939221748));
#41188=CARTESIAN_POINT('Ctrl Pts',(0.00165516114396223,-0.154301508895166,
0.728755535266946));
#41189=CARTESIAN_POINT('Ctrl Pts',(-0.0443040153143291,-0.139729208016517,
0.726122131312144));
#41190=CARTESIAN_POINT('Ctrl Pts',(-0.0902631917726212,-0.125156907137867,
0.723488727357341));
#41191=CARTESIAN_POINT('Ctrl Pts',(-0.128329751121212,-0.0856922994439281,
0.720855323402539));
#41192=CARTESIAN_POINT('Ctrl Pts',(-0.141235637963126,-0.0392376340275311,
0.718221919447737));
#41193=CARTESIAN_POINT('Ctrl Pts',(-0.144758384781757,-0.0265575271266455,
0.717503114493255));
#41194=CARTESIAN_POINT('Ctrl Pts',(-0.146406528193996,-0.0133566238911661,
0.716784309538773));
#41195=CARTESIAN_POINT('Ctrl Pts',(-0.146293122286189,-0.000127967976324597,
0.716065504584291));
#41196=CARTESIAN_POINT('Ctrl Pts',(-0.146220133725287,-0.000111981377959844,
0.708934495415709));
#41197=CARTESIAN_POINT('Ctrl Pts',(-0.146335612821056,-0.016128633179466,
0.709803692929329));
#41198=CARTESIAN_POINT('Ctrl Pts',(-0.143907730109974,-0.0321112532361818,
0.71067289044295));
#41199=CARTESIAN_POINT('Ctrl Pts',(-0.138785978242991,-0.047178134378496,
0.71154208795657));
#41200=CARTESIAN_POINT('Ctrl Pts',(-0.123257214278523,-0.0928597774990785,
0.714177429023076));
#41201=CARTESIAN_POINT('Ctrl Pts',(-0.0829648830371437,-0.130123431139663,
0.716812770089582));
#41202=CARTESIAN_POINT('Ctrl Pts',(-0.0362113622873864,-0.142042463234138,
0.719448111156088));
#41203=CARTESIAN_POINT('Ctrl Pts',(0.0105421584623702,-0.153961495328613,
0.722083452222593));
#41204=CARTESIAN_POINT('Ctrl Pts',(0.063756868720506,-0.140535905876979,
0.724718793289099));
#41205=CARTESIAN_POINT('Ctrl Pts',(0.0992605327204626,-0.107864131039655,
0.727354134355605));
#41206=CARTESIAN_POINT('Ctrl Pts',(0.13476419672042,-0.075192356202331,
0.729989475422111));
#41207=CARTESIAN_POINT('Ctrl Pts',(0.152556814462199,-0.0232743959793195,
0.732624816488617));
#41208=CARTESIAN_POINT('Ctrl Pts',(0.144556272029555,0.024306549251931,
0.735260157555123));
#41209=CARTESIAN_POINT('Ctrl Pts',(0.136555729596912,0.0718874944831808,
0.737895498621628));
#41210=CARTESIAN_POINT('Ctrl Pts',(0.102762026989844,0.115131424722669,
0.740530839688134));
#41211=CARTESIAN_POINT('Ctrl Pts',(0.058525606626993,0.13439522866968,0.74316618075464));
#41212=CARTESIAN_POINT('Ctrl Pts',(0.0142891862641413,0.15365903261669,
0.745801521821146));
#41213=CARTESIAN_POINT('Ctrl Pts',(-0.0403899518544944,0.148942710271224,
0.748436862887652));
#41214=CARTESIAN_POINT('Ctrl Pts',(-0.0806743706113798,0.122388602614794,
0.751072203954158));
#41215=CARTESIAN_POINT('Ctrl Pts',(-0.120735958293688,0.0959813775627587,
0.753692967774675));
#41216=CARTESIAN_POINT('Ctrl Pts',(-0.146561633397375,0.047977288078364,
0.756313731595192));
#41217=CARTESIAN_POINT('Ctrl Pts',(-0.14658533994215,-4.90005960534454E-6,
0.758934495415709));
#41218=CARTESIAN_POINT('Origin',(0.,0.,0.));
#41219=CARTESIAN_POINT('',(-0.146164975321328,8.31911013993853E-5,0.816065504584291));
#41220=CARTESIAN_POINT('',(-0.146233275186053,0.000116309547457056,0.808934495415709));
#41221=CARTESIAN_POINT('',(-0.14635,-1.79227059055215E-17,0.));
#41222=CARTESIAN_POINT('Ctrl Pts',(-0.146164975321328,8.31911013993853E-5,
0.816065504584291));
#41223=CARTESIAN_POINT('Ctrl Pts',(-0.146262710135629,0.0187799830896948,
0.815051823663067));
#41224=CARTESIAN_POINT('Ctrl Pts',(-0.142931951335767,0.037443276248974,
0.814038142741842));
#41225=CARTESIAN_POINT('Ctrl Pts',(-0.136010977838838,0.054663650141277,
0.813024461820618));
#41226=CARTESIAN_POINT('Ctrl Pts',(-0.118031238261729,0.0993998188524282,
0.810391057865816));
#41227=CARTESIAN_POINT('Ctrl Pts',(-0.0758215305972079,0.13439788253602,
0.807757653911014));
#41228=CARTESIAN_POINT('Ctrl Pts',(-0.028529425342275,0.143781679589591,
0.805124249956212));
#41229=CARTESIAN_POINT('Ctrl Pts',(0.0187626799126572,0.153165476643161,
0.80249084600141));
#41230=CARTESIAN_POINT('Ctrl Pts',(0.0711371827580015,0.136935007066712,
0.799857442046606));
#41231=CARTESIAN_POINT('Ctrl Pts',(0.104835580177757,0.102452897995539,
0.797224038091804));
#41232=CARTESIAN_POINT('Ctrl Pts',(0.138533977597513,0.0679707889243652,
0.794590634137002));
#41233=CARTESIAN_POINT('Ctrl Pts',(0.15355626959168,0.0152370403584678,
0.791957230182201));
#41234=CARTESIAN_POINT('Ctrl Pts',(0.143087905965057,-0.0318268624597296,
0.789323826227399));
#41235=CARTESIAN_POINT('Ctrl Pts',(0.132619542338435,-0.0788907652779263,
0.786690422272596));
#41236=CARTESIAN_POINT('Ctrl Pts',(0.096660523091021,-0.120284822348423,
0.784057018317793));
#41237=CARTESIAN_POINT('Ctrl Pts',(0.0515228742830193,-0.137231523355512,
0.781423614362991));
#41238=CARTESIAN_POINT('Ctrl Pts',(0.00638522547501753,-0.1541782243626,
0.778790210408188));
#41239=CARTESIAN_POINT('Ctrl Pts',(-0.0479310528935715,-0.146677569306282,
0.776156806453387));
#41240=CARTESIAN_POINT('Ctrl Pts',(-0.0867865839024083,-0.118132069714372,
0.773523402498585));
#41241=CARTESIAN_POINT('Ctrl Pts',(-0.123466686745614,-0.0911847643100577,
0.771037436527154));
#41242=CARTESIAN_POINT('Ctrl Pts',(-0.146368799251201,-0.045483147880463,
0.768551470555722));
#41243=CARTESIAN_POINT('Ctrl Pts',(-0.146564965442509,4.80374956639621E-5,
0.766065504584291));
#41244=CARTESIAN_POINT('Ctrl Pts',(-0.14658533994215,-4.90005960534454E-6,
0.758934495415709));
#41245=CARTESIAN_POINT('Ctrl Pts',(-0.146609310208618,-0.0485208624767226,
0.761584413728203));
#41246=CARTESIAN_POINT('Ctrl Pts',(-0.120122621218798,-0.0970137112575841,
0.764234332040698));
#41247=CARTESIAN_POINT('Ctrl Pts',(-0.0793243537302287,-0.123267883191947,
0.766884250353192));
#41248=CARTESIAN_POINT('Ctrl Pts',(-0.0387505182093485,-0.149377630477176,
0.769519591419698));
#41249=CARTESIAN_POINT('Ctrl Pts',(0.0159771533787021,-0.153492702582488,
0.772154932486204));
#41250=CARTESIAN_POINT('Ctrl Pts',(0.0599991778729333,-0.13374387011901,
0.77479027355271));
#41251=CARTESIAN_POINT('Ctrl Pts',(0.104021202367166,-0.113995037655531,
0.777425614619216));
#41252=CARTESIAN_POINT('Ctrl Pts',(0.13733757976758,-0.0703823006232647,
0.780060955685721));
#41253=CARTESIAN_POINT('Ctrl Pts',(0.14481468818493,-0.022716297290398,
0.782696296752227));
#41254=CARTESIAN_POINT('Ctrl Pts',(0.152291796602279,0.0249497060424673,
0.785331637818733));
#41255=CARTESIAN_POINT('Ctrl Pts',(0.133929636036564,0.0766689756759309,
0.787966978885239));
#41256=CARTESIAN_POINT('Ctrl Pts',(0.0980690284933123,0.108948564888508,
0.790602319951745));
#41257=CARTESIAN_POINT('Ctrl Pts',(0.0622084209500598,0.141228154101085,
0.793237661018251));
#41258=CARTESIAN_POINT('Ctrl Pts',(0.00884936642926935,0.154068062892775,
0.795873002084756));
#41259=CARTESIAN_POINT('Ctrl Pts',(-0.0377703306973942,0.141635893595607,
0.798508343151262));
#41260=CARTESIAN_POINT('Ctrl Pts',(-0.084390027824057,0.129203724298439,
0.801143684217768));
#41261=CARTESIAN_POINT('Ctrl Pts',(-0.124270367556593,0.0914994769124139,
0.803779025284273));
#41262=CARTESIAN_POINT('Ctrl Pts',(-0.139296118286606,0.0456499204587224,
0.806414366350779));
#41263=CARTESIAN_POINT('Ctrl Pts',(-0.144085736300807,0.0310348862098803,
0.807254409372422));
#41264=CARTESIAN_POINT('Ctrl Pts',(-0.146349920545361,0.0155922205493257,
0.808094452394066));
#41265=CARTESIAN_POINT('Ctrl Pts',(-0.146233275186053,0.000116309547457056,
0.808934495415709));
#41266=CARTESIAN_POINT('Origin',(0.,0.,0.));
#41267=CARTESIAN_POINT('',(-0.146273246343463,-0.000123611542196964,0.866065504584292));
#41268=CARTESIAN_POINT('',(-0.146190615322833,-9.92620605964336E-5,0.858934495415709));
#41269=CARTESIAN_POINT('',(-0.14635,-1.79227059055215E-17,0.));
#41270=CARTESIAN_POINT('Ctrl Pts',(-0.146273246343463,-0.000123611542196964,
0.866065504584292));
#41271=CARTESIAN_POINT('Ctrl Pts',(-0.14598570205562,0.0344841852260994,
0.864185580725214));
#41272=CARTESIAN_POINT('Ctrl Pts',(-0.13368920007778,0.0692748383916789,
0.862305656866136));
#41273=CARTESIAN_POINT('Ctrl Pts',(-0.111287960012964,0.0954050911579531,
0.860425733007059));
#41274=CARTESIAN_POINT('Ctrl Pts',(-0.0799082241293448,0.13200844115132,
0.857792329052257));
#41275=CARTESIAN_POINT('Ctrl Pts',(-0.0287004609307042,0.151617916172533,
0.855158925097454));
#41276=CARTESIAN_POINT('Ctrl Pts',(0.0191028994225217,0.145335216041435,
0.852525521142652));
#41277=CARTESIAN_POINT('Ctrl Pts',(0.0669062597757476,0.139052515910338,
0.84989211718785));
#41278=CARTESIAN_POINT('Ctrl Pts',(0.111305217283559,0.10687764062693,0.847258713233048));
#41279=CARTESIAN_POINT('Ctrl Pts',(0.132160826244895,0.0634075368078452,
0.844625309278246));
#41280=CARTESIAN_POINT('Ctrl Pts',(0.15301643520623,0.0199374329887607,
0.841991905323443));
#41281=CARTESIAN_POINT('Ctrl Pts',(0.15032869562109,-0.0348278993660004,
0.839358501368641));
#41282=CARTESIAN_POINT('Ctrl Pts',(0.12531596597325,-0.076046177073106,
0.836725097413839));
#41283=CARTESIAN_POINT('Ctrl Pts',(0.10030323632541,-0.117264454780212,
0.834091693459036));
#41284=CARTESIAN_POINT('Ctrl Pts',(0.0529655166148703,-0.144935677839662,
0.831458289504234));
#41285=CARTESIAN_POINT('Ctrl Pts',(0.00477698054298851,-0.14650698356075,
0.828824885549432));
#41286=CARTESIAN_POINT('Ctrl Pts',(-0.0434115555288926,-0.148078289281839,
0.826191481594629));
#41287=CARTESIAN_POINT('Ctrl Pts',(-0.0924509079621152,-0.123549677664568,
0.823558077639828));
#41288=CARTESIAN_POINT('Ctrl Pts',(-0.120095698433879,-0.084048234986577,
0.820924673685025));
#41289=CARTESIAN_POINT('Ctrl Pts',(-0.137099129982578,-0.059752153692848,
0.819304950651447));
#41290=CARTESIAN_POINT('Ctrl Pts',(-0.146008808497438,-0.0297917172680741,
0.817685227617869));
#41291=CARTESIAN_POINT('Ctrl Pts',(-0.146164975321328,8.31911013993853E-5,
0.816065504584291));
#41292=CARTESIAN_POINT('Ctrl Pts',(-0.146233275186053,0.000116309547457056,
0.808934495415709));
#41293=CARTESIAN_POINT('Ctrl Pts',(-0.145983986542363,-0.0329580355137906,
0.810729793460572));
#41294=CARTESIAN_POINT('Ctrl Pts',(-0.134860471440613,-0.0661842257005933,
0.812525091505434));
#41295=CARTESIAN_POINT('Ctrl Pts',(-0.114274246165196,-0.0918080661847913,
0.814320389550297));
#41296=CARTESIAN_POINT('Ctrl Pts',(-0.0840554615862833,-0.129421630853252,
0.816955730616803));
#41297=CARTESIAN_POINT('Ctrl Pts',(-0.0334467307009701,-0.150653894668816,
0.819591071683309));
#41298=CARTESIAN_POINT('Ctrl Pts',(0.0145634383780638,-0.145860313412396,
0.822226412749814));
#41299=CARTESIAN_POINT('Ctrl Pts',(0.0625736074570984,-0.141066732155975,
0.82486175381632));
#41300=CARTESIAN_POINT('Ctrl Pts',(0.107985214729854,-0.110247305827569,
0.827497094882826));
#41301=CARTESIAN_POINT('Ctrl Pts',(0.130170526119325,-0.0674014545208048,
0.830132435949332));
#41302=CARTESIAN_POINT('Ctrl Pts',(0.152355837508797,-0.0245556032140414,
0.832767777015837));
#41303=CARTESIAN_POINT('Ctrl Pts',(0.151314853014986,0.0303166730710795,
0.835403118082343));
#41304=CARTESIAN_POINT('Ctrl Pts',(0.127520386856677,0.0722902292399131,
0.838038459148849));
#41305=CARTESIAN_POINT('Ctrl Pts',(0.103725920698368,0.114263785408748,
0.840673800215355));
#41306=CARTESIAN_POINT('Ctrl Pts',(0.0571779728755602,0.143338621461295,
0.843309141281861));
#41307=CARTESIAN_POINT('Ctrl Pts',(0.00902055110528975,0.146307747926884,
0.845944482348367));
#41308=CARTESIAN_POINT('Ctrl Pts',(-0.0391368706649794,0.149276874392473,
0.848579823414872));
#41309=CARTESIAN_POINT('Ctrl Pts',(-0.088903766382711,0.126140291271107,
0.851215164481378));
#41310=CARTESIAN_POINT('Ctrl Pts',(-0.117674187241089,0.087407636925452,
0.853850505547884));
#41311=CARTESIAN_POINT('Ctrl Pts',(-0.136175085157248,0.0625004974853221,
0.855545168837159));
#41312=CARTESIAN_POINT('Ctrl Pts',(-0.145993587468369,0.0311441202011877,
0.857239832126434));
#41313=CARTESIAN_POINT('Ctrl Pts',(-0.146190615322833,-9.92620605964336E-5,
0.858934495415709));
#41314=CARTESIAN_POINT('Origin',(0.,0.,-0.0924367114736152));
#41315=CARTESIAN_POINT('',(-0.117713232580125,-9.94762513365651E-5,0.882563288526385));
#41316=CARTESIAN_POINT('',(-0.11796233779121,-2.11776828218935E-5,0.892436711473616));
#41317=CARTESIAN_POINT('',(-0.117775,-1.30487598617993E-14,-0.0924367114736152));
#41318=CARTESIAN_POINT('',(-0.11766859746431,0.00500517689819253,0.932224999999999));
#41319=CARTESIAN_POINT('Ctrl Pts',(-0.117713232580125,-9.94762513365794E-5,
0.882563288526385));
#41320=CARTESIAN_POINT('Ctrl Pts',(-0.117805978893427,-0.0112620890991194,
0.88331676862211));
#41321=CARTESIAN_POINT('Ctrl Pts',(-0.111244449407799,-0.0613316426944826,
0.886703652672637));
#41322=CARTESIAN_POINT('Ctrl Pts',(-0.0402800891732956,-0.133026134299755,
0.892723940677965));
#41323=CARTESIAN_POINT('Ctrl Pts',(0.0894243408305711,-0.10638650575871,
0.900624152542373));
#41324=CARTESIAN_POINT('Ctrl Pts',(0.137929356340621,0.0167100404698593,
0.908524364406779));
#41325=CARTESIAN_POINT('Ctrl Pts',(0.0614290966487016,0.124766721395902,
0.916424576271187));
#41326=CARTESIAN_POINT('Ctrl Pts',(-0.0710668305166857,0.11939070761148,
0.924324788135593));
#41327=CARTESIAN_POINT('Ctrl Pts',(-0.116012267804409,0.0439444575637681,
0.929591596045198));
#41328=CARTESIAN_POINT('Ctrl Pts',(-0.11766859746431,0.00500517689817995,
0.932225));
#41329=CARTESIAN_POINT('',(-0.0334019664626758,0.112939183906323,0.932224999999999));
#41330=CARTESIAN_POINT('Origin',(0.,0.,0.932225));
#41331=CARTESIAN_POINT('Ctrl Pts',(-0.11796233779121,-2.11776828218909E-5,
0.892436711473617));
#41332=CARTESIAN_POINT('Ctrl Pts',(-0.117965690360961,-0.00128932424828905,
0.892522768983215));
#41333=CARTESIAN_POINT('Ctrl Pts',(-0.117371901374032,-0.0413888390951994,
0.89524416755932));
#41334=CARTESIAN_POINT('Ctrl Pts',(-0.0720261204166176,-0.118897020856024,
0.90060090720193));
#41335=CARTESIAN_POINT('Ctrl Pts',(0.0602520802431792,-0.125231345176025,
0.908506930401448));
#41336=CARTESIAN_POINT('Ctrl Pts',(0.137949690524835,-0.017881538827179,
0.916412953600965));
#41337=CARTESIAN_POINT('Ctrl Pts',(0.0900118016872842,0.105886249500893,
0.924318976800482));
#41338=CARTESIAN_POINT('Ctrl Pts',(0.00399973323748277,0.12400080376067,
0.929589658933494));
#41339=CARTESIAN_POINT('Ctrl Pts',(-0.0334019664626807,0.112939183906322,
0.932225));
#41340=CARTESIAN_POINT('Origin',(0.,0.,-0.0924367114736152));
#41341=CARTESIAN_POINT('',(-0.117626101595281,6.69479464755203E-5,0.832563288526385));
#41342=CARTESIAN_POINT('',(-0.117646735358023,-7.98810330651378E-5,0.842436711473617));
#41343=CARTESIAN_POINT('',(-0.117775,-1.30487598617993E-14,-0.0924367114736152));
#41344=CARTESIAN_POINT('Ctrl Pts',(-0.117626101595281,6.69479464755242E-5,
0.832563288526385));
#41345=CARTESIAN_POINT('Ctrl Pts',(-0.117500426517155,-0.023974851392196,
0.834183011559963));
#41346=CARTESIAN_POINT('Ctrl Pts',(-0.0986730411655657,-0.0872854052949152,
0.838436138548343));
#41347=CARTESIAN_POINT('Ctrl Pts',(0.00452896330992775,-0.13890521184416,
0.845322669491525));
#41348=CARTESIAN_POINT('Ctrl Pts',(0.118813895436517,-0.0721000537472655,
0.853222881355933));
#41349=CARTESIAN_POINT('Ctrl Pts',(0.125302761776928,0.0601169674638447,
0.861123093220339));
#41350=CARTESIAN_POINT('Ctrl Pts',(0.0181127265090936,0.137795052940508,
0.869023305084746));
#41351=CARTESIAN_POINT('Ctrl Pts',(-0.0937244491952465,0.0949681812626695,
0.876170036853428));
#41352=CARTESIAN_POINT('Ctrl Pts',(-0.11748183163376,0.0277511097711188,
0.880683364667308));
#41353=CARTESIAN_POINT('Ctrl Pts',(-0.117713232580125,-9.94762513365794E-5,
0.882563288526385));
#41354=CARTESIAN_POINT('Ctrl Pts',(-0.117646735358023,-7.9881033065143E-5,
0.842436711473617));
#41355=CARTESIAN_POINT('Ctrl Pts',(-0.117734748084911,-0.0140363608293074,
0.843377389250847));
#41356=CARTESIAN_POINT('Ctrl Pts',(-0.108999987861276,-0.0669858868324248,
0.846953408094583));
#41357=CARTESIAN_POINT('Ctrl Pts',(-0.0306982239304521,-0.135581215292453,
0.853164768004825));
#41358=CARTESIAN_POINT('Ctrl Pts',(0.0968538014257187,-0.0997179081430208,
0.861070791204343));
#41359=CARTESIAN_POINT('Ctrl Pts',(0.136419444538435,0.0267352712365894,
0.86897681440386));
#41360=CARTESIAN_POINT('Ctrl Pts',(0.0520445414416943,0.128903423908239,
0.876882837603378));
#41361=CARTESIAN_POINT('Ctrl Pts',(-0.0781668699995673,0.11412164151165,
0.884702803293296));
#41362=CARTESIAN_POINT('Ctrl Pts',(-0.117863024541527,0.0375451567622119,
0.889887427916709));
#41363=CARTESIAN_POINT('Ctrl Pts',(-0.11796233779121,-2.11776828218909E-5,
0.892436711473617));
#41364=CARTESIAN_POINT('Origin',(0.,0.,-0.0924367114736152));
#41365=CARTESIAN_POINT('',(-0.117947993201171,3.86581212928119E-5,0.782563288526384));
#41366=CARTESIAN_POINT('',(-0.117681065835582,9.35999791555828E-5,0.792436711473616));
#41367=CARTESIAN_POINT('',(-0.117775,-1.30487598617993E-14,-0.0924367114736152));
#41368=CARTESIAN_POINT('Ctrl Pts',(-0.117947993201171,3.86581212928078E-5,
0.782563288526385));
#41369=CARTESIAN_POINT('Ctrl Pts',(-0.117790128676528,-0.0366025127545069,
0.785049254497816));
#41370=CARTESIAN_POINT('Ctrl Pts',(-0.0798361540276521,-0.112340416450435,
0.790168624424051));
#41371=CARTESIAN_POINT('Ctrl Pts',(0.0488494678181175,-0.130110898691923,
0.797921398305084));
#41372=CARTESIAN_POINT('Ctrl Pts',(0.135663410254684,-0.0301754342953877,
0.805821610169492));
#41373=CARTESIAN_POINT('Ctrl Pts',(0.0993958918478579,0.0971368425207782,
0.813721822033898));
#41374=CARTESIAN_POINT('Ctrl Pts',(-0.0270490771841315,0.136321199631122,
0.821622033898304));
#41375=CARTESIAN_POINT('Ctrl Pts',(-0.10806095418056,0.0691504233541856,
0.827902522729134));
#41376=CARTESIAN_POINT('Ctrl Pts',(-0.11770475357857,0.0151131705390384,
0.831549607605161));
#41377=CARTESIAN_POINT('Ctrl Pts',(-0.117626101595281,6.69479464755242E-5,
0.832563288526385));
#41378=CARTESIAN_POINT('Ctrl Pts',(-0.117681065835582,9.35999791555758E-5,
0.792436711473616));
#41379=CARTESIAN_POINT('Ctrl Pts',(-0.117480451076367,-0.0265229424847173,
0.794232009518479));
#41380=CARTESIAN_POINT('Ctrl Pts',(-0.0953885925249484,-0.0925118216380055,
0.798662648629848));
#41381=CARTESIAN_POINT('Ctrl Pts',(0.0138111005924944,-0.138325195186183,
0.80572862880772));
#41382=CARTESIAN_POINT('Ctrl Pts',(0.123445922182148,-0.0639194978340518,
0.813634652007238));
#41383=CARTESIAN_POINT('Ctrl Pts',(0.120932728835538,0.0685557124046954,
0.821540675206756));
#41384=CARTESIAN_POINT('Ctrl Pts',(0.0085545008581314,0.138749538494654,
0.829446698406273));
#41385=CARTESIAN_POINT('Ctrl Pts',(-0.0972993756118875,0.0895381706496827,
0.83641204382856));
#41386=CARTESIAN_POINT('Ctrl Pts',(-0.117488177410916,0.0250631961509614,
0.840742048184341));
#41387=CARTESIAN_POINT('Ctrl Pts',(-0.117646735358023,-7.9881033065143E-5,
0.842436711473617));
#41388=CARTESIAN_POINT('Origin',(0.,0.,-0.0924367114736152));
#41389=CARTESIAN_POINT('',(-0.117729227722965,-0.000102982086865302,0.732563288526385));
#41390=CARTESIAN_POINT('',(-0.117964389557135,-3.94331754086097E-6,0.742436711473616));
#41391=CARTESIAN_POINT('',(-0.117775,-1.30487598617993E-14,-0.0924367114736152));
#41392=CARTESIAN_POINT('Ctrl Pts',(-0.117729227722965,-0.000102982086865302,
0.732563288526385));
#41393=CARTESIAN_POINT('Ctrl Pts',(-0.117820491001352,-0.0107487282458691,
0.733282093480867));
#41394=CARTESIAN_POINT('Ctrl Pts',(-0.111634982628329,-0.060291927513671,
0.73663430239015));
#41395=CARTESIAN_POINT('Ctrl Pts',(-0.0420051819866054,-0.132478981273086,
0.742619915254238));
#41396=CARTESIAN_POINT('Ctrl Pts',(0.0880063312515965,-0.107563941317063,
0.750520127118644));
#41397=CARTESIAN_POINT('Ctrl Pts',(0.1381735813042,0.0149391196739674,0.758420338983051));
#41398=CARTESIAN_POINT('Ctrl Pts',(0.0629820334107182,0.123888575547709,
0.766320550847457));
#41399=CARTESIAN_POINT('Ctrl Pts',(-0.069350334823955,0.120439391087123,
0.774220762711865));
#41400=CARTESIAN_POINT('Ctrl Pts',(-0.116921686943853,0.0431900873220952,
0.77963500860484));
#41401=CARTESIAN_POINT('Ctrl Pts',(-0.117957355850309,0.00221177730489086,
0.782415850543013));
#41402=CARTESIAN_POINT('Ctrl Pts',(-0.117947993201171,3.86581212928078E-5,
0.782563288526385));
#41403=CARTESIAN_POINT('Ctrl Pts',(-0.117964389557135,-3.94331754086175E-6,
0.742436711473616));
#41404=CARTESIAN_POINT('Ctrl Pts',(-0.117964495672005,-0.000218720446770248,
0.742451288719605));
#41405=CARTESIAN_POINT('Ctrl Pts',(-0.117867006535742,-0.039261788207105,
0.745101207032099));
#41406=CARTESIAN_POINT('Ctrl Pts',(-0.0752264694457675,-0.116899882557203,
0.750386466411098));
#41407=CARTESIAN_POINT('Ctrl Pts',(0.0568996293847587,-0.126834681679914,
0.758292489610617));
#41408=CARTESIAN_POINT('Ctrl Pts',(0.137333582544999,-0.0215427765762162,
0.766198512810132));
#41409=CARTESIAN_POINT('Ctrl Pts',(0.0930027975645983,0.103320297856606,
0.774104536009652));
#41410=CARTESIAN_POINT('Ctrl Pts',(-0.035819122070238,0.13431900488649,
0.782010559209168));
#41411=CARTESIAN_POINT('Ctrl Pts',(-0.110236635830862,0.0639621230870467,
0.788121284363823));
#41412=CARTESIAN_POINT('Ctrl Pts',(-0.117774936058969,0.0125478221742061,
0.791596668451973));
#41413=CARTESIAN_POINT('Ctrl Pts',(-0.117681065835582,9.35999791555758E-5,
0.792436711473616));
#41414=CARTESIAN_POINT('Origin',(0.,0.,-0.0924367114736152));
#41415=CARTESIAN_POINT('',(-0.117617624673989,6.03055670430245E-5,0.682563288526385));
#41416=CARTESIAN_POINT('',(-0.117670490259622,-9.01168895870441E-5,0.692436711473616));
#41417=CARTESIAN_POINT('',(-0.117775,-1.30487598617993E-14,-0.0924367114736152));
#41418=CARTESIAN_POINT('Ctrl Pts',(-0.117617624673989,6.03055670430289E-5,
0.682563288526385));
#41419=CARTESIAN_POINT('Ctrl Pts',(-0.117507328717046,-0.0234710821212703,
0.68414833641872));
#41420=CARTESIAN_POINT('Ctrl Pts',(-0.0992894616255371,-0.0862548596187289,
0.688366788265857));
#41421=CARTESIAN_POINT('Ctrl Pts',(0.00271304928865532,-0.138952348570324,
0.695218644067796));
#41422=CARTESIAN_POINT('Ctrl Pts',(0.117860843754417,-0.0736473850127282,
0.703118855932203));
#41423=CARTESIAN_POINT('Ctrl Pts',(0.126078691992566,0.0584746033489104,
0.711019067796611));
#41424=CARTESIAN_POINT('Ctrl Pts',(0.0199109026571207,0.137545162630623,
0.718919279661016));
#41425=CARTESIAN_POINT('Ctrl Pts',(-0.0930178497353151,0.0959867468400004,
0.726100686570943));
#41426=CARTESIAN_POINT('Ctrl Pts',(-0.117486140108619,0.0282528811088558,
0.730648689526065));
#41427=CARTESIAN_POINT('Ctrl Pts',(-0.117729227722965,-0.000102982086865302,
0.732563288526385));
#41428=CARTESIAN_POINT('Ctrl Pts',(-0.117670490259622,-9.01168895870632E-5,
0.692436711473616));
#41429=CARTESIAN_POINT('Ctrl Pts',(-0.117763421933718,-0.0129794996427261,
0.693305908987236));
#41430=CARTESIAN_POINT('Ctrl Pts',(-0.109885703418251,-0.0648380928819097,
0.696810447567362));
#41431=CARTESIAN_POINT('Ctrl Pts',(-0.0343406886760894,-0.134704570618338,
0.702950327213994));
#41432=CARTESIAN_POINT('Ctrl Pts',(0.0941327483034478,-0.102291886006113,
0.710856350413511));
#41433=CARTESIAN_POINT('Ctrl Pts',(0.137088516418336,0.0230508765206803,
0.718762373613029));
#41434=CARTESIAN_POINT('Ctrl Pts',(0.0555021824679276,0.127452391053421,
0.726668396812546));
#41435=CARTESIAN_POINT('Ctrl Pts',(-0.0762633445254468,0.116087019895361,
0.734559842766075));
#41436=CARTESIAN_POINT('Ctrl Pts',(-0.117945311741555,0.0386096693093802,
0.739815947653099));
#41437=CARTESIAN_POINT('Ctrl Pts',(-0.117964389557135,-3.94331754086175E-6,
0.742436711473616));
#41438=CARTESIAN_POINT('Origin',(0.,0.,-0.0924367114736152));
#41439=CARTESIAN_POINT('',(-0.117940203002297,4.70676520639361E-5,0.632563288526384));
#41440=CARTESIAN_POINT('',(-0.117656000082187,8.43516556759474E-5,0.642436711473616));
#41441=CARTESIAN_POINT('',(-0.117775,-1.30487598617993E-14,-0.0924367114736152));
#41442=CARTESIAN_POINT('Ctrl Pts',(-0.117940203002297,4.7067652063935E-5,
0.632563288526384));
#41443=CARTESIAN_POINT('Ctrl Pts',(-0.117755638437952,-0.0360893706242894,
0.635014579356573));
#41444=CARTESIAN_POINT('Ctrl Pts',(-0.0807233593759693,-0.111374211355997,
0.640099274141563));
#41445=CARTESIAN_POINT('Ctrl Pts',(0.0471445089225743,-0.130738330601145,
0.647817372881356));
#41446=CARTESIAN_POINT('Ctrl Pts',(0.135257361515437,-0.0319462355497722,
0.655717584745763));
#41447=CARTESIAN_POINT('Ctrl Pts',(0.100657174442164,0.0958292702846084,
0.66361779661017));
#41448=CARTESIAN_POINT('Ctrl Pts',(-0.0252648283287276,0.136663104967713,
0.671518008474576));
#41449=CARTESIAN_POINT('Ctrl Pts',(-0.107599838532302,0.0701921319068488,
0.677833172446648));
#41450=CARTESIAN_POINT('Ctrl Pts',(-0.11769057479473,0.0156240453509343,
0.681514932463917));
#41451=CARTESIAN_POINT('Ctrl Pts',(-0.117617624673989,6.03055670430289E-5,
0.682563288526385));
#41452=CARTESIAN_POINT('Ctrl Pts',(-0.117656000082187,8.43516556759457E-5,
0.642436711473616));
#41453=CARTESIAN_POINT('Ctrl Pts',(-0.117484912294625,-0.0254861849147704,
0.644160529254868));
#41454=CARTESIAN_POINT('Ctrl Pts',(-0.0967548225821553,-0.0904011202578769,
0.648519688102626));
#41455=CARTESIAN_POINT('Ctrl Pts',(0.0100790193068892,-0.138647097388359,
0.655514188016889));
#41456=CARTESIAN_POINT('Ctrl Pts',(0.121678866262096,-0.0672224497442505,
0.663420211216407));
#41457=CARTESIAN_POINT('Ctrl Pts',(0.122735961854403,0.0652724131012164,
0.671326234415924));
#41458=CARTESIAN_POINT('Ctrl Pts',(0.0122899564463577,0.138468628991968,
0.679232257615441));
#41459=CARTESIAN_POINT('Ctrl Pts',(-0.0959511456548746,0.0916518108144888,
0.686269083301339));
#41460=CARTESIAN_POINT('Ctrl Pts',(-0.117481660132417,0.0261001331898457,
0.69067056792073));
#41461=CARTESIAN_POINT('Ctrl Pts',(-0.117670490259622,-9.01168895870632E-5,
0.692436711473616));
#41462=CARTESIAN_POINT('Origin',(0.,0.,-0.0924367114736152));
#41463=CARTESIAN_POINT('',(-0.117743952026517,-0.000104311439111954,0.582563288526385));
#41464=CARTESIAN_POINT('',(-0.11796202899481,1.53301186523688E-5,0.592436711473616));
#41465=CARTESIAN_POINT('',(-0.117775,-1.30487598617993E-14,-0.0924367114736152));
#41466=CARTESIAN_POINT('Ctrl Pts',(-0.117743952026517,-0.000104311439111965,
0.582563288526385));
#41467=CARTESIAN_POINT('Ctrl Pts',(-0.117832850528047,-0.0102332806752188,
0.583247418339623));
#41468=CARTESIAN_POINT('Ctrl Pts',(-0.112015701243022,-0.0592509231652696,
0.586564952107665));
#41469=CARTESIAN_POINT('Ctrl Pts',(-0.0437333382095171,-0.131918576929031,
0.592515889830509));
#41470=CARTESIAN_POINT('Ctrl Pts',(0.0865927525795457,-0.108705156320324,
0.600416101694915));
#41471=CARTESIAN_POINT('Ctrl Pts',(0.138357057429181,0.0131316590523252,
0.608316313559322));
#41472=CARTESIAN_POINT('Ctrl Pts',(0.0645961051971127,0.123054699232873,
0.616216525423729));
#41473=CARTESIAN_POINT('Ctrl Pts',(-0.0677700447892944,0.121335637135943,
0.624116737288135));
#41474=CARTESIAN_POINT('Ctrl Pts',(-0.116658230525945,0.0442240676066805,
0.629565658322354));
#41475=CARTESIAN_POINT('Ctrl Pts',(-0.117953914810415,0.00273174284681649,
0.63238117540177));
#41476=CARTESIAN_POINT('Ctrl Pts',(-0.117940203002297,4.7067652063935E-5,
0.632563288526384));
#41477=CARTESIAN_POINT('Ctrl Pts',(-0.11796202899481,1.53301186523688E-5,
0.592436711473616));
#41478=CARTESIAN_POINT('Ctrl Pts',(-0.11789197517919,-0.0379767160352311,
0.5950151495225));
#41479=CARTESIAN_POINT('Ctrl Pts',(-0.077400231210687,-0.114927628746102,
0.600228928637889));
#41480=CARTESIAN_POINT('Ctrl Pts',(0.0534615168199478,-0.12832174587234,
0.608078048819785));
#41481=CARTESIAN_POINT('Ctrl Pts',(0.136703270562712,-0.0252352939724056,
0.615984072019302));
#41482=CARTESIAN_POINT('Ctrl Pts',(0.0957529101571512,0.100776904302778,
0.623890095218819));
#41483=CARTESIAN_POINT('Ctrl Pts',(-0.0321870028708045,0.135235354440354,
0.631796118418337));
#41484=CARTESIAN_POINT('Ctrl Pts',(-0.109365567925802,0.0661098894434327,
0.637978323836602));
#41485=CARTESIAN_POINT('Ctrl Pts',(-0.117746468172191,0.0136055832811398,
0.641525188188362));
#41486=CARTESIAN_POINT('Ctrl Pts',(-0.117656000082187,8.43516556759457E-5,
0.642436711473616));
#41487=CARTESIAN_POINT('Origin',(0.,0.,-0.0924367114736152));
#41488=CARTESIAN_POINT('',(-0.117610072962214,5.33056148506657E-5,0.532563288526385));
#41489=CARTESIAN_POINT('',(-0.117697192808605,-9.79052972080175E-5,0.542436711473616));
#41490=CARTESIAN_POINT('',(-0.117775,-1.30487598617993E-14,-0.0924367114736152));
#41491=CARTESIAN_POINT('Ctrl Pts',(-0.117610072962214,5.330561485066E-5,
0.532563288526385));
#41492=CARTESIAN_POINT('Ctrl Pts',(-0.117515081084069,-0.02296700464597,
0.534113661277477));
#41493=CARTESIAN_POINT('Ctrl Pts',(-0.0998958154709599,-0.0852230040130838,
0.538297437983371));
#41494=CARTESIAN_POINT('Ctrl Pts',(0.000896453507092177,-0.13897594101512,
0.545114618644068));
#41495=CARTESIAN_POINT('Ctrl Pts',(0.116888066275103,-0.0751817515916976,
0.553014830508475));
#41496=CARTESIAN_POINT('Ctrl Pts',(0.126832290918542,0.0568215257651788,
0.560915042372882));
#41497=CARTESIAN_POINT('Ctrl Pts',(0.0217071709283622,0.137273138451102,
0.568815254237287));
#41498=CARTESIAN_POINT('Ctrl Pts',(-0.0923030266130234,0.097000942567024,
0.576031336288457));
#41499=CARTESIAN_POINT('Ctrl Pts',(-0.117490655726745,0.0287559098676526,
0.580614014384821));
#41500=CARTESIAN_POINT('Ctrl Pts',(-0.117743952026517,-0.000104311439111965,
0.582563288526385));
#41501=CARTESIAN_POINT('Ctrl Pts',(-0.117697192808605,-9.79052972080122E-5,
0.542436711473616));
#41502=CARTESIAN_POINT('Ctrl Pts',(-0.11779135888071,-0.011920519912767,
0.543234428723626));
#41503=CARTESIAN_POINT('Ctrl Pts',(-0.110735559311442,-0.0626905594030618,
0.546667487040141));
#41504=CARTESIAN_POINT('Ctrl Pts',(-0.0379577228913647,-0.133730383672961,
0.552735886423163));
#41505=CARTESIAN_POINT('Ctrl Pts',(0.0913424031974019,-0.104791076063462,
0.56064190962268));
#41506=CARTESIAN_POINT('Ctrl Pts',(0.137659831668342,0.0193487722984857,
0.568547932822197));
#41507=CARTESIAN_POINT('Ctrl Pts',(0.0589161298691768,0.125910658348106,
0.576453956021715));
#41508=CARTESIAN_POINT('Ctrl Pts',(-0.0733516660922674,0.11808529682354,
0.584359979221232));
#41509=CARTESIAN_POINT('Ctrl Pts',(-0.117576903938907,0.0405212291720611,
0.589687564371866));
#41510=CARTESIAN_POINT('Ctrl Pts',(-0.117963574998021,0.000853768751192661,
0.592379808455994));
#41511=CARTESIAN_POINT('Ctrl Pts',(-0.11796202899481,1.53301186523688E-5,
0.592436711473616));
#41512=CARTESIAN_POINT('Origin',(0.,0.,-0.0924367114736152));
#41513=CARTESIAN_POINT('',(-0.117931139389423,5.50751932371175E-5,0.482563288526385));
#41514=CARTESIAN_POINT('',(-0.117634119017629,7.2868354416035E-5,0.492436711473616));
#41515=CARTESIAN_POINT('',(-0.117775,-1.30487598617993E-14,-0.0924367114736152));
#41516=CARTESIAN_POINT('Ctrl Pts',(-0.117931139389423,5.50751932371233E-5,
0.482563288526385));
#41517=CARTESIAN_POINT('Ctrl Pts',(-0.117723480179333,-0.0355774509071747,
0.48497990421533));
#41518=CARTESIAN_POINT('Ctrl Pts',(-0.0815990427908323,-0.11040399129502,
0.490029923859077));
#41519=CARTESIAN_POINT('Ctrl Pts',(0.0454314893010671,-0.131343426138561,
0.497713347457628));
#41520=CARTESIAN_POINT('Ctrl Pts',(0.134828208757446,-0.0337115697229769,
0.505613559322033));
#41521=CARTESIAN_POINT('Ctrl Pts',(0.10190123992053,0.0945053073249706,
0.513513771186441));
#41522=CARTESIAN_POINT('Ctrl Pts',(-0.0234762303627364,0.136981686432473,
0.521413983050847));
#41523=CARTESIAN_POINT('Ctrl Pts',(-0.107129919570411,0.0712336270252472,
0.527763822164162));
#41524=CARTESIAN_POINT('Ctrl Pts',(-0.117676430661069,0.0161344153441048,
0.531480257322675));
#41525=CARTESIAN_POINT('Ctrl Pts',(-0.117610072962214,5.330561485066E-5,
0.532563288526385));
#41526=CARTESIAN_POINT('Ctrl Pts',(-0.117634119017629,7.28683544160419E-5,
0.492436711473616));
#41527=CARTESIAN_POINT('Ctrl Pts',(-0.117494141600147,-0.0244488239796579,
0.494089048991258));
#41528=CARTESIAN_POINT('Ctrl Pts',(-0.0980773705094754,-0.0882836093782272,
0.498376727575405));
#41529=CARTESIAN_POINT('Ctrl Pts',(0.00633962999064621,-0.138868330932566,
0.505299747226058));
#41530=CARTESIAN_POINT('Ctrl Pts',(0.119823436886959,-0.0704765792090683,
0.513205770425575));
#41531=CARTESIAN_POINT('Ctrl Pts',(0.124450111907394,0.0619416975118724,
0.521111793625093));
#41532=CARTESIAN_POINT('Ctrl Pts',(0.0160164158031762,0.138087213996209,
0.52901781682461));
#41533=CARTESIAN_POINT('Ctrl Pts',(-0.0945587588515482,0.0937580907599652,
0.536126122774119));
#41534=CARTESIAN_POINT('Ctrl Pts',(-0.117480271566393,0.0271367046984328,
0.54059908765712));
#41535=CARTESIAN_POINT('Ctrl Pts',(-0.117697192808605,-9.79052972080122E-5,
0.542436711473616));
#41536=CARTESIAN_POINT('Origin',(0.,0.,-0.0924367114736152));
#41537=CARTESIAN_POINT('',(-0.117758961667293,-0.000104950384427651,0.432563288526384));
#41538=CARTESIAN_POINT('',(-0.117952286276812,3.39956489144189E-5,0.442436711473616));
#41539=CARTESIAN_POINT('',(-0.117775,-1.30487598617993E-14,-0.0924367114736152));
#41540=CARTESIAN_POINT('Ctrl Pts',(-0.117758961667293,-0.000104950384427652,
0.432563288526384));
#41541=CARTESIAN_POINT('Ctrl Pts',(-0.117844817924839,-0.00971740507401162,
0.43321274319838));
#41542=CARTESIAN_POINT('Ctrl Pts',(-0.11238834839588,-0.0582101957930696,
0.436495601825179));
#41543=CARTESIAN_POINT('Ctrl Pts',(-0.045454021205161,-0.13133563022352,
0.44241186440678));
#41544=CARTESIAN_POINT('Ctrl Pts',(0.085164376794762,-0.109827795821861,
0.450312076271186));
#41545=CARTESIAN_POINT('Ctrl Pts',(0.138516891217783,0.0113219546585138,
0.458212288135593));
#41546=CARTESIAN_POINT('Ctrl Pts',(0.0661991384108791,0.12219979494085,
0.4661125));
#41547=CARTESIAN_POINT('Ctrl Pts',(-0.0661781734963363,0.122211149911198,
0.474012711864406));
#41548=CARTESIAN_POINT('Ctrl Pts',(-0.116387669202521,0.0452586237679377,
0.479496308039868));
#41549=CARTESIAN_POINT('Ctrl Pts',(-0.117949767953432,0.00325157581050499,
0.482346500260528));
#41550=CARTESIAN_POINT('Ctrl Pts',(-0.117931139389423,5.50751932371233E-5,
0.482563288526385));
#41551=CARTESIAN_POINT('Ctrl Pts',(-0.117952286276812,3.39956489144155E-5,
0.442436711473616));
#41552=CARTESIAN_POINT('Ctrl Pts',(-0.117810336120504,-0.0369130001778165,
0.444943669258889));
#41553=CARTESIAN_POINT('Ctrl Pts',(-0.0792807483010678,-0.11295446192069,
0.450085968110668));
#41554=CARTESIAN_POINT('Ctrl Pts',(0.0499845850166584,-0.129715633233345,
0.457863608028953));
#41555=CARTESIAN_POINT('Ctrl Pts',(0.135973695209673,-0.0289094872912353,
0.465769631228471));
#41556=CARTESIAN_POINT('Ctrl Pts',(0.0984334954810092,0.0981603342078928,
0.473675654427988));
#41557=CARTESIAN_POINT('Ctrl Pts',(-0.0285315135918273,0.136053507770195,
0.481581677627505));
#41558=CARTESIAN_POINT('Ctrl Pts',(-0.108458155672614,0.0682577387762276,
0.487835363309382));
#41559=CARTESIAN_POINT('Ctrl Pts',(-0.117717393951882,0.0146612380616908,
0.491453707924752));
#41560=CARTESIAN_POINT('Ctrl Pts',(-0.117634119017629,7.28683544160419E-5,
0.492436711473616));
#41561=CARTESIAN_POINT('Origin',(0.,0.,-0.0924367114736152));
#41562=CARTESIAN_POINT('',(-0.117603494801586,4.59807059966066E-5,0.382563288526384));
#41563=CARTESIAN_POINT('',(-0.117726185906756,-0.000103034036682964,0.392436711473616));
#41564=CARTESIAN_POINT('',(-0.117775,-1.30487598617993E-14,-0.0924367114736152));
#41565=CARTESIAN_POINT('Ctrl Pts',(-0.117603494801586,4.59807059966007E-5,
0.382563288526384));
#41566=CARTESIAN_POINT('Ctrl Pts',(-0.117523654559104,-0.0224626175592834,
0.384078986136234));
#41567=CARTESIAN_POINT('Ctrl Pts',(-0.100492247037195,-0.0841899886309759,
0.388228087700885));
#41568=CARTESIAN_POINT('Ctrl Pts',(-0.000920295459793275,-0.138975785179272,
0.395010593220339));
#41569=CARTESIAN_POINT('Ctrl Pts',(0.115895314901344,-0.0767032710765764,
0.402910805084745));
#41570=CARTESIAN_POINT('Ctrl Pts',(0.127564216682018,0.0551587384938402,
0.410811016949152));
#41571=CARTESIAN_POINT('Ctrl Pts',(0.0234997298595607,0.136977656960748,
0.418711228813559));
#41572=CARTESIAN_POINT('Ctrl Pts',(-0.0915774899741938,0.0980128855194841,
0.42596198600597));
#41573=CARTESIAN_POINT('Ctrl Pts',(-0.117496688612794,0.0292591044291153,
0.430579339243578));
#41574=CARTESIAN_POINT('Ctrl Pts',(-0.117758961667293,-0.000104950384427652,
0.432563288526384));
#41575=CARTESIAN_POINT('Ctrl Pts',(-0.117726185906756,-0.000103034036682944,
0.392436711473616));
#41576=CARTESIAN_POINT('Ctrl Pts',(-0.117818125179144,-0.0108595471866994,
0.393162948460015));
#41577=CARTESIAN_POINT('Ctrl Pts',(-0.111550100869322,-0.0605437012261054,
0.39652452651292));
#41578=CARTESIAN_POINT('Ctrl Pts',(-0.0415471952570256,-0.13265909245389,
0.40252144563233));
#41579=CARTESIAN_POINT('Ctrl Pts',(0.0884857325734624,-0.107214175253801,
0.410427468831849));
#41580=CARTESIAN_POINT('Ctrl Pts',(0.138131189387156,0.0156326185555932,
0.418333492031365));
#41581=CARTESIAN_POINT('Ctrl Pts',(0.062287297122381,0.124277499418049,
0.426239515230884));
#41582=CARTESIAN_POINT('Ctrl Pts',(-0.0701433255283678,0.120018824057881,
0.4341455384304));
#41583=CARTESIAN_POINT('Ctrl Pts',(-0.117063601095489,0.0426502166584235,
0.439544603844645));
#41584=CARTESIAN_POINT('Ctrl Pts',(-0.117959555656036,0.00192608038356173,
0.442308328192384));
#41585=CARTESIAN_POINT('Ctrl Pts',(-0.117952286276812,3.39956489144155E-5,
0.442436711473616));
#41586=CARTESIAN_POINT('Origin',(0.,0.,-0.0924367114736152));
#41587=CARTESIAN_POINT('',(-0.117920926539219,6.26243704048756E-5,0.332563288526384));
#41588=CARTESIAN_POINT('',(-0.117615878293784,5.9477676878486E-5,0.342436711473616));
#41589=CARTESIAN_POINT('',(-0.117775,-1.30487598617993E-14,-0.0924367114736152));
#41590=CARTESIAN_POINT('Ctrl Pts',(-0.117920926539219,6.26243704048737E-5,
0.332563288526384));
#41591=CARTESIAN_POINT('Ctrl Pts',(-0.117693603628949,-0.0350666637837455,
0.334945229074087));
#41592=CARTESIAN_POINT('Ctrl Pts',(-0.0824632530796663,-0.109429893167014,
0.339960573576592));
#41593=CARTESIAN_POINT('Ctrl Pts',(0.0437107063235388,-0.131926077644361,
0.347609322033898));
#41594=CARTESIAN_POINT('Ctrl Pts',(0.134376016486386,-0.0354711432460098,
0.355509533898305));
#41595=CARTESIAN_POINT('Ctrl Pts',(0.103127892463174,0.0931651952503325,
0.363409745762711));
#41596=CARTESIAN_POINT('Ctrl Pts',(-0.0216836207666979,0.137276860396698,
0.371309957627119));
#41597=CARTESIAN_POINT('Ctrl Pts',(-0.106651080731,0.0722748925449633,0.377694471881676));
#41598=CARTESIAN_POINT('Ctrl Pts',(-0.117662370625513,0.0166442803494234,
0.381445582181431));
#41599=CARTESIAN_POINT('Ctrl Pts',(-0.117603494801586,4.59807059966007E-5,
0.382563288526384));
#41600=CARTESIAN_POINT('Ctrl Pts',(-0.117615878293784,5.94776768784704E-5,
0.342436711473616));
#41601=CARTESIAN_POINT('Ctrl Pts',(-0.11750760701874,-0.0234105356203755,
0.344017568727647));
#41602=CARTESIAN_POINT('Ctrl Pts',(-0.0993568477409689,-0.0861600913990265,
0.348233767048184));
#41603=CARTESIAN_POINT('Ctrl Pts',(0.00259563734382704,-0.138988729439456,
0.355085306435226));
#41604=CARTESIAN_POINT('Ctrl Pts',(0.117881001348277,-0.0736795342380946,
0.362991329634744));
#41605=CARTESIAN_POINT('Ctrl Pts',(0.12607389627645,0.0585660048329233,
0.370897352834261));
#41606=CARTESIAN_POINT('Ctrl Pts',(0.0197312453245754,0.137605531147394,
0.378803376033779));
#41607=CARTESIAN_POINT('Ctrl Pts',(-0.0931217327741457,0.0958562111818821,
0.385983162246897));
#41608=CARTESIAN_POINT('Ctrl Pts',(-0.117484499455465,0.0281732773148422,
0.39052760739351));
#41609=CARTESIAN_POINT('Ctrl Pts',(-0.117726185906756,-0.000103034036682944,
0.392436711473616));
#41610=CARTESIAN_POINT('Origin',(0.,0.,-0.0924367114736152));
#41611=CARTESIAN_POINT('',(-0.117774170260593,-0.000104886777209015,0.282563288526384));
#41612=CARTESIAN_POINT('',(-0.11793628481875,5.1384428605368E-5,0.292436711473616));
#41613=CARTESIAN_POINT('',(-0.117775,-1.30487598617993E-14,-0.0924367114736152));
#41614=CARTESIAN_POINT('Ctrl Pts',(-0.117774170260593,-0.00010488677720901,
0.282563288526384));
#41615=CARTESIAN_POINT('Ctrl Pts',(-0.117856360533384,-0.0092011162257308,
0.283178068057138));
#41616=CARTESIAN_POINT('Ctrl Pts',(-0.112752995425492,-0.057169777637724,
0.286426251542693));
#41617=CARTESIAN_POINT('Ctrl Pts',(-0.0471669369944997,-0.130730240818604,
0.292307838983051));
#41618=CARTESIAN_POINT('Ctrl Pts',(0.0837214480778729,-0.110931667893667,
0.300208050847457));
#41619=CARTESIAN_POINT('Ctrl Pts',(0.138653055169421,0.00951031556331505,
0.308108262711865));
#41620=CARTESIAN_POINT('Ctrl Pts',(0.0677908594821406,0.121324009085596,
0.316008474576271));
#41621=CARTESIAN_POINT('Ctrl Pts',(-0.0645749936433688,0.123065779182871,
0.323908686440678));
#41622=CARTESIAN_POINT('Ctrl Pts',(-0.116109941121323,0.0462937466385656,
0.329426957757382));
#41623=CARTESIAN_POINT('Ctrl Pts',(-0.117944925204334,0.00377125198361699,
0.332311825119284));
#41624=CARTESIAN_POINT('Ctrl Pts',(-0.117920926539219,6.26243704048737E-5,
0.332563288526384));
#41625=CARTESIAN_POINT('Ctrl Pts',(-0.11793628481875,5.13844286053676E-5,
0.292436711473616));
#41626=CARTESIAN_POINT('Ctrl Pts',(-0.117738942084994,-0.0358551097426003,
0.294872188995279));
#41627=CARTESIAN_POINT('Ctrl Pts',(-0.0811119992076199,-0.110963296543085,
0.299943007583447));
#41628=CARTESIAN_POINT('Ctrl Pts',(0.046471358419155,-0.131015331511595,
0.307649167238122));
#41629=CARTESIAN_POINT('Ctrl Pts',(0.135145386671506,-0.0325626888604762,
0.315555190437639));
#41630=CARTESIAN_POINT('Ctrl Pts',(0.101042606300054,0.0954724879559945,
0.323461213637157));
#41631=CARTESIAN_POINT('Ctrl Pts',(-0.0248553070174182,0.136772869961425,
0.331367236836674));
#41632=CARTESIAN_POINT('Ctrl Pts',(-0.107513748550757,0.0704052555566997,
0.33769240278216));
#41633=CARTESIAN_POINT('Ctrl Pts',(-0.117688098797311,0.0157147489149463,
0.341382227661141));
#41634=CARTESIAN_POINT('Ctrl Pts',(-0.117615878293784,5.94776768784704E-5,
0.342436711473616));
#41635=CARTESIAN_POINT('Origin',(0.,0.,-0.0924367114736152));
#41636=CARTESIAN_POINT('',(-0.117597921122191,3.83764452643825E-5,0.232563288526384));
#41637=CARTESIAN_POINT('',(-0.117756807889117,-0.000105309437279225,0.242436711473616));
#41638=CARTESIAN_POINT('',(-0.117775,-1.30487598617993E-14,-0.0924367114736152));
#41639=CARTESIAN_POINT('Ctrl Pts',(-0.117597921122191,3.83764452643858E-5,
0.232563288526384));
#41640=CARTESIAN_POINT('Ctrl Pts',(-0.117532990113526,-0.0219578937617309,
0.234044310994991));
#41641=CARTESIAN_POINT('Ctrl Pts',(-0.101078828998682,-0.0831558954107903,
0.238158737418399));
#41642=CARTESIAN_POINT('Ctrl Pts',(-0.00273688716624997,-0.138951881091211,
0.24490656779661));
#41643=CARTESIAN_POINT('Ctrl Pts',(0.114882759277182,-0.0782116834669906,
0.252806779661017));
#41644=CARTESIAN_POINT('Ctrl Pts',(0.128274344207101,0.0534865256689417,
0.260706991525423));
#41645=CARTESIAN_POINT('Ctrl Pts',(0.0252882731449639,0.136658768658679,
0.26860720338983));
#41646=CARTESIAN_POINT('Ctrl Pts',(-0.090841176153826,0.099022467675047,
0.275892635723484));
#41647=CARTESIAN_POINT('Ctrl Pts',(-0.117504299056729,0.0297625209893518,
0.280544664102335));
#41648=CARTESIAN_POINT('Ctrl Pts',(-0.117774170260593,-0.00010488677720901,
0.282563288526384));
#41649=CARTESIAN_POINT('Ctrl Pts',(-0.117756807889117,-0.000105309437279212,
0.242436711473616));
#41650=CARTESIAN_POINT('Ctrl Pts',(-0.117843399042527,-0.00979668321532341,
0.243091468196405));
#41651=CARTESIAN_POINT('Ctrl Pts',(-0.112329964982903,-0.058397845463228,
0.246381565985699));
#41652=CARTESIAN_POINT('Ctrl Pts',(-0.0451064993838265,-0.131491474848312,
0.252307004841499));
#41653=CARTESIAN_POINT('Ctrl Pts',(0.0855648107118161,-0.1095594241143,
0.260213028041017));
#41654=CARTESIAN_POINT('Ctrl Pts',(0.138502247321704,0.0119051136596435,
0.268119051240535));
#41655=CARTESIAN_POINT('Ctrl Pts',(0.0656132363391791,0.122554100141606,
0.276025074440052));
#41656=CARTESIAN_POINT('Ctrl Pts',(-0.066884052510702,0.121865203254083,
0.283931097639569));
#41657=CARTESIAN_POINT('Ctrl Pts',(-0.1165204945288,0.0447817101515102,
0.289401643317424));
#41658=CARTESIAN_POINT('Ctrl Pts',(-0.117952479432728,0.00299799310969985,
0.292236847928773));
#41659=CARTESIAN_POINT('Ctrl Pts',(-0.11793628481875,5.13844286053676E-5,
0.292436711473616));
#41660=CARTESIAN_POINT('Origin',(0.,0.,-0.0924367114736152));
#41661=CARTESIAN_POINT('',(-0.117909687164366,6.9664588846411E-5,0.182563288526384));
#41662=CARTESIAN_POINT('',(-0.117601649275994,4.45452448404882E-5,0.192436711473616));
#41663=CARTESIAN_POINT('',(-0.117775,-1.30487598617993E-14,-0.0924367114736152));
#41664=CARTESIAN_POINT('Ctrl Pts',(-0.117909687164366,6.96645888464118E-5,
0.182563288526384));
#41665=CARTESIAN_POINT('Ctrl Pts',(-0.11766595726848,-0.0345569219122136,
0.184910553932844));
#41666=CARTESIAN_POINT('Ctrl Pts',(-0.0833160382623138,-0.10845204978507,
0.189891223294105));
#41667=CARTESIAN_POINT('Ctrl Pts',(0.0419824540321544,-0.132486185591528,
0.197505296610169));
#41668=CARTESIAN_POINT('Ctrl Pts',(0.133900861976353,-0.0372246554226585,
0.205405508474576));
#41669=CARTESIAN_POINT('Ctrl Pts',(0.10433692245731,0.0918091630494651,
0.213305720338983));
#41670=CARTESIAN_POINT('Ctrl Pts',(-0.0198873058616059,0.137548576426424,
0.221205932203389));
#41671=CARTESIAN_POINT('Ctrl Pts',(-0.10616324692175,0.0733158722115256,
0.22762512159919));
#41672=CARTESIAN_POINT('Ctrl Pts',(-0.117648443848114,0.0171536431540524,
0.231410907040188));
#41673=CARTESIAN_POINT('Ctrl Pts',(-0.117597921122191,3.83764452643858E-5,
0.232563288526384));
#41674=CARTESIAN_POINT('Ctrl Pts',(-0.117601649275994,4.45452448404882E-5,
0.192436711473616));
#41675=CARTESIAN_POINT('Ctrl Pts',(-0.11752478280801,-0.0223710360060294,
0.193946088464036));
#41676=CARTESIAN_POINT('Ctrl Pts',(-0.100593880386987,-0.0840313287987434,
0.198090806520963));
#41677=CARTESIAN_POINT('Ctrl Pts',(-0.00115024004832317,-0.139008205490464,
0.204870865644395));
#41678=CARTESIAN_POINT('Ctrl Pts',(0.115852970087698,-0.0768289890996742,
0.212776888843912));
#41679=CARTESIAN_POINT('Ctrl Pts',(0.127606135899372,0.055147786219953,
0.22068291204343));
#41680=CARTESIAN_POINT('Ctrl Pts',(0.0234317475993789,0.137023930205902,
0.228588935242947));
#41681=CARTESIAN_POINT('Ctrl Pts',(-0.0916394876575414,0.0979452740831826,
0.235840201719676));
#41682=CARTESIAN_POINT('Ctrl Pts',(-0.11749487688974,0.0292102859676066,
0.240456127129899));
#41683=CARTESIAN_POINT('Ctrl Pts',(-0.117756807889117,-0.000105309437279212,
0.242436711473616));
#41684=CARTESIAN_POINT('Origin',(0.,0.,-0.0924367114736152));
#41685=CARTESIAN_POINT('',(-0.117789487689835,-0.000104112672946744,0.132563288526384));
#41686=CARTESIAN_POINT('',(-0.117915129103549,6.69430946510577E-5,0.142436711473616));
#41687=CARTESIAN_POINT('',(-0.117775,-1.30487598617993E-14,-0.0924367114736152));
#41688=CARTESIAN_POINT('Ctrl Pts',(-0.117789487689835,-0.000104112672946739,
0.132563288526384));
#41689=CARTESIAN_POINT('Ctrl Pts',(-0.117867447370286,-0.00868443076951223,
0.133143392915894));
#41690=CARTESIAN_POINT('Ctrl Pts',(-0.113109713752316,-0.056129702894726,
0.136356901260207));
#41691=CARTESIAN_POINT('Ctrl Pts',(-0.0488717923313075,-0.130102508888041,
0.142203813559322));
#41692=CARTESIAN_POINT('Ctrl Pts',(0.0822642127117346,-0.112016585630158,
0.150104025423729));
#41693=CARTESIAN_POINT('Ctrl Pts',(0.138765526166673,0.00769705224861128,
0.158004237288135));
#41694=CARTESIAN_POINT('Ctrl Pts',(0.0693709963376258,0.12042749084372,
0.165904449152542));
#41695=CARTESIAN_POINT('Ctrl Pts',(-0.0629607791409001,0.123899379163224,
0.173804661016949));
#41696=CARTESIAN_POINT('Ctrl Pts',(-0.115824984153554,0.0473294249038356,
0.179357607474896));
#41697=CARTESIAN_POINT('Ctrl Pts',(-0.117939398554652,0.00429074720192216,
0.182277149978042));
#41698=CARTESIAN_POINT('Ctrl Pts',(-0.117909687164366,6.96645888464118E-5,
0.182563288526384));
#41699=CARTESIAN_POINT('Ctrl Pts',(-0.117915129103549,6.69430946510529E-5,
0.142436711473616));
#41700=CARTESIAN_POINT('Ctrl Pts',(-0.117677363460081,-0.0348022339441635,
0.144800708731668));
#41701=CARTESIAN_POINT('Ctrl Pts',(-0.0828943760199795,-0.108955331093341,
0.149800047056226));
#41702=CARTESIAN_POINT('Ctrl Pts',(0.0429243879661372,-0.132219897211806,
0.15743472644729));
#41703=CARTESIAN_POINT('Ctrl Pts',(0.134218946443888,-0.0361922458912883,
0.165340749646808));
#41704=CARTESIAN_POINT('Ctrl Pts',(0.103578348063976,0.0927153171784346,
0.173246772846325));
#41705=CARTESIAN_POINT('Ctrl Pts',(-0.0211610525014389,0.137392918706172,
0.181152796045843));
#41706=CARTESIAN_POINT('Ctrl Pts',(-0.106531690673769,0.0725519877028229,
0.187549442254939));
#41707=CARTESIAN_POINT('Ctrl Pts',(-0.117658990074321,0.0167661061227608,
0.19131074739753));
#41708=CARTESIAN_POINT('Ctrl Pts',(-0.117601649275994,4.45452448404882E-5,
0.192436711473616));
#41709=CARTESIAN_POINT('Origin',(0.,0.,-0.0924367114736152));
#41710=CARTESIAN_POINT('',(-0.117593357284741,3.06645980543279E-5,0.0825632885263843));
#41711=CARTESIAN_POINT('',(-0.117788324723582,-0.000104604007662518,0.0924367114736157));
#41712=CARTESIAN_POINT('',(-0.117775,-1.30487598617993E-14,-0.0924367114736152));
#41713=CARTESIAN_POINT('Ctrl Pts',(-0.117593357284741,3.06645980543228E-5,
0.0825632885263843));
#41714=CARTESIAN_POINT('Ctrl Pts',(-0.11754301899516,-0.021452746571923,
0.0840096358537477));
#41715=CARTESIAN_POINT('Ctrl Pts',(-0.101655671713158,-0.0821210291969121,
0.0880893871359134));
#41716=CARTESIAN_POINT('Ctrl Pts',(-0.0045529857407016,-0.138904079109577,
0.0948025423728811));
#41717=CARTESIAN_POINT('Ctrl Pts',(0.113850559027731,-0.0797068119457511,
0.102702754237288));
#41718=CARTESIAN_POINT('Ctrl Pts',(0.12896255920279,0.0518052156568057,
0.110602966101695));
#41719=CARTESIAN_POINT('Ctrl Pts',(0.0270724914422277,0.136316505597261,
0.118503177966102));
#41720=CARTESIAN_POINT('Ctrl Pts',(-0.0900940209439092,0.100029588267392,
0.125823285440998));
#41721=CARTESIAN_POINT('Ctrl Pts',(-0.117513546702531,0.0302662202125134,
0.130509988961092));
#41722=CARTESIAN_POINT('Ctrl Pts',(-0.117789487689835,-0.000104112672946739,
0.132563288526384));
#41723=CARTESIAN_POINT('Ctrl Pts',(-0.117788324723582,-0.00010460400766255,
0.0924367114736157));
#41724=CARTESIAN_POINT('Ctrl Pts',(-0.117866887107117,-0.00873205619380746,
0.093019987932794));
#41725=CARTESIAN_POINT('Ctrl Pts',(-0.113075788730874,-0.0562533105277103,
0.0962386054584782));
#41726=CARTESIAN_POINT('Ctrl Pts',(-0.0486330432543111,-0.130228357167641,
0.102092564050668));
#41727=CARTESIAN_POINT('Ctrl Pts',(0.0825817545836372,-0.111825131042891,
0.109998587250186));
#41728=CARTESIAN_POINT('Ctrl Pts',(0.138772738128538,0.00816897019039422,
0.117904610449703));
#41729=CARTESIAN_POINT('Ctrl Pts',(0.0688915313895657,0.120741708772585,
0.12581063364922));
#41730=CARTESIAN_POINT('Ctrl Pts',(-0.0635762130827019,0.123623095373164,
0.133716656848738));
#41731=CARTESIAN_POINT('Ctrl Pts',(-0.115947056638979,0.0469156369390546,
0.139258682790203));
#41732=CARTESIAN_POINT('Ctrl Pts',(-0.117942420266852,0.00406928923237253,
0.142165367665162));
#41733=CARTESIAN_POINT('Ctrl Pts',(-0.117915129103549,6.69430946510529E-5,
0.142436711473616));
#41734=CARTESIAN_POINT('Origin',(0.,0.,-0.0924367114736152));
#41735=CARTESIAN_POINT('',(-0.117896184020664,8.43438525025023E-5,0.0325632885263842));
#41736=CARTESIAN_POINT('',(-0.117591431864639,2.92794590778037E-5,0.0424367114736158));
#41737=CARTESIAN_POINT('',(-0.117775,-1.30487598617993E-14,-0.0924367114736152));
#41738=CARTESIAN_POINT('Ctrl Pts',(-0.117896184020664,8.43438525024954E-5,
0.0325632885263842));
#41739=CARTESIAN_POINT('Ctrl Pts',(-0.117638881596538,-0.0340384192378303,
0.0348758787916007));
#41740=CARTESIAN_POINT('Ctrl Pts',(-0.0841595758608773,-0.107483448399194,
0.0398218730116195));
#41741=CARTESIAN_POINT('Ctrl Pts',(0.040248222246223,-0.133016439153077,
0.0474012711864405));
#41742=CARTESIAN_POINT('Ctrl Pts',(0.133402197487182,-0.0389756054074351,
0.0553014830508473));
#41743=CARTESIAN_POINT('Ctrl Pts',(0.105528454455023,0.0904394425945055,
0.0632016949152541));
#41744=CARTESIAN_POINT('Ctrl Pts',(-0.0180877669633101,0.137795734956694,
0.0711019067796609));
#41745=CARTESIAN_POINT('Ctrl Pts',(-0.105666299933038,0.0743567679416689,
0.0775557713167041));
#41746=CARTESIAN_POINT('Ctrl Pts',(-0.117634671289428,0.017662685017247,
0.0813762318989454));
#41747=CARTESIAN_POINT('Ctrl Pts',(-0.117593357284741,3.06645980543228E-5,
0.0825632885263843));
#41748=CARTESIAN_POINT('Ctrl Pts',(-0.117591431864639,2.92794590778002E-5,
0.0424367114736158));
#41749=CARTESIAN_POINT('Ctrl Pts',(-0.11754501123181,-0.0213296840770181,
0.0438746082004259));
#41750=CARTESIAN_POINT('Ctrl Pts',(-0.101789620521557,-0.0818995216066154,
0.0479478459937417));
#41751=CARTESIAN_POINT('Ctrl Pts',(-0.00489492837772915,-0.138925734589418,
0.0546564248535634));
#41752=CARTESIAN_POINT('Ctrl Pts',(0.113740629398734,-0.0799231888543136,
0.062562448053081));
#41753=CARTESIAN_POINT('Ctrl Pts',(0.129045816271948,0.0516898037714297,
0.0704684712525983));
#41754=CARTESIAN_POINT('Ctrl Pts',(0.0271151839788463,0.136342686033388,
0.0783744944521158));
#41755=CARTESIAN_POINT('Ctrl Pts',(-0.0901114389347958,0.100024405106452,
0.0856972411924549));
#41756=CARTESIAN_POINT('Ctrl Pts',(-0.117511929055312,0.0302482226905713,
0.0903846468662882));
#41757=CARTESIAN_POINT('Ctrl Pts',(-0.117788324723582,-0.00010460400766255,
0.0924367114736157));
#41758=CARTESIAN_POINT('Origin',(0.,0.,0.95));
#41759=CARTESIAN_POINT('',(-0.143203996033626,-2.30855198111598E-5,0.907000235762439));
#41760=CARTESIAN_POINT('Ctrl Pts',(-0.0334019664626807,0.112939183906322,
0.932225));
#41761=CARTESIAN_POINT('Ctrl Pts',(-0.0250603177854857,0.115799805022824,
0.931847596094215));
#41762=CARTESIAN_POINT('Ctrl Pts',(-0.0164278988467134,0.117636476238285,
0.931473565046676));
#41763=CARTESIAN_POINT('Ctrl Pts',(-0.00767106646971057,0.118512486061759,
0.931100514589335));
#41764=CARTESIAN_POINT('Ctrl Pts',(-0.00420439075546036,0.118859282922739,
0.930952830483373));
#41765=CARTESIAN_POINT('Ctrl Pts',(-0.000716143526927236,0.119054988716296,
0.930805221836912));
#41766=CARTESIAN_POINT('Ctrl Pts',(0.00277797710115842,0.119101360153194,
0.930657787404542));
#41767=CARTESIAN_POINT('Ctrl Pts',(0.00969984845123832,0.119193222213692,
0.930365719018224));
#41768=CARTESIAN_POINT('Ctrl Pts',(0.0166142532722655,0.118700388967513,
0.930075608100973));
#41769=CARTESIAN_POINT('Ctrl Pts',(0.02344427759502,0.117646722051856,0.929786344238933));
#41770=CARTESIAN_POINT('Ctrl Pts',(0.0272709497102665,0.117056381869396,
0.929624277765593));
#41771=CARTESIAN_POINT('Ctrl Pts',(0.0310712076772195,0.116289673696229,
0.929462477186978));
#41772=CARTESIAN_POINT('Ctrl Pts',(0.0348314922052066,0.115348424870015,
0.929300747212246));
#41773=CARTESIAN_POINT('Ctrl Pts',(0.0378910930422447,0.114582566415658,
0.929169153668624));
#41774=CARTESIAN_POINT('Ctrl Pts',(0.04092399616764,0.113700812218856,0.929037612549819));
#41775=CARTESIAN_POINT('Ctrl Pts',(0.0439095212807944,0.11270886835725,
0.928906608402292));
#41776=CARTESIAN_POINT('Ctrl Pts',(0.0525514734098646,0.10983757066528,
0.928527401553001));
#41777=CARTESIAN_POINT('Ctrl Pts',(0.0608263773706973,0.106040058117234,
0.928151455604188));
#41778=CARTESIAN_POINT('Ctrl Pts',(0.0685605494008651,0.101344813008116,
0.927776330408337));
#41779=CARTESIAN_POINT('Ctrl Pts',(0.072435687838791,0.0989923020054058,
0.927588377249316));
#41780=CARTESIAN_POINT('Ctrl Pts',(0.0761749070710193,0.0964136602636579,
0.92740063013395));
#41781=CARTESIAN_POINT('Ctrl Pts',(0.0797540201577765,0.0936080366646606,
0.927212782134414));
#41782=CARTESIAN_POINT('Ctrl Pts',(0.0820668650566089,0.091795025432075,
0.927091393601291));
#41783=CARTESIAN_POINT('Ctrl Pts',(0.0843049421929101,0.089893314502136,
0.926970374334797));
#41784=CARTESIAN_POINT('Ctrl Pts',(0.0864667806566824,0.087910346105634,
0.926849671848167));
#41785=CARTESIAN_POINT('Ctrl Pts',(0.0931618700565369,0.0817692070177022,
0.9264758631884));
#41786=CARTESIAN_POINT('Ctrl Pts',(0.0991298287989589,0.0748505421836024,
0.926105008552812));
#41787=CARTESIAN_POINT('Ctrl Pts',(0.104322127839002,0.0673319773813505,
0.925734762248716));
#41788=CARTESIAN_POINT('Ctrl Pts',(0.106370940812892,0.0643652505050492,
0.925588667922192));
#41789=CARTESIAN_POINT('Ctrl Pts',(0.108298617033319,0.0613046783141235,
0.925442668312145));
#41790=CARTESIAN_POINT('Ctrl Pts',(0.110100560923862,0.0581597986785966,
0.925296619306966));
#41791=CARTESIAN_POINT('Ctrl Pts',(0.11158855048605,0.0555628542917283,
0.925176016553231));
#41792=CARTESIAN_POINT('Ctrl Pts',(0.112988026000293,0.0529128751968171,
0.925055591079489));
#41793=CARTESIAN_POINT('Ctrl Pts',(0.114293875604956,0.0502227205878152,
0.92493557115538));
#41794=CARTESIAN_POINT('Ctrl Pts',(0.118434599880109,0.0416924974643938,
0.924554999448279));
#41795=CARTESIAN_POINT('Ctrl Pts',(0.121649070098747,0.0327401005258095,
0.924177564198185));
#41796=CARTESIAN_POINT('Ctrl Pts',(0.123868271499824,0.0235442585075687,
0.923800796649243));
#41797=CARTESIAN_POINT('Ctrl Pts',(0.124741985203477,0.0199237970280188,
0.923652460869335));
#41798=CARTESIAN_POINT('Ctrl Pts',(0.125460929083487,0.0162653271532848,
0.923504228586243));
#41799=CARTESIAN_POINT('Ctrl Pts',(0.126018750659753,0.0125790928555092,
0.923355949140843));
#41800=CARTESIAN_POINT('Ctrl Pts',(0.126424880564737,0.00989527772751904,
0.923247992188954));
#41801=CARTESIAN_POINT('Ctrl Pts',(0.126745061646254,0.00719882962072188,
0.923140094926841));
#41802=CARTESIAN_POINT('Ctrl Pts',(0.126976603796028,0.00450277675306522,
0.923032557085152));
#41803=CARTESIAN_POINT('Ctrl Pts',(0.12757677314312,-0.00248553311139155,
0.922753813382129));
#41804=CARTESIAN_POINT('Ctrl Pts',(0.127585234929588,-0.00948784607823892,
0.922476804764986));
#41805=CARTESIAN_POINT('Ctrl Pts',(0.126969800827767,-0.0164342950540157,
0.922200564268829));
#41806=CARTESIAN_POINT('Ctrl Pts',(0.126365890166078,-0.0232506781321251,
0.921929496123068));
#41807=CARTESIAN_POINT('Ctrl Pts',(0.125161228392162,-0.0300136540166471,
0.921659167602865));
#41808=CARTESIAN_POINT('Ctrl Pts',(0.123399407242885,-0.0366692095497128,
0.921388665049245));
#41809=CARTESIAN_POINT('Ctrl Pts',(0.122693706044386,-0.0393351064361743,
0.921280314677605));
#41810=CARTESIAN_POINT('Ctrl Pts',(0.121898903213358,-0.0419812756064514,
0.921172034233936));
#41811=CARTESIAN_POINT('Ctrl Pts',(0.121020997998916,-0.0445959600773696,
0.921064109665588));
#41812=CARTESIAN_POINT('Ctrl Pts',(0.118352374694664,-0.0525439797468811,
0.920736044615448));
#41813=CARTESIAN_POINT('Ctrl Pts',(0.11491247387436,-0.0602240203343106,
0.920410355973602));
#41814=CARTESIAN_POINT('Ctrl Pts',(0.110787244183297,-0.067540847099726,
0.920085467703143));
#41815=CARTESIAN_POINT('Ctrl Pts',(0.108602638591366,-0.0714156327150692,
0.919913416014983));
#41816=CARTESIAN_POINT('Ctrl Pts',(0.106225299026755,-0.0751884756223749,
0.919741588788067));
#41817=CARTESIAN_POINT('Ctrl Pts',(0.103664831029184,-0.0788439383503402,
0.919569751954905));
#41818=CARTESIAN_POINT('Ctrl Pts',(0.101376332819864,-0.0821111222851215,
0.919416167420609));
#41819=CARTESIAN_POINT('Ctrl Pts',(0.0989387376213173,-0.0852871325232165,
0.919262431231772));
#41820=CARTESIAN_POINT('Ctrl Pts',(0.0963759957044455,-0.088340202919688,
0.919109404658397));
#41821=CARTESIAN_POINT('Ctrl Pts',(0.0909694481938422,-0.0947811832006395,
0.918786568623332));
#41822=CARTESIAN_POINT('Ctrl Pts',(0.0849957607581912,-0.100695240401247,
0.918466028662098));
#41823=CARTESIAN_POINT('Ctrl Pts',(0.0785257616471073,-0.105984325129946,
0.918146284163942));
#41824=CARTESIAN_POINT('Ctrl Pts',(0.0742361136603187,-0.109491019840235,
0.917934291655249));
#41825=CARTESIAN_POINT('Ctrl Pts',(0.0697277556719998,-0.112722769515888,
0.917722648813756));
#41826=CARTESIAN_POINT('Ctrl Pts',(0.0650165017469215,-0.115645838880061,
0.917510918298299));
#41827=CARTESIAN_POINT('Ctrl Pts',(0.0626218558869296,-0.117131582604068,
0.917403299475299));
#41828=CARTESIAN_POINT('Ctrl Pts',(0.0601741524651638,-0.118537526250906,
0.917295638036625));
#41829=CARTESIAN_POINT('Ctrl Pts',(0.0576864529767728,-0.119853555264988,
0.917188346403244));
#41830=CARTESIAN_POINT('Ctrl Pts',(0.0492417976832846,-0.12432090006769,
0.916824138079852));
#41831=CARTESIAN_POINT('Ctrl Pts',(0.0403105010214407,-0.127774185485052,
0.916462909477301));
#41832=CARTESIAN_POINT('Ctrl Pts',(0.0310751541446225,-0.130251129571305,
0.916102510949096));
#41833=CARTESIAN_POINT('Ctrl Pts',(0.0264632552530831,-0.131488052865922,
0.91592253702988));
#41834=CARTESIAN_POINT('Ctrl Pts',(0.0217750625284288,-0.132480793424065,
0.915742770110557));
#41835=CARTESIAN_POINT('Ctrl Pts',(0.0170316000051624,-0.133229777506063,
0.915562942492132));
#41836=CARTESIAN_POINT('Ctrl Pts',(0.0138158762359995,-0.133737534424853,
0.91544103240133));
#41837=CARTESIAN_POINT('Ctrl Pts',(0.0105740209053218,-0.134132938348625,
0.915319069467609));
#41838=CARTESIAN_POINT('Ctrl Pts',(0.0073287749381158,-0.134414943979412,
0.91519757274014));
#41839=CARTESIAN_POINT('Ctrl Pts',(-0.00265707911089655,-0.135282695483764,
0.91482371861623));
#41840=CARTESIAN_POINT('Ctrl Pts',(-0.0127097596984602,-0.135087239355917,
0.914452927180717));
#41841=CARTESIAN_POINT('Ctrl Pts',(-0.0226366995613315,-0.13384562451132,
0.914082871556714));
#41842=CARTESIAN_POINT('Ctrl Pts',(-0.0278509024051071,-0.133193456598246,
0.913888496944428));
#41843=CARTESIAN_POINT('Ctrl Pts',(-0.0330306231776361,-0.132251796770583,
0.913694325339435));
#41844=CARTESIAN_POINT('Ctrl Pts',(-0.0381476304341873,-0.131017345860063,
0.913500019539069));
#41845=CARTESIAN_POINT('Ctrl Pts',(-0.0414017963667409,-0.130232295556825,
0.913376450569093));
#41846=CARTESIAN_POINT('Ctrl Pts',(-0.0446227244193663,-0.129330489295675,
0.913253123242388));
#41847=CARTESIAN_POINT('Ctrl Pts',(-0.0477977620148837,-0.128314174106561,
0.913130170982833));
#41848=CARTESIAN_POINT('Ctrl Pts',(-0.0560508514351662,-0.125672397471604,
0.912810572879819));
#41849=CARTESIAN_POINT('Ctrl Pts',(-0.0640066574241223,-0.122256042832264,
0.912493045231938));
#41850=CARTESIAN_POINT('Ctrl Pts',(-0.0715409466919047,-0.118061015146759,
0.912176128537659));
#41851=CARTESIAN_POINT('Ctrl Pts',(-0.0762921378140006,-0.11541559265395,
0.911976277996913));
#41852=CARTESIAN_POINT('Ctrl Pts',(-0.080875618778813,-0.112459902541578,
0.911776670412738));
#41853=CARTESIAN_POINT('Ctrl Pts',(-0.0852772318261866,-0.109220115387155,
0.911576939781678));
#41854=CARTESIAN_POINT('Ctrl Pts',(-0.0875530243079477,-0.107545028738423,
0.911473671851569));
#41855=CARTESIAN_POINT('Ctrl Pts',(-0.0897785308463731,-0.105794887026521,
0.911370439409319));
#41856=CARTESIAN_POINT('Ctrl Pts',(-0.0919449058640415,-0.10397965349885,
0.911267529872683));
#41857=CARTESIAN_POINT('Ctrl Pts',(-0.0992562147283688,-0.0978534136403538,
0.910920220011141));
#41858=CARTESIAN_POINT('Ctrl Pts',(-0.105919754790705,-0.0909713378622389,
0.910575510440108));
#41859=CARTESIAN_POINT('Ctrl Pts',(-0.111868517901189,-0.0834835697610656,
0.910231536759666));
#41860=CARTESIAN_POINT('Ctrl Pts',(-0.115372944257836,-0.0790725129751651,
0.910028901285812));
#41861=CARTESIAN_POINT('Ctrl Pts',(-0.118628912335923,-0.0744505089078481,
0.909826521196012));
#41862=CARTESIAN_POINT('Ctrl Pts',(-0.121618006629831,-0.0696436476859399,
0.90962401532803));
#41863=CARTESIAN_POINT('Ctrl Pts',(-0.123117391998195,-0.0672324365713985,
0.90952243461307));
#41864=CARTESIAN_POINT('Ctrl Pts',(-0.124548834320201,-0.0647754742963825,
0.909420860177745));
#41865=CARTESIAN_POINT('Ctrl Pts',(-0.125905418138961,-0.0622851116177192,
0.9093196043405));
#41866=CARTESIAN_POINT('Ctrl Pts',(-0.130761030150815,-0.0533713719953201,
0.908957179953008));
#41867=CARTESIAN_POINT('Ctrl Pts',(-0.134679363933253,-0.0440025983801541,
0.908597596571227));
#41868=CARTESIAN_POINT('Ctrl Pts',(-0.13756687326497,-0.0343371686472044,
0.908238737834252));
#41869=CARTESIAN_POINT('Ctrl Pts',(-0.139097796244526,-0.0292126731787653,
0.908048475215596));
#41870=CARTESIAN_POINT('Ctrl Pts',(-0.14033830847868,-0.0240043037722782,
0.907858416294146));
#41871=CARTESIAN_POINT('Ctrl Pts',(-0.14126916593033,-0.0187337321988357,
0.90766824565692));
#41872=CARTESIAN_POINT('Ctrl Pts',(-0.141766581419635,-0.0159173354095375,
0.907566625564177));
#41873=CARTESIAN_POINT('Ctrl Pts',(-0.142175147764435,-0.0130838950804596,
0.90746500095103));
#41874=CARTESIAN_POINT('Ctrl Pts',(-0.142491067194012,-0.010247236235083,
0.907363696319434));
#41875=CARTESIAN_POINT('Ctrl Pts',(-0.142699030773042,-0.00837991922086784,
0.907297009462638));
#41876=CARTESIAN_POINT('Ctrl Pts',(-0.142867069971313,-0.00651002641398622,
0.907230418639425));
#41877=CARTESIAN_POINT('Ctrl Pts',(-0.142994592382579,-0.00463854690639179,
0.907163910672075));
#41878=CARTESIAN_POINT('Ctrl Pts',(-0.143099304951117,-0.00310181760319464,
0.907109298937397));
#41879=CARTESIAN_POINT('Ctrl Pts',(-0.143176698406437,-0.00156401794929073,
0.907054743068754));
#41880=CARTESIAN_POINT('Ctrl Pts',(-0.143227225569541,-2.57112916194508E-5,
0.907000235770274));
#41881=CARTESIAN_POINT('',(-0.00156150813732516,0.146115848505824,0.90365));
#41882=CARTESIAN_POINT('Ctrl Pts',(-0.00156268643911937,0.146080787864432,
0.90365));
#41883=CARTESIAN_POINT('Ctrl Pts',(-0.0117053345256504,0.14465327094795,
0.904950888122905));
#41884=CARTESIAN_POINT('Ctrl Pts',(-0.0216455209286645,0.142222180286059,
0.906261527257655));
#41885=CARTESIAN_POINT('Ctrl Pts',(-0.0312038210265984,0.138800205489803,
0.907591018110418));
#41886=CARTESIAN_POINT('Ctrl Pts',(-0.0379790896742497,0.136374586047791,
0.908533409288742));
#41887=CARTESIAN_POINT('Ctrl Pts',(-0.0445622616029078,0.133450051590279,
0.909485272488055));
#41888=CARTESIAN_POINT('Ctrl Pts',(-0.0508780053273359,0.130018961446113,
0.910449848959387));
#41889=CARTESIAN_POINT('Ctrl Pts',(-0.0536010334441123,0.128539649532677,
0.910865725373444));
#41890=CARTESIAN_POINT('Ctrl Pts',(-0.0562660125378511,0.126970478129068,
0.911282720586817));
#41891=CARTESIAN_POINT('Ctrl Pts',(-0.058866712211968,0.125312368815247,
0.911700977969885));
#41892=CARTESIAN_POINT('Ctrl Pts',(-0.0626444387166601,0.12290383100335,
0.912308530628704));
#41893=CARTESIAN_POINT('Ctrl Pts',(-0.0662873724862372,0.120307303169936,
0.912918858991888));
#41894=CARTESIAN_POINT('Ctrl Pts',(-0.069778152687478,0.117522359853825,
0.913532898033536));
#41895=CARTESIAN_POINT('Ctrl Pts',(-0.0759775260377567,0.112576501798998,
0.914623386993416));
#41896=CARTESIAN_POINT('Ctrl Pts',(-0.081698277829649,0.107036582207071,
0.915725579133695));
#41897=CARTESIAN_POINT('Ctrl Pts',(-0.0868900966390514,0.100989570353443,
0.916844711368391));
#41898=CARTESIAN_POINT('Ctrl Pts',(-0.0896166640492451,0.0978138845187795,
0.917432441717011));
#41899=CARTESIAN_POINT('Ctrl Pts',(-0.0921993947360654,0.0944939977198656,
0.918025537507845));
#41900=CARTESIAN_POINT('Ctrl Pts',(-0.0946128443867119,0.0910668838926417,
0.918620601845101));
#41901=CARTESIAN_POINT('Ctrl Pts',(-0.0989927195077328,0.0848474334123951,
0.919700511461385));
#41902=CARTESIAN_POINT('Ctrl Pts',(-0.102828650181205,0.0782631455551165,
0.92078926141647));
#41903=CARTESIAN_POINT('Ctrl Pts',(-0.106079098770626,0.0713949254017264,
0.921892245864136));
#41904=CARTESIAN_POINT('Ctrl Pts',(-0.108178735463834,0.0669583786746003,
0.922604721866953));
#41905=CARTESIAN_POINT('Ctrl Pts',(-0.110033655020259,0.062403198537532,
0.923323137285097));
#41906=CARTESIAN_POINT('Ctrl Pts',(-0.111627678155428,0.0577512547785083,
0.92404894598959));
#41907=CARTESIAN_POINT('Ctrl Pts',(-0.112967174079103,0.0538421147134128,
0.924658860475512));
#41908=CARTESIAN_POINT('Ctrl Pts',(-0.114123078730198,0.049859612891567,
0.925274762706783));
#41909=CARTESIAN_POINT('Ctrl Pts',(-0.11507803961208,0.0458466780964684,
0.925893033154576));
#41910=CARTESIAN_POINT('Ctrl Pts',(-0.117097308962912,0.0373613082845972,
0.92720036897266));
#41911=CARTESIAN_POINT('Ctrl Pts',(-0.118230954345967,0.0287177049851521,
0.928521669794669));
#41912=CARTESIAN_POINT('Ctrl Pts',(-0.118391771793402,0.020045083810393,
0.929866742826164));
#41913=CARTESIAN_POINT('Ctrl Pts',(-0.11848473133085,0.0150319284238029,
0.930644254028062));
#41914=CARTESIAN_POINT('Ctrl Pts',(-0.118251755364909,0.0100092161799773,
0.931429708350036));
#41915=CARTESIAN_POINT('Ctrl Pts',(-0.11766859746431,0.00500517689817996,
0.932225));
#41916=CARTESIAN_POINT('',(-0.115101970897782,0.0902398078595341,0.90365));
#41917=CARTESIAN_POINT('Origin',(0.,0.,0.90365));
#41918=CARTESIAN_POINT('Ctrl Pts',(-0.143227225569541,-2.57112916194508E-5,
0.907000235770274));
#41919=CARTESIAN_POINT('Ctrl Pts',(-0.143488833522934,0.00793898000868948,
0.90671802038504));
#41920=CARTESIAN_POINT('Ctrl Pts',(-0.143031870701996,0.0159171358242676,
0.906437106818573));
#41921=CARTESIAN_POINT('Ctrl Pts',(-0.141906651187533,0.0238323323994448,
0.906156482679268));
#41922=CARTESIAN_POINT('Ctrl Pts',(-0.141282697379586,0.0282214466835871,
0.906000871709079));
#41923=CARTESIAN_POINT('Ctrl Pts',(-0.140452894046849,0.0325912439394045,
0.905845349734719));
#41924=CARTESIAN_POINT('Ctrl Pts',(-0.139423292881505,0.0369284672537908,
0.905689744135006));
#41925=CARTESIAN_POINT('Ctrl Pts',(-0.13875911501036,0.0397263348598034,
0.905589365658919));
#41926=CARTESIAN_POINT('Ctrl Pts',(-0.138011948498085,0.0425090563696419,
0.905489007617642));
#41927=CARTESIAN_POINT('Ctrl Pts',(-0.13718658538945,0.0452640319758816,
0.905388954073411));
#41928=CARTESIAN_POINT('Ctrl Pts',(-0.134156179660795,0.0553792088866476,
0.905021597172627));
#41929=CARTESIAN_POINT('Ctrl Pts',(-0.130067939373984,0.0651554859252432,
0.904657113682601));
#41930=CARTESIAN_POINT('Ctrl Pts',(-0.125020727014944,0.07442120635967,
0.904293300817012));
#41931=CARTESIAN_POINT('Ctrl Pts',(-0.122044721725445,0.0798845851641063,
0.904078784578074));
#41932=CARTESIAN_POINT('Ctrl Pts',(-0.118734281499311,0.0851703778496932,
0.903864501493536));
#41933=CARTESIAN_POINT('Ctrl Pts',(-0.115101970897782,0.0902398078595341,
0.90365));
#41934=CARTESIAN_POINT('',(-0.05,-6.12323399573676E-18,1.));
#41935=CARTESIAN_POINT('',(-0.1,-1.22464679914735E-17,0.95));
#41936=CARTESIAN_POINT('Origin',(0.,0.,1.));
#41937=CARTESIAN_POINT('Ctrl Pts',(0.0850780204044548,-0.119080027477571,
-0.0164977839420937));
#41938=CARTESIAN_POINT('Ctrl Pts',(0.124484376148786,-0.090925728145445,
-0.0138643799872915));
#41939=CARTESIAN_POINT('Ctrl Pts',(0.17250686669983,0.00706609547096537,
-0.00859757207768696));
#41940=CARTESIAN_POINT('Ctrl Pts',(0.0881701387729916,0.148625694711589,
-0.000697360213280174));
#41941=CARTESIAN_POINT('Ctrl Pts',(-0.0762274913006873,0.154908116339636,
0.00720285165112661));
#41942=CARTESIAN_POINT('Ctrl Pts',(-0.171431501518862,0.0208683089584473,
0.0151030635155334));
#41943=CARTESIAN_POINT('Ctrl Pts',(-0.111122107950137,-0.132218525770778,
0.0230032753799401));
#41944=CARTESIAN_POINT('Ctrl Pts',(0.050013392704176,-0.165289372702636,
0.030903487244347));
#41945=CARTESIAN_POINT('Ctrl Pts',(0.165768725130536,-0.0484320089270095,
0.0388036991087536));
#41946=CARTESIAN_POINT('Ctrl Pts',(0.131132152914396,0.112382189969905,
0.0467039109731606));
#41947=CARTESIAN_POINT('Ctrl Pts',(-0.0224762869461261,0.171228238683186,
0.0546041228375672));
#41948=CARTESIAN_POINT('Ctrl Pts',(-0.155692220471689,0.0747310615070771,
0.062504334701974));
#41949=CARTESIAN_POINT('Ctrl Pts',(-0.147655869299913,-0.0895687367181161,
0.0704045465663809));
#41950=CARTESIAN_POINT('Ctrl Pts',(-0.00565764774487061,-0.172605493336333,
0.0783047584307876));
#41951=CARTESIAN_POINT('Ctrl Pts',(0.141473396847448,-0.0990455693335685,
0.0862049702951944));
#41952=CARTESIAN_POINT('Ctrl Pts',(0.160251925615185,0.0643743860018943,
0.0941051821596012));
#41953=CARTESIAN_POINT('Ctrl Pts',(0.0336409180434769,0.169390113302136,
0.102005394024008));
#41954=CARTESIAN_POINT('Ctrl Pts',(-0.123490994764231,0.120725758497873,
0.109905605888415));
#41955=CARTESIAN_POINT('Ctrl Pts',(-0.168584982150601,-0.0374678050106281,
0.117805817752822));
#41956=CARTESIAN_POINT('Ctrl Pts',(-0.0607292448116094,-0.16166845405022,
0.125706029617228));
#41957=CARTESIAN_POINT('Ctrl Pts',(0.102223455999678,-0.139194458136055,
0.133606241481635));
#41958=CARTESIAN_POINT('Ctrl Pts',(0.172433324173149,0.00956453913465353,
0.141506453346042));
#41959=CARTESIAN_POINT('Ctrl Pts',(0.086202040450112,0.149646047845283,
0.149406665210448));
#41960=CARTESIAN_POINT('Ctrl Pts',(-0.0782365529804317,0.153960298370095,
0.157306877074856));
#41961=CARTESIAN_POINT('Ctrl Pts',(-0.171694572067167,0.0185931582621336,
0.165207088939262));
#41962=CARTESIAN_POINT('Ctrl Pts',(-0.109381677027807,-0.133642733856025,
0.173107300803669));
#41963=CARTESIAN_POINT('Ctrl Pts',(0.052168390130379,-0.164630467088263,
0.181007512668076));
#41964=CARTESIAN_POINT('Ctrl Pts',(0.166388377416592,-0.04625623707159,
0.188907724532483));
#41965=CARTESIAN_POINT('Ctrl Pts',(0.129651527078137,0.114084236996722,
0.19680793639689));
#41966=CARTESIAN_POINT('Ctrl Pts',(-0.0247124365344563,0.170921113648968,
0.204708148261296));
#41967=CARTESIAN_POINT('Ctrl Pts',(-0.156655896226217,0.072688800963294,
0.212608360125703));
#41968=CARTESIAN_POINT('Ctrl Pts',(-0.146472369316595,-0.0914908554698463,
0.22050857199011));
#41969=CARTESIAN_POINT('Ctrl Pts',(-0.00340092071136592,-0.172664893209074,
0.228408783854516));
#41970=CARTESIAN_POINT('Ctrl Pts',(0.142756033285632,-0.0971876873308804,
0.236308995718923));
#41971=CARTESIAN_POINT('Ctrl Pts',(0.159396733387471,0.0664636215805494,
0.24420920758333));
#41972=CARTESIAN_POINT('Ctrl Pts',(0.0314238061962717,0.169815417475675,
0.252109419447737));
#41973=CARTESIAN_POINT('Ctrl Pts',(-0.12505855466298,0.119101173436036,
0.260009631312144));
#41974=CARTESIAN_POINT('Ctrl Pts',(-0.168080803576887,-0.0396683132637571,
0.26790984317655));
#41975=CARTESIAN_POINT('Ctrl Pts',(-0.0586107512557457,-0.162448488590979,
0.275810055040957));
#41976=CARTESIAN_POINT('Ctrl Pts',(0.104034251124571,-0.137846313701876,
0.283710266905363));
#41977=CARTESIAN_POINT('Ctrl Pts',(0.172293565052386,0.0118177430073507,
0.291610478769771));
#41978=CARTESIAN_POINT('Ctrl Pts',(0.084238525028331,0.150760082612412,
0.299510690634177));
#41979=CARTESIAN_POINT('Ctrl Pts',(-0.0802424140921812,0.15292444732255,
0.307410902498584));
#41980=CARTESIAN_POINT('Ctrl Pts',(-0.171922949352315,0.0163472044781485,
0.315311114362991));
#41981=CARTESIAN_POINT('Ctrl Pts',(-0.107625373942229,-0.135061136127476,
0.323211326227398));
#41982=CARTESIAN_POINT('Ctrl Pts',(0.0543159572952621,-0.163934463708362,
0.331111538091804));
#41983=CARTESIAN_POINT('Ctrl Pts',(0.166978815646636,-0.0440772813759624,
0.339011749956212));
#41984=CARTESIAN_POINT('Ctrl Pts',(0.128149157817753,0.11576927467532,0.346911961820618));
#41985=CARTESIAN_POINT('Ctrl Pts',(-0.0269445799125943,0.17058347288522,
0.354812173685025));
#41986=CARTESIAN_POINT('Ctrl Pts',(-0.157592688461949,0.070634808356674,
0.362712385549432));
#41987=CARTESIAN_POINT('Ctrl Pts',(-0.145263900126163,-0.0933977030145032,
0.370612597413839));
#41988=CARTESIAN_POINT('Ctrl Pts',(-0.00114358090037083,-0.172694596994154,
0.378512809278245));
#41989=CARTESIAN_POINT('Ctrl Pts',(0.144014258847901,-0.0953132984254496,
0.386413021142653));
#41990=CARTESIAN_POINT('Ctrl Pts',(0.15851431213257,0.0685415527792242,
0.394313233007058));
#41991=CARTESIAN_POINT('Ctrl Pts',(0.0292013200165327,0.170211675620508,
0.402213444871466));
#41992=CARTESIAN_POINT('Ctrl Pts',(-0.126604742061452,0.117456250986493,
0.410113656735872));
#41993=CARTESIAN_POINT('Ctrl Pts',(-0.167547904549645,-0.0418620507055259,
0.418013868600279));
#41994=CARTESIAN_POINT('Ctrl Pts',(-0.0564822415909637,-0.163200759781041,
0.425914080464686));
#41995=CARTESIAN_POINT('Ctrl Pts',(0.105827268468801,-0.136474616162425,
0.433814292329093));
#41996=CARTESIAN_POINT('Ctrl Pts',(0.172124364506242,0.0140689285864832,
0.441714504193499));
#41997=CARTESIAN_POINT('Ctrl Pts',(0.0822606147860967,0.15184835482567,
0.449614716057907));
#41998=CARTESIAN_POINT('Ctrl Pts',(-0.0822345632875265,0.151862464780335,
0.457514927922313));
#41999=CARTESIAN_POINT('Ctrl Pts',(-0.172121948383532,0.0140984571108209,
0.465415139786721));
#42000=CARTESIAN_POINT('Ctrl Pts',(-0.105850679763545,-0.13645645899643,
0.473315351651126));
#42001=CARTESIAN_POINT('Ctrl Pts',(0.0564542429141223,-0.163210447169421,
0.481215563515534));
#42002=CARTESIAN_POINT('Ctrl Pts',(0.167540720455548,-0.0418907937079863,
0.48911577537994));
#42003=CARTESIAN_POINT('Ctrl Pts',(0.126624890361875,0.117434529628606,
0.497015987244348));
#42004=CARTESIAN_POINT('Ctrl Pts',(-0.0291721189860838,0.170216682737359,
0.504916199108753));
#42005=CARTESIAN_POINT('Ctrl Pts',(-0.158502551179345,0.068568745634494,
0.512816410973161));
#42006=CARTESIAN_POINT('Ctrl Pts',(-0.14403060816614,-0.0952885907102249,
0.520716622837567));
#42007=CARTESIAN_POINT('Ctrl Pts',(0.00111395432615138,-0.172694790639464,
0.528616834701974));
#42008=CARTESIAN_POINT('Ctrl Pts',(0.145247875180311,-0.0934226223344961,
0.536517046566381));
#42009=CARTESIAN_POINT('Ctrl Pts',(0.157604803871184,0.0706077715621608,
0.544417258430788));
#42010=CARTESIAN_POINT('Ctrl Pts',(0.0269738439003715,0.170578847907609,
0.552317470295194));
#42011=CARTESIAN_POINT('Ctrl Pts',(-0.128129295177092,0.11579125755285,
0.560217682159602));
#42012=CARTESIAN_POINT('Ctrl Pts',(-0.166986374851081,-0.0440486347386962,
0.568117894024008));
#42013=CARTESIAN_POINT('Ctrl Pts',(-0.0543440802119571,-0.163925143142123,
0.576018105888415));
#42014=CARTESIAN_POINT('Ctrl Pts',(0.107602201995467,-0.135079597771001,
0.583918317752822));
#42015=CARTESIAN_POINT('Ctrl Pts',(0.171925751260969,0.0163177100599224,
0.591818529617229));
#42016=CARTESIAN_POINT('Ctrl Pts',(0.0802686478080903,0.152910679114674,
0.599718741481635));
#42017=CARTESIAN_POINT('Ctrl Pts',(-0.0842126601987931,0.150774531902743,
0.607618953346042));
#42018=CARTESIAN_POINT('Ctrl Pts',(-0.172291535128485,0.0118473005919646,
0.615519165210449));
#42019=CARTESIAN_POINT('Ctrl Pts',(-0.104057897766774,-0.137828464116146,
0.623419377074855));
#42020=CARTESIAN_POINT('Ctrl Pts',(0.0585828816032124,-0.162458541146064,
0.631319588939263));
#42021=CARTESIAN_POINT('Ctrl Pts',(0.168073995820709,-0.0396971477198862,
0.639219800803669));
#42022=CARTESIAN_POINT('Ctrl Pts',(0.12507898518031,0.119079717309719,0.647120012668075));
#42023=CARTESIAN_POINT('Ctrl Pts',(-0.0313946731132146,0.169820805875821,
0.655020224532484));
#42024=CARTESIAN_POINT('Ctrl Pts',(-0.159385328899637,0.0664909658504678,
0.662920436396888));
#42025=CARTESIAN_POINT('Ctrl Pts',(-0.142772704183121,-0.0971631954436711,
0.670820648261297));
#42026=CARTESIAN_POINT('Ctrl Pts',(0.00337129920097031,-0.172665474109675,
0.678720860125702));
#42027=CARTESIAN_POINT('Ctrl Pts',(0.146456671479165,-0.0915159821406338,
0.68662107199011));
#42028=CARTESIAN_POINT('Ctrl Pts',(0.156668364025577,0.0726619248576747,
0.694521283854517));
#42029=CARTESIAN_POINT('Ctrl Pts',(0.0247417584705585,0.17091687158558,
0.702421495718924));
#42030=CARTESIAN_POINT('Ctrl Pts',(-0.129631953475511,0.114106477666574,
0.71032170758333));
#42031=CARTESIAN_POINT('Ctrl Pts',(-0.166396310469803,-0.0462276917499887,
0.718221919447737));
#42032=CARTESIAN_POINT('Ctrl Pts',(-0.0521966324240299,-0.164621514831807,
0.726122131312144));
#42033=CARTESIAN_POINT('Ctrl Pts',(0.109358748279947,-0.133661497021884,
0.73402234317655));
#42034=CARTESIAN_POINT('Ctrl Pts',(0.171697759489448,0.0185637033690059,
0.741922555040957));
#42035=CARTESIAN_POINT('Ctrl Pts',(0.0782629640387094,0.153946873541983,
0.749822766905365));
#42036=CARTESIAN_POINT('Ctrl Pts',(-0.0861763659646394,0.149660835369141,
0.75772297876977));
#42037=CARTESIAN_POINT('Ctrl Pts',(-0.17243168220941,0.00959411813254083,
0.765623190634177));
#42038=CARTESIAN_POINT('Ctrl Pts',(-0.102247331262163,-0.139176914249964,
0.773523402498585));
#42039=CARTESIAN_POINT('Ctrl Pts',(0.0607015038436091,-0.161678879418918,
0.78142361436299));
#42040=CARTESIAN_POINT('Ctrl Pts',(0.168578561585846,-0.0374967082074332,
0.7893238262274));
#42041=CARTESIAN_POINT('Ctrl Pts',(0.123511685603348,0.120704537490262,
0.797224038091803));
#42042=CARTESIAN_POINT('Ctrl Pts',(-0.0336118229326868,0.169395946219611,
0.805124249956213));
#42043=CARTESIAN_POINT('Ctrl Pts',(-0.16024094592625,0.0644017551688373,
0.813024461820617));
#42044=CARTESIAN_POINT('Ctrl Pts',(-0.141490260395339,-0.0990210660472952,
0.820924673685026));
#42045=CARTESIAN_POINT('Ctrl Pts',(0.0056277969043301,-0.172606900899112,
0.828824885549431));
#42046=CARTESIAN_POINT('Ctrl Pts',(0.147640956035951,-0.0895932317207615,
0.836725097413839));
#42047=CARTESIAN_POINT('Ctrl Pts',(0.15570417479137,0.0747027653435218,
0.844625309278246));
#42048=CARTESIAN_POINT('Ctrl Pts',(0.022507302267937,0.171227391193745,
0.852525521142652));
#42049=CARTESIAN_POINT('Ctrl Pts',(-0.131115987327984,0.112398966130108,
0.860425733007058));
#42050=CARTESIAN_POINT('Ctrl Pts',(-0.16577111303378,-0.0483927087664539,
0.868325944871467));
#42051=CARTESIAN_POINT('Ctrl Pts',(-0.050052991301314,-0.165301420121155,
0.876226156735872));
#42052=CARTESIAN_POINT('Ctrl Pts',(0.111120800514148,-0.132198387754511,
0.884126368600279));
#42053=CARTESIAN_POINT('Ctrl Pts',(0.171394279774569,0.0207642914265632,
0.892026580464686));
#42054=CARTESIAN_POINT('Ctrl Pts',(0.0763332480962674,0.155038078338273,
0.899926792329093));
#42055=CARTESIAN_POINT('Ctrl Pts',(-0.0883093241020301,0.148357716484315,
0.9078270041935));
#42056=CARTESIAN_POINT('Ctrl Pts',(-0.14415958729081,0.0546064221138428,
0.913093812103104));
#42057=CARTESIAN_POINT('Ctrl Pts',(-0.146217781693074,0.00621955117001918,
0.915727216057906));
#42058=CARTESIAN_POINT('Ctrl Pts',(0.0795408277542851,-0.111329858282328,
-0.0109985226280626));
#42059=CARTESIAN_POINT('Ctrl Pts',(0.116382471927282,-0.0850079450187934,
-0.00836511867326029));
#42060=CARTESIAN_POINT('Ctrl Pts',(0.161279480944341,0.00660620780878029,
-0.00309831076365578));
#42061=CARTESIAN_POINT('Ctrl Pts',(0.0824316996078882,0.138952584071836,
0.00480190110075102));
#42062=CARTESIAN_POINT('Ctrl Pts',(-0.0712663238620885,0.144826122433691,
0.0127021129651578));
#42063=CARTESIAN_POINT('Ctrl Pts',(-0.160274104511912,0.0195101221266785,
0.0206023248295645));
#42064=CARTESIAN_POINT('Ctrl Pts',(-0.103889869629501,-0.123613254448834,
0.0285025366939713));
#42065=CARTESIAN_POINT('Ctrl Pts',(0.0467583358848584,-0.154531728186116,
0.0364027485583782));
#42066=CARTESIAN_POINT('Ctrl Pts',(0.154979882582751,-0.0452798744204848,
0.0443029604227849));
#42067=CARTESIAN_POINT('Ctrl Pts',(0.122597586761272,0.105067940844772,
0.0522031722871918));
#42068=CARTESIAN_POINT('Ctrl Pts',(-0.0210134469518542,0.160084070774355,
0.0601033841515984));
#42069=CARTESIAN_POINT('Ctrl Pts',(-0.145559194164939,0.0698672872613988,
0.0680035960160053));
#42070=CARTESIAN_POINT('Ctrl Pts',(-0.138045878489652,-0.0837392716191075,
0.0759038078804119));
#42071=CARTESIAN_POINT('Ctrl Pts',(-0.00528942707681416,-0.16137168859408,
0.083804019744819));
#42072=CARTESIAN_POINT('Ctrl Pts',(0.132265784240875,-0.0925993168709629,
0.0917042316092254));
#42073=CARTESIAN_POINT('Ctrl Pts',(0.149822136811053,0.0601846625535317,
0.0996044434736326));
#42074=CARTESIAN_POINT('Ctrl Pts',(0.0314514425097271,0.15836557740051,
0.107504655338039));
#42075=CARTESIAN_POINT('Ctrl Pts',(-0.115453743482173,0.112868479032945,
0.115404867202446));
#42076=CARTESIAN_POINT('Ctrl Pts',(-0.157612847166081,-0.0350292615003714,
0.123305079066853));
#42077=CARTESIAN_POINT('Ctrl Pts',(-0.0567767606515088,-0.151146472329493,
0.13120529093126));
#42078=CARTESIAN_POINT('Ctrl Pts',(0.0955703749036966,-0.130135167300756,
0.139105502795666));
#42079=CARTESIAN_POINT('Ctrl Pts',(0.161210724837657,0.00894204350597287,
0.147005714660073));
#42080=CARTESIAN_POINT('Ctrl Pts',(0.0805916924126166,0.139906528844762,
0.15490592652448));
#42081=CARTESIAN_POINT('Ctrl Pts',(-0.0731446283672545,0.143939991967805,
0.162806138388887));
#42082=CARTESIAN_POINT('Ctrl Pts',(-0.160520053454664,0.0173830466635891,
0.170706350253294));
#42083=CARTESIAN_POINT('Ctrl Pts',(-0.102262712397196,-0.124944769797408,
0.1786065621177));
#42084=CARTESIAN_POINT('Ctrl Pts',(0.0487730780976374,-0.153915706589351,
0.186506773982107));
#42085=CARTESIAN_POINT('Ctrl Pts',(0.155559205603179,-0.0432457098552795,
0.194406985846514));
#42086=CARTESIAN_POINT('Ctrl Pts',(0.121213325537862,0.106659212347636,
0.202307197710921));
#42087=CARTESIAN_POINT('Ctrl Pts',(-0.0231040596435062,0.159796934574786,
0.210207409575327));
#42088=CARTESIAN_POINT('Ctrl Pts',(-0.146460150332438,0.0679579445972159,
0.218107621439734));
#42089=CARTESIAN_POINT('Ctrl Pts',(-0.136939405068282,-0.0855362917640029,
0.226007833304141));
#42090=CARTESIAN_POINT('Ctrl Pts',(-0.00317957619632727,-0.16142722250312,
0.233908045168548));
#42091=CARTESIAN_POINT('Ctrl Pts',(0.133464941949482,-0.0908623527095838,
0.241808257032955));
#42092=CARTESIAN_POINT('Ctrl Pts',(0.149022603660681,0.0621379229433468,
0.249708468897361));
#42093=CARTESIAN_POINT('Ctrl Pts',(0.0293786285125025,0.158763201203343,
0.257608680761768));
#42094=CARTESIAN_POINT('Ctrl Pts',(-0.11691928077733,0.111349627983502,
0.265508892626175));
#42095=CARTESIAN_POINT('Ctrl Pts',(-0.157141482401145,-0.0370865525269131,
0.273409104490581));
#42096=CARTESIAN_POINT('Ctrl Pts',(-0.0547961465019971,-0.15187573933352,
0.281309316354988));
#42097=CARTESIAN_POINT('Ctrl Pts',(0.0972633167756718,-0.12887476509914,
0.289209528219395));
#42098=CARTESIAN_POINT('Ctrl Pts',(0.161080061758064,0.0110486005260055,
0.297109740083802));
#42099=CARTESIAN_POINT('Ctrl Pts',(0.0787559698462676,0.140948058103473,
0.305009951948209));
#42100=CARTESIAN_POINT('Ctrl Pts',(-0.0750199406092437,0.142971557942657,
0.312910163812615));
#42101=CARTESIAN_POINT('Ctrl Pts',(-0.160733567100311,0.0152832678696448,
0.320810375677022));
#42102=CARTESIAN_POINT('Ctrl Pts',(-0.100620716020809,-0.12627085719605,
0.328710587541429));
#42103=CARTESIAN_POINT('Ctrl Pts',(0.050780873638021,-0.153265001687028,
0.336610799405836));
#42104=CARTESIAN_POINT('Ctrl Pts',(0.156111215926553,-0.0412085686659782,
0.344511011270243));
#42105=CARTESIAN_POINT('Ctrl Pts',(0.119808736032893,0.108234581533658,
0.35241122313465));
#42106=CARTESIAN_POINT('Ctrl Pts',(-0.0251909268639622,0.15948126872238,
0.360311434999056));
#42107=CARTESIAN_POINT('Ctrl Pts',(-0.147335972660104,0.066037633436295,
0.368211646863463));
#42108=CARTESIAN_POINT('Ctrl Pts',(-0.135809587528269,-0.0873190346085379,
0.37611185872787));
#42109=CARTESIAN_POINT('Ctrl Pts',(-0.00106915242017828,-0.16145499305586,
0.384012070592276));
#42110=CARTESIAN_POINT('Ctrl Pts',(0.134641277532382,-0.0891099559758252,
0.391912282456683));
#42111=CARTESIAN_POINT('Ctrl Pts',(0.148197613649053,0.0640806146840961,
0.39981249432109));
#42112=CARTESIAN_POINT('Ctrl Pts',(0.0273007899642087,0.159133669400588,
0.407712706185496));
#42113=CARTESIAN_POINT('Ctrl Pts',(-0.118364836573682,0.109811763178865,
0.415612918049904));
#42114=CARTESIAN_POINT('Ctrl Pts',(-0.156643266416161,-0.0391375134115731,
0.42351312991431));
#42115=CARTESIAN_POINT('Ctrl Pts',(-0.0528061681290295,-0.152579049928534,
0.431413341778717));
#42116=CARTESIAN_POINT('Ctrl Pts',(0.0989396379107883,-0.12759234271557,
0.439313553643124));
#42117=CARTESIAN_POINT('Ctrl Pts',(0.160921873410089,0.0131532706104934,
0.447213765507531));
#42118=CARTESIAN_POINT('Ctrl Pts',(0.0769067893276909,0.14196550153073,
0.455113977371937));
#42119=CARTESIAN_POINT('Ctrl Pts',(-0.0768824333571298,0.14197869315729,
0.463014189236344));
#42120=CARTESIAN_POINT('Ctrl Pts',(-0.160919614537593,0.0131808773091078,
0.470914401100751));
#42121=CARTESIAN_POINT('Ctrl Pts',(-0.098961525511766,-0.127575367285184,
0.478814612965158));
#42122=CARTESIAN_POINT('Ctrl Pts',(0.0527799917097706,-0.152588106825801,
0.486714824829564));
#42123=CARTESIAN_POINT('Ctrl Pts',(0.156636549889514,-0.0391643857129832,
0.494615036693972));
#42124=CARTESIAN_POINT('Ctrl Pts',(0.118383673548094,0.109791455527395,
0.502515248558378));
#42125=CARTESIAN_POINT('Ctrl Pts',(-0.027273489444968,0.15913835063573,
0.510415460422786));
#42126=CARTESIAN_POINT('Ctrl Pts',(-0.14818661814222,0.0641060377276359,
0.518315672287191));
#42127=CARTESIAN_POINT('Ctrl Pts',(-0.13465656277644,-0.0890868563302129,
0.526215884151598));
#42128=CARTESIAN_POINT('Ctrl Pts',(0.00104145405313166,-0.161455174098016,
0.534116096016006));
#42129=CARTESIAN_POINT('Ctrl Pts',(0.135794605545242,-0.0873423320868967,
0.542016307880412));
#42130=CARTESIAN_POINT('Ctrl Pts',(0.147347299553637,0.0660123562965002,
0.549916519744819));
#42131=CARTESIAN_POINT('Ctrl Pts',(0.025218286243035,0.15947694475544,0.557816731609225));
#42132=CARTESIAN_POINT('Ctrl Pts',(-0.119790166126449,0.108255133684104,
0.565716943473633));
#42133=CARTESIAN_POINT('Ctrl Pts',(-0.156118283149977,-0.0411817864579589,
0.573617155338038));
#42134=CARTESIAN_POINT('Ctrl Pts',(-0.0508071662111437,-0.153256287737759,
0.581517367202447));
#42135=CARTESIAN_POINT('Ctrl Pts',(0.10059905219016,-0.126288117287442,
0.589417579066852));
#42136=CARTESIAN_POINT('Ctrl Pts',(0.160736186650373,0.0152556930573902,
0.597317790931261));
#42137=CARTESIAN_POINT('Ctrl Pts',(0.0750444669377644,0.14295868582074,
0.605218002795666));
#42138=CARTESIAN_POINT('Ctrl Pts',(-0.0787317883956269,0.140961566980476,
0.613118214660074));
#42139=CARTESIAN_POINT('Ctrl Pts',(-0.161078163949129,0.0110762343935455,
0.62101842652448));
#42140=CARTESIAN_POINT('Ctrl Pts',(-0.097285424406824,-0.128858077230555,
0.628918638388887));
#42141=CARTESIAN_POINT('Ctrl Pts',(0.0547700907096662,-0.151885137631092,
0.636818850253293));
#42142=CARTESIAN_POINT('Ctrl Pts',(0.157135117718952,-0.037113510329848,
0.644719062117701));
#42143=CARTESIAN_POINT('Ctrl Pts',(0.116938381600928,0.111329568301349,
0.652619273982107));
#42144=CARTESIAN_POINT('Ctrl Pts',(-0.0293513915183856,0.158768238906452,
0.660519485846514));
#42145=CARTESIAN_POINT('Ctrl Pts',(-0.149011941419152,0.0621634875469089,
0.668419697710921));
#42146=CARTESIAN_POINT('Ctrl Pts',(-0.133480527843221,-0.0908394548451002,
0.676319909575327));
#42147=CARTESIAN_POINT('Ctrl Pts',(0.00315188256353199,-0.161427765596558,
0.684220121439734));
#42148=CARTESIAN_POINT('Ctrl Pts',(0.136924728904249,-0.0855597830979986,
0.692120333304141));
#42149=CARTESIAN_POINT('Ctrl Pts',(0.14647180668124,0.0679328176880866,
0.700020545168548));
#42150=CARTESIAN_POINT('Ctrl Pts',(0.0231314731994126,0.159792968600594,
0.707920757032954));
#42151=CARTESIAN_POINT('Ctrl Pts',(-0.121195025857785,0.106680005512326,
0.715820968897362));
#42152=CARTESIAN_POINT('Ctrl Pts',(-0.155566622343907,-0.0432190223689262,
0.723721180761768));
#42153=CARTESIAN_POINT('Ctrl Pts',(-0.0487994822782217,-0.1539073369789,
0.731621392626175));
#42154=CARTESIAN_POINT('Ctrl Pts',(0.102241275937164,-0.124962311786944,
0.739521604490582));
#42155=CARTESIAN_POINT('Ctrl Pts',(0.160523033427699,0.0173555088039932,
0.747421816354988));
#42156=CARTESIAN_POINT('Ctrl Pts',(0.0731693204960455,0.143927440877225,
0.755322028219396));
#42157=CARTESIAN_POINT('Ctrl Pts',(-0.0805676889177445,0.139920353941802,
0.763222240083802));
#42158=CARTESIAN_POINT('Ctrl Pts',(-0.161209189739,0.00896969739313117,
0.771122451948209));
#42159=CARTESIAN_POINT('Ctrl Pts',(-0.0955926962756769,-0.130118765235746,
0.779022663812615));
#42160=CARTESIAN_POINT('Ctrl Pts',(0.0567508251684453,-0.151156219176586,
0.786922875677023));
#42161=CARTESIAN_POINT('Ctrl Pts',(0.157606844475459,-0.0350562835700847,
0.794823087541428));
#42162=CARTESIAN_POINT('Ctrl Pts',(0.115473087684851,0.112848639167101,
0.802723299405837));
#42163=CARTESIAN_POINT('Ctrl Pts',(-0.0314242410165019,0.158371030690115,
0.810623511270242));
#42164=CARTESIAN_POINT('Ctrl Pts',(-0.149811871720937,0.0602102504337274,
0.81852372313465));
#42165=CARTESIAN_POINT('Ctrl Pts',(-0.132281550246616,-0.0925764083493082,
0.826423934999057));
#42166=CARTESIAN_POINT('Ctrl Pts',(0.00526151903952945,-0.161373004547461,
0.834324146863462));
#42167=CARTESIAN_POINT('Ctrl Pts',(0.138031935836139,-0.0837621723962628,
0.842224358727871));
#42168=CARTESIAN_POINT('Ctrl Pts',(0.145570370453223,0.0698408327169628,
0.850124570592276));
#42169=CARTESIAN_POINT('Ctrl Pts',(0.0210424436816558,0.160083278442666,
0.858024782456684));
#42170=CARTESIAN_POINT('Ctrl Pts',(-0.122582473291093,0.105083625150338,
0.86592499432109));
#42171=CARTESIAN_POINT('Ctrl Pts',(-0.154982115072408,-0.0452431320599261,
0.873825206185497));
#42172=CARTESIAN_POINT('Ctrl Pts',(-0.0467953572586411,-0.154542991514022,
0.881725418049904));
#42173=CARTESIAN_POINT('Ctrl Pts',(0.103888647286289,-0.123594427089244,
0.88962562991431));
#42174=CARTESIAN_POINT('Ctrl Pts',(0.160239305296586,0.0194128744409952,
0.897525841778718));
#42175=CARTESIAN_POINT('Ctrl Pts',(0.0713651976137454,0.14494762602415,
0.905426053643123));
#42176=CARTESIAN_POINT('Ctrl Pts',(-0.0825618262402486,0.138702046860037,
0.913326265507531));
#42177=CARTESIAN_POINT('Ctrl Pts',(-0.134777147462009,0.0510524339304846,
0.918593073417135));
#42178=CARTESIAN_POINT('Ctrl Pts',(-0.136701386950153,0.00581475974607277,
0.921226477371938));
#42179=CARTESIAN_POINT('Ctrl Pts',(0.0740036351041154,-0.103579689087084,
-0.00549926131403137));
#42180=CARTESIAN_POINT('Ctrl Pts',(0.108280567705778,-0.0790901618921417,
-0.00286585735922911));
#42181=CARTESIAN_POINT('Ctrl Pts',(0.150052095188851,0.00614632014659505,
0.00240095055037541));
#42182=CARTESIAN_POINT('Ctrl Pts',(0.0766932604427849,0.129279473432083,
0.0103011624147822));
#42183=CARTESIAN_POINT('Ctrl Pts',(-0.0663051564234898,0.134744128527746,
0.018201374279189));
#42184=CARTESIAN_POINT('Ctrl Pts',(-0.149116707504962,0.0181519352949098,
0.0261015861435957));
#42185=CARTESIAN_POINT('Ctrl Pts',(-0.0966576313088641,-0.115007983126889,
0.0340017980080025));
#42186=CARTESIAN_POINT('Ctrl Pts',(0.0435032790655407,-0.143774083669597,
0.0419020098724094));
#42187=CARTESIAN_POINT('Ctrl Pts',(0.144191040034967,-0.04212773991396,
0.0498022217368161));
#42188=CARTESIAN_POINT('Ctrl Pts',(0.114063020608148,0.0977536917196387,
0.0577024336012229));
#42189=CARTESIAN_POINT('Ctrl Pts',(-0.0195506069575822,0.148939902865525,
0.0656026454656297));
#42190=CARTESIAN_POINT('Ctrl Pts',(-0.13542616785819,0.0650035130157202,
0.0735028573300364));
#42191=CARTESIAN_POINT('Ctrl Pts',(-0.12843588767939,-0.0779098065200985,
0.0814030691944432));
#42192=CARTESIAN_POINT('Ctrl Pts',(-0.00492120640875794,-0.150137883851829,
0.0893032810588501));
#42193=CARTESIAN_POINT('Ctrl Pts',(0.123058171634303,-0.0861530644083569,
0.0972034929232567));
#42194=CARTESIAN_POINT('Ctrl Pts',(0.139392348006922,0.0559949391051687,
0.105103704787664));
#42195=CARTESIAN_POINT('Ctrl Pts',(0.0292619669759775,0.147341041498886,
0.11300391665207));
#42196=CARTESIAN_POINT('Ctrl Pts',(-0.107416492200115,0.105011199568016,
0.120904128516477));
#42197=CARTESIAN_POINT('Ctrl Pts',(-0.146640712181561,-0.0325907179901145,
0.128804340380884));
#42198=CARTESIAN_POINT('Ctrl Pts',(-0.0528242764914083,-0.140624490608767,
0.136704552245291));
#42199=CARTESIAN_POINT('Ctrl Pts',(0.0889172938077157,-0.121075876465457,
0.144604764109697));
#42200=CARTESIAN_POINT('Ctrl Pts',(0.149988125502165,0.00831954787729212,
0.152504975974104));
#42201=CARTESIAN_POINT('Ctrl Pts',(0.0749813443751213,0.130167009844241,
0.160405187838511));
#42202=CARTESIAN_POINT('Ctrl Pts',(-0.0680527037540773,0.133919685565514,
0.168305399702918));
#42203=CARTESIAN_POINT('Ctrl Pts',(-0.149345534842162,0.0161729350650448,
0.176205611567325));
#42204=CARTESIAN_POINT('Ctrl Pts',(-0.0951437477665844,-0.116246805738792,
0.184105823431731));
#42205=CARTESIAN_POINT('Ctrl Pts',(0.0453777660648959,-0.143200946090439,
0.192006035296138));
#42206=CARTESIAN_POINT('Ctrl Pts',(0.144730033789766,-0.040235182638969,
0.199906247160545));
#42207=CARTESIAN_POINT('Ctrl Pts',(0.112775123997586,0.0992341876985505,
0.207806459024951));
#42208=CARTESIAN_POINT('Ctrl Pts',(-0.021495682752556,0.148672755500605,
0.215706670889359));
#42209=CARTESIAN_POINT('Ctrl Pts',(-0.136264404438658,0.063227088231138,
0.223606882753765));
#42210=CARTESIAN_POINT('Ctrl Pts',(-0.127406440819969,-0.0795817280581598,
0.231507094618172));
#42211=CARTESIAN_POINT('Ctrl Pts',(-0.00295823168128856,-0.150189551797165,
0.239407306482579));
#42212=CARTESIAN_POINT('Ctrl Pts',(0.124173850613332,-0.0845370180882872,
0.247307518346986));
#42213=CARTESIAN_POINT('Ctrl Pts',(0.138648473933891,0.0578122243061442,
0.255207730211393));
#42214=CARTESIAN_POINT('Ctrl Pts',(0.0273334508287331,0.147710984931011,
0.263107942075799));
#42215=CARTESIAN_POINT('Ctrl Pts',(-0.108780006891681,0.103598082530968,
0.271008153940206));
#42216=CARTESIAN_POINT('Ctrl Pts',(-0.146202161225402,-0.0345047917900689,
0.278908365804612));
#42217=CARTESIAN_POINT('Ctrl Pts',(-0.0509815417482485,-0.141302990076062,
0.28680857766902));
#42218=CARTESIAN_POINT('Ctrl Pts',(0.0904923824267724,-0.119903216496403,
0.294708789533426));
#42219=CARTESIAN_POINT('Ctrl Pts',(0.149866558463742,0.0102794580446603,
0.302609001397833));
#42220=CARTESIAN_POINT('Ctrl Pts',(0.0732734146642041,0.131136033594535,
0.31050921326224));
#42221=CARTESIAN_POINT('Ctrl Pts',(-0.0697974671263062,0.133018668562764,
0.318409425126647));
#42222=CARTESIAN_POINT('Ctrl Pts',(-0.149544184848307,0.0142193312611412,
0.326309636991054));
#42223=CARTESIAN_POINT('Ctrl Pts',(-0.0936160580993886,-0.117480578264625,
0.33420984885546));
#42224=CARTESIAN_POINT('Ctrl Pts',(0.0472457899807798,-0.142595539665694,
0.342110060719868));
#42225=CARTESIAN_POINT('Ctrl Pts',(0.14524361620647,-0.0383398559559941,
0.350010272584273));
#42226=CARTESIAN_POINT('Ctrl Pts',(0.111468314248034,0.100699888391995,
0.357910484448681));
#42227=CARTESIAN_POINT('Ctrl Pts',(-0.02343727381533,0.148379064559539,
0.365810696313087));
#42228=CARTESIAN_POINT('Ctrl Pts',(-0.137079256858259,0.0614404585159162,
0.373710908177495));
#42229=CARTESIAN_POINT('Ctrl Pts',(-0.126355274930375,-0.0812403662025727,
0.381611120041901));
#42230=CARTESIAN_POINT('Ctrl Pts',(-0.000994723939985704,-0.150215389117566,
0.389511331906308));
#42231=CARTESIAN_POINT('Ctrl Pts',(0.125268296216863,-0.0829066135262008,
0.397411543770714));
#42232=CARTESIAN_POINT('Ctrl Pts',(0.137880915165535,0.0596196765889682,
0.405311755635121));
#42233=CARTESIAN_POINT('Ctrl Pts',(0.0254002599118846,0.148055663180668,
0.413211967499528));
#42234=CARTESIAN_POINT('Ctrl Pts',(-0.110124931085911,0.102167275371236,
0.421112179363935));
#42235=CARTESIAN_POINT('Ctrl Pts',(-0.145738628282677,-0.0364129761176204,
0.429012391228342));
#42236=CARTESIAN_POINT('Ctrl Pts',(-0.0491300946670952,-0.141957340076027,
0.436912603092748));
#42237=CARTESIAN_POINT('Ctrl Pts',(0.0920520073527751,-0.118710069268716,
0.444812814957155));
#42238=CARTESIAN_POINT('Ctrl Pts',(0.149719382313936,0.0122376126345037,
0.452713026821562));
#42239=CARTESIAN_POINT('Ctrl Pts',(0.0715529638692849,0.13208264823579,
0.460613238685969));
#42240=CARTESIAN_POINT('Ctrl Pts',(-0.071530303426733,0.132094921534244,
0.468513450550375));
#42241=CARTESIAN_POINT('Ctrl Pts',(-0.149717280691655,0.0122632975073946,
0.476413662414783));
#42242=CARTESIAN_POINT('Ctrl Pts',(-0.0920723712599867,-0.118694275573937,
0.484313874279189));
#42243=CARTESIAN_POINT('Ctrl Pts',(0.0491057405054188,-0.141965766482181,
0.492214086143596));
#42244=CARTESIAN_POINT('Ctrl Pts',(0.14573237932348,-0.03643797771798,0.500114298008002));
#42245=CARTESIAN_POINT('Ctrl Pts',(0.110142456734312,0.102148381426183,
0.50801450987241));
#42246=CARTESIAN_POINT('Ctrl Pts',(-0.0253748599038521,0.148060018534101,
0.515914721736816));
#42247=CARTESIAN_POINT('Ctrl Pts',(-0.137870685105096,0.0596433298207777,
0.523814933601224));
#42248=CARTESIAN_POINT('Ctrl Pts',(-0.125282517386741,-0.0828851219502007,
0.531715145465628));
#42249=CARTESIAN_POINT('Ctrl Pts',(0.00096895378011186,-0.150215557556568,
0.539615357330038));
#42250=CARTESIAN_POINT('Ctrl Pts',(0.126341335910172,-0.0812620418392971,
0.547515569194442));
#42251=CARTESIAN_POINT('Ctrl Pts',(0.137089795236089,0.0614169410308395,
0.55541578105885));
#42252=CARTESIAN_POINT('Ctrl Pts',(0.0234627285856986,0.148375041603271,
0.563315992923257));
#42253=CARTESIAN_POINT('Ctrl Pts',(-0.111451037075805,0.100719009815358,
0.571216204787664));
#42254=CARTESIAN_POINT('Ctrl Pts',(-0.145250191448873,-0.0383149381772212,
0.57911641665207));
#42255=CARTESIAN_POINT('Ctrl Pts',(-0.0472702522103304,-0.142587432333395,
0.587016628516477));
#42256=CARTESIAN_POINT('Ctrl Pts',(0.0935959023848529,-0.117496636803883,
0.594916840380884));
#42257=CARTESIAN_POINT('Ctrl Pts',(0.149546622039777,0.0141936760548576,
0.60281705224529));
#42258=CARTESIAN_POINT('Ctrl Pts',(0.0698202860674386,0.133006692526806,
0.610717264109698));
#42259=CARTESIAN_POINT('Ctrl Pts',(-0.0732509165924606,0.13114860205821,
0.618617475974104));
#42260=CARTESIAN_POINT('Ctrl Pts',(-0.149864792769772,0.0103051681951267,
0.626517687838512));
#42261=CARTESIAN_POINT('Ctrl Pts',(-0.0905129510468744,-0.119887690344964,
0.634417899702917));
#42262=CARTESIAN_POINT('Ctrl Pts',(0.0509572998161204,-0.141311734116118,
0.642318111567325));
#42263=CARTESIAN_POINT('Ctrl Pts',(0.146196239617194,-0.0345298729398102,
0.650218323431731));
#42264=CARTESIAN_POINT('Ctrl Pts',(0.108797778021546,0.103579419292979,
0.658118535296138));
#42265=CARTESIAN_POINT('Ctrl Pts',(-0.0273081099235566,0.147715671937082,
0.666018747160545));
#42266=CARTESIAN_POINT('Ctrl Pts',(-0.138638553938667,0.0578360092433499,
0.673918959024952));
#42267=CARTESIAN_POINT('Ctrl Pts',(-0.124188351503322,-0.0845157142465292,
0.681819170889359));
#42268=CARTESIAN_POINT('Ctrl Pts',(0.00293246592609361,-0.150190057083441,
0.689719382753765));
#42269=CARTESIAN_POINT('Ctrl Pts',(0.127392786329333,-0.0796035840553634,
0.697619594618173));
#42270=CARTESIAN_POINT('Ctrl Pts',(0.136275249336903,0.0632037105184985,
0.705519806482578));
#42271=CARTESIAN_POINT('Ctrl Pts',(0.0215211879282666,0.148669065615609,
0.713420018346986));
#42272=CARTESIAN_POINT('Ctrl Pts',(-0.11275809824006,0.0992535333580773,
0.721320230211393));
#42273=CARTESIAN_POINT('Ctrl Pts',(-0.144736934218011,-0.0402103529878636,
0.729220442075799));
#42274=CARTESIAN_POINT('Ctrl Pts',(-0.0454023321324136,-0.143193159125993,
0.737120653940206));
#42275=CARTESIAN_POINT('Ctrl Pts',(0.0951238035943801,-0.116263126552003,
0.745020865804613));
#42276=CARTESIAN_POINT('Ctrl Pts',(0.149348307365949,0.0161473142389802,
0.75292107766902));
#42277=CARTESIAN_POINT('Ctrl Pts',(0.0680756769533821,0.133908008212467,
0.760821289533426));
#42278=CARTESIAN_POINT('Ctrl Pts',(-0.0749590118708499,0.130179872514462,
0.768721501397833));
#42279=CARTESIAN_POINT('Ctrl Pts',(-0.149986697268588,0.00834527665372157,
0.77662171326224));
#42280=CARTESIAN_POINT('Ctrl Pts',(-0.0889380612891912,-0.121060616221528,
0.784521925126647));
#42281=CARTESIAN_POINT('Ctrl Pts',(0.0528001464932815,-0.140633558934255,
0.792422136991054));
#42282=CARTESIAN_POINT('Ctrl Pts',(0.146635127365071,-0.0326158589327362,
0.80032234885546));
#42283=CARTESIAN_POINT('Ctrl Pts',(0.107434489766355,0.104992740843939,
0.808222560719866));
#42284=CARTESIAN_POINT('Ctrl Pts',(-0.0292366591003167,0.147346115160618,
0.816122772584275));
#42285=CARTESIAN_POINT('Ctrl Pts',(-0.139382797515625,0.0560187456986177,
0.82402298444868));
#42286=CARTESIAN_POINT('Ctrl Pts',(-0.123072840097892,-0.0861317506513214,
0.831923196313088));
#42287=CARTESIAN_POINT('Ctrl Pts',(0.00489524117472862,-0.150139108195811,
0.839823408177494));
#42288=CARTESIAN_POINT('Ctrl Pts',(0.128422915636328,-0.0779311130717641,
0.847723620041902));
#42289=CARTESIAN_POINT('Ctrl Pts',(0.135436566115076,0.0649789000904037,
0.855623831906308));
#42290=CARTESIAN_POINT('Ctrl Pts',(0.0195775850953746,0.148939165691587,
0.863524043770715));
#42291=CARTESIAN_POINT('Ctrl Pts',(-0.114048959254202,0.0977682841705676,
0.871424255635121));
#42292=CARTESIAN_POINT('Ctrl Pts',(-0.144193117111036,-0.0420935553533985,
0.879324467499528));
#42293=CARTESIAN_POINT('Ctrl Pts',(-0.0435377232159684,-0.143784562906888,
0.887224679363934));
#42294=CARTESIAN_POINT('Ctrl Pts',(0.09665649405843,-0.114990466423977,
0.895124891228342));
#42295=CARTESIAN_POINT('Ctrl Pts',(0.149084330818603,0.0180614574554272,
0.903025103092748));
#42296=CARTESIAN_POINT('Ctrl Pts',(0.0663971471312236,0.134857173710026,
0.910925314957155));
#42297=CARTESIAN_POINT('Ctrl Pts',(-0.0768143283784672,0.129046377235758,
0.918825526821562));
#42298=CARTESIAN_POINT('Ctrl Pts',(-0.125394707633209,0.0474984457471263,
0.924092334731166));
#42299=CARTESIAN_POINT('Ctrl Pts',(-0.127184992207232,0.00540996832212636,
0.926725738685969));
#42300=CARTESIAN_POINT('Ctrl Pts',(0.0684664424539458,-0.0958295198918399,
-1.80411241501588E-16));
#42301=CARTESIAN_POINT('Ctrl Pts',(0.100178663484274,-0.0731723787654901,
0.00263340395480208));
#42302=CARTESIAN_POINT('Ctrl Pts',(0.138824709433362,0.00568643248440989,
0.00790021186440659));
#42303=CARTESIAN_POINT('Ctrl Pts',(0.0709548212776815,0.119606362792331,
0.0158004237288134));
#42304=CARTESIAN_POINT('Ctrl Pts',(-0.0613439889848912,0.1246621346218,
0.0237006355932201));
#42305=CARTESIAN_POINT('Ctrl Pts',(-0.137959310498012,0.016793748463141,
0.0316008474576269));
#42306=CARTESIAN_POINT('Ctrl Pts',(-0.0894253929882274,-0.106402711804945,
0.0395010593220337));
#42307=CARTESIAN_POINT('Ctrl Pts',(0.040248222246223,-0.133016439153077,
0.0474012711864405));
#42308=CARTESIAN_POINT('Ctrl Pts',(0.133402197487182,-0.0389756054074351,
0.0553014830508473));
#42309=CARTESIAN_POINT('Ctrl Pts',(0.105528454455023,0.0904394425945055,
0.0632016949152541));
#42310=CARTESIAN_POINT('Ctrl Pts',(-0.0180877669633101,0.137795734956694,
0.0711019067796609));
#42311=CARTESIAN_POINT('Ctrl Pts',(-0.125293141551441,0.0601397387700418,
0.0790021186440675));
#42312=CARTESIAN_POINT('Ctrl Pts',(-0.118825896869129,-0.0720803414210898,
0.0869023305084746));
#42313=CARTESIAN_POINT('Ctrl Pts',(-0.0045529857407016,-0.138904079109577,
0.0948025423728811));
#42314=CARTESIAN_POINT('Ctrl Pts',(0.113850559027731,-0.0797068119457511,
0.102702754237288));
#42315=CARTESIAN_POINT('Ctrl Pts',(0.12896255920279,0.0518052156568057,
0.110602966101695));
#42316=CARTESIAN_POINT('Ctrl Pts',(0.0270724914422277,0.136316505597261,
0.118503177966102));
#42317=CARTESIAN_POINT('Ctrl Pts',(-0.0993792409180562,0.0971539201030866,
0.126403389830508));
#42318=CARTESIAN_POINT('Ctrl Pts',(-0.135668577197041,-0.0301521744798576,
0.134303601694915));
#42319=CARTESIAN_POINT('Ctrl Pts',(-0.0488717923313075,-0.130102508888041,
0.142203813559322));
#42320=CARTESIAN_POINT('Ctrl Pts',(0.0822642127117346,-0.112016585630158,
0.150104025423729));
#42321=CARTESIAN_POINT('Ctrl Pts',(0.138765526166673,0.00769705224861128,
0.158004237288135));
#42322=CARTESIAN_POINT('Ctrl Pts',(0.0693709963376258,0.12042749084372,
0.165904449152542));
#42323=CARTESIAN_POINT('Ctrl Pts',(-0.0629607791409001,0.123899379163224,
0.173804661016949));
#42324=CARTESIAN_POINT('Ctrl Pts',(-0.138171016229659,0.0149628234665004,
0.181704872881356));
#42325=CARTESIAN_POINT('Ctrl Pts',(-0.088024783135973,-0.107548841680175,
0.189605084745762));
#42326=CARTESIAN_POINT('Ctrl Pts',(0.0419824540321544,-0.132486185591528,
0.197505296610169));
#42327=CARTESIAN_POINT('Ctrl Pts',(0.133900861976353,-0.0372246554226585,
0.205405508474576));
#42328=CARTESIAN_POINT('Ctrl Pts',(0.10433692245731,0.0918091630494651,
0.213305720338983));
#42329=CARTESIAN_POINT('Ctrl Pts',(-0.0198873058616059,0.137548576426424,
0.221205932203389));
#42330=CARTESIAN_POINT('Ctrl Pts',(-0.126068658544878,0.0584962318650602,
0.229106144067797));
#42331=CARTESIAN_POINT('Ctrl Pts',(-0.117873476571655,-0.0736271643523165,
0.237006355932203));
#42332=CARTESIAN_POINT('Ctrl Pts',(-0.00273688716624997,-0.138951881091211,
0.24490656779661));
#42333=CARTESIAN_POINT('Ctrl Pts',(0.114882759277182,-0.0782116834669906,
0.252806779661017));
#42334=CARTESIAN_POINT('Ctrl Pts',(0.128274344207101,0.0534865256689417,
0.260706991525423));
#42335=CARTESIAN_POINT('Ctrl Pts',(0.0252882731449639,0.136658768658679,
0.26860720338983));
#42336=CARTESIAN_POINT('Ctrl Pts',(-0.100640733006032,0.0958465370784341,
0.276507415254237));
#42337=CARTESIAN_POINT('Ctrl Pts',(-0.13526284004966,-0.0319230310532247,
0.284407627118644));
#42338=CARTESIAN_POINT('Ctrl Pts',(-0.0471669369944997,-0.130730240818604,
0.292307838983051));
#42339=CARTESIAN_POINT('Ctrl Pts',(0.0837214480778729,-0.110931667893667,
0.300208050847457));
#42340=CARTESIAN_POINT('Ctrl Pts',(0.138653055169421,0.00951031556331505,
0.308108262711865));
#42341=CARTESIAN_POINT('Ctrl Pts',(0.0677908594821406,0.121324009085596,
0.316008474576271));
#42342=CARTESIAN_POINT('Ctrl Pts',(-0.0645749936433688,0.123065779182871,
0.323908686440678));
#42343=CARTESIAN_POINT('Ctrl Pts',(-0.138354802596303,0.0131553946526375,
0.331808898305084));
#42344=CARTESIAN_POINT('Ctrl Pts',(-0.0866114001779684,-0.108690299333199,
0.339709110169492));
#42345=CARTESIAN_POINT('Ctrl Pts',(0.0437107063235388,-0.131926077644361,
0.347609322033898));
#42346=CARTESIAN_POINT('Ctrl Pts',(0.134376016486386,-0.0354711432460098,
0.355509533898305));
#42347=CARTESIAN_POINT('Ctrl Pts',(0.103127892463174,0.0931651952503325,
0.363409745762711));
#42348=CARTESIAN_POINT('Ctrl Pts',(-0.0216836207666979,0.137276860396698,
0.371309957627119));
#42349=CARTESIAN_POINT('Ctrl Pts',(-0.126822541056414,0.0568432835955372,
0.379210169491525));
#42350=CARTESIAN_POINT('Ctrl Pts',(-0.116900962332481,-0.0751616977966073,
0.387110381355933));
#42351=CARTESIAN_POINT('Ctrl Pts',(-0.000920295459793275,-0.138975785179272,
0.395010593220339));
#42352=CARTESIAN_POINT('Ctrl Pts',(0.115895314901344,-0.0767032710765764,
0.402910805084745));
#42353=CARTESIAN_POINT('Ctrl Pts',(0.127564216682018,0.0551587384938402,
0.410811016949152));
#42354=CARTESIAN_POINT('Ctrl Pts',(0.0234997298595607,0.136977656960748,
0.418711228813559));
#42355=CARTESIAN_POINT('Ctrl Pts',(-0.10188502559814,0.0945227875636074,
0.426611440677966));
#42356=CARTESIAN_POINT('Ctrl Pts',(-0.134833990149192,-0.0336884388236675,
0.434511652542373));
#42357=CARTESIAN_POINT('Ctrl Pts',(-0.045454021205161,-0.13133563022352,
0.44241186440678));
#42358=CARTESIAN_POINT('Ctrl Pts',(0.085164376794762,-0.109827795821861,
0.450312076271186));
#42359=CARTESIAN_POINT('Ctrl Pts',(0.138516891217783,0.0113219546585138,
0.458212288135593));
#42360=CARTESIAN_POINT('Ctrl Pts',(0.0661991384108791,0.12219979494085,
0.4661125));
#42361=CARTESIAN_POINT('Ctrl Pts',(-0.0661781734963363,0.122211149911198,
0.474012711864406));
#42362=CARTESIAN_POINT('Ctrl Pts',(-0.138514946845716,0.0113457177056816,
0.481912923728814));
#42363=CARTESIAN_POINT('Ctrl Pts',(-0.0851832170082076,-0.109813183862691,
0.48981313559322));
#42364=CARTESIAN_POINT('Ctrl Pts',(0.0454314893010671,-0.131343426138561,
0.497713347457628));
#42365=CARTESIAN_POINT('Ctrl Pts',(0.134828208757446,-0.0337115697229769,
0.505613559322033));
#42366=CARTESIAN_POINT('Ctrl Pts',(0.10190123992053,0.0945053073249706,
0.513513771186441));
#42367=CARTESIAN_POINT('Ctrl Pts',(-0.0234762303627364,0.136981686432473,
0.521413983050847));
#42368=CARTESIAN_POINT('Ctrl Pts',(-0.127554752067971,0.0551806219139196,
0.529314194915254));
#42369=CARTESIAN_POINT('Ctrl Pts',(-0.115908471997041,-0.0766833875701887,
0.537214406779661));
#42370=CARTESIAN_POINT('Ctrl Pts',(0.000896453507092177,-0.13897594101512,
0.545114618644068));
#42371=CARTESIAN_POINT('Ctrl Pts',(0.116888066275103,-0.0751817515916976,
0.553014830508475));
#42372=CARTESIAN_POINT('Ctrl Pts',(0.126832290918542,0.0568215257651788,
0.560915042372882));
#42373=CARTESIAN_POINT('Ctrl Pts',(0.0217071709283622,0.137273138451102,
0.568815254237287));
#42374=CARTESIAN_POINT('Ctrl Pts',(-0.103111908025161,0.0931828859466119,
0.576715466101696));
#42375=CARTESIAN_POINT('Ctrl Pts',(-0.134382099747769,-0.0354480898964837,
0.584615677966101));
#42376=CARTESIAN_POINT('Ctrl Pts',(-0.0437333382095171,-0.131918576929031,
0.592515889830509));
#42377=CARTESIAN_POINT('Ctrl Pts',(0.0865927525795457,-0.108705156320324,
0.600416101694915));
#42378=CARTESIAN_POINT('Ctrl Pts',(0.138357057429181,0.0131316590523252,
0.608316313559322));
#42379=CARTESIAN_POINT('Ctrl Pts',(0.0645961051971127,0.123054699232873,
0.616216525423729));
#42380=CARTESIAN_POINT('Ctrl Pts',(-0.0677700447892944,0.121335637135943,
0.624116737288135));
#42381=CARTESIAN_POINT('Ctrl Pts',(-0.138651421590416,0.00953410199670787,
0.632016949152542));
#42382=CARTESIAN_POINT('Ctrl Pts',(-0.0837404776869246,-0.110917303459374,
0.639917161016949));
#42383=CARTESIAN_POINT('Ctrl Pts',(0.0471445089225743,-0.130738330601145,
0.647817372881356));
#42384=CARTESIAN_POINT('Ctrl Pts',(0.135257361515437,-0.0319462355497722,
0.655717584745763));
#42385=CARTESIAN_POINT('Ctrl Pts',(0.100657174442164,0.0958292702846084,
0.66361779661017));
#42386=CARTESIAN_POINT('Ctrl Pts',(-0.0252648283287276,0.136663104967713,
0.671518008474576));
#42387=CARTESIAN_POINT('Ctrl Pts',(-0.128265166458182,0.0535085309397911,
0.679418220338983));
#42388=CARTESIAN_POINT('Ctrl Pts',(-0.114896175163422,-0.0781919736479584,
0.68731843220339));
#42389=CARTESIAN_POINT('Ctrl Pts',(0.00271304928865532,-0.138952348570324,
0.695218644067796));
#42390=CARTESIAN_POINT('Ctrl Pts',(0.117860843754417,-0.0736473850127282,
0.703118855932203));
#42391=CARTESIAN_POINT('Ctrl Pts',(0.126078691992566,0.0584746033489104,
0.711019067796611));
#42392=CARTESIAN_POINT('Ctrl Pts',(0.0199109026571207,0.137545162630623,
0.718919279661016));
#42393=CARTESIAN_POINT('Ctrl Pts',(-0.104321170622334,0.0918270612038291,
0.726819491525424));
#42394=CARTESIAN_POINT('Ctrl Pts',(-0.133907246092115,-0.0372016836068011,
0.73471970338983));
#42395=CARTESIAN_POINT('Ctrl Pts',(-0.0420051819866054,-0.132478981273086,
0.742619915254238));
#42396=CARTESIAN_POINT('Ctrl Pts',(0.0880063312515965,-0.107563941317063,
0.750520127118644));
#42397=CARTESIAN_POINT('Ctrl Pts',(0.1381735813042,0.0149391196739674,0.758420338983051));
#42398=CARTESIAN_POINT('Ctrl Pts',(0.0629820334107182,0.123888575547709,
0.766320550847457));
#42399=CARTESIAN_POINT('Ctrl Pts',(-0.069350334823955,0.120439391087123,
0.774220762711865));
#42400=CARTESIAN_POINT('Ctrl Pts',(-0.138764204798178,0.00772085591431189,
0.78212097457627));
#42401=CARTESIAN_POINT('Ctrl Pts',(-0.0822834263027052,-0.112002467207309,
0.790021186440679));
#42402=CARTESIAN_POINT('Ctrl Pts',(0.0488494678181175,-0.130110898691923,
0.797921398305084));
#42403=CARTESIAN_POINT('Ctrl Pts',(0.135663410254684,-0.0301754342953877,
0.805821610169492));
#42404=CARTESIAN_POINT('Ctrl Pts',(0.0993958918478579,0.0971368425207782,
0.813721822033898));
#42405=CARTESIAN_POINT('Ctrl Pts',(-0.0270490771841315,0.136321199631122,
0.821622033898304));
#42406=CARTESIAN_POINT('Ctrl Pts',(-0.128953723310312,0.0518272409635079,
0.829522245762713));
#42407=CARTESIAN_POINT('Ctrl Pts',(-0.113864129949169,-0.0796870929533346,
0.837422457627119));
#42408=CARTESIAN_POINT('Ctrl Pts',(0.00452896330992775,-0.13890521184416,
0.845322669491525));
#42409=CARTESIAN_POINT('Ctrl Pts',(0.118813895436517,-0.0721000537472655,
0.853222881355933));
#42410=CARTESIAN_POINT('Ctrl Pts',(0.125302761776928,0.0601169674638447,
0.861123093220339));
#42411=CARTESIAN_POINT('Ctrl Pts',(0.0181127265090936,0.137795052940508,
0.869023305084746));
#42412=CARTESIAN_POINT('Ctrl Pts',(-0.105515445217312,0.0904529431907972,
0.876923516949153));
#42413=CARTESIAN_POINT('Ctrl Pts',(-0.133404119149664,-0.0389439786468707,
0.88482372881356));
#42414=CARTESIAN_POINT('Ctrl Pts',(-0.0402800891732956,-0.133026134299755,
0.892723940677965));
#42415=CARTESIAN_POINT('Ctrl Pts',(0.0894243408305711,-0.10638650575871,
0.900624152542373));
#42416=CARTESIAN_POINT('Ctrl Pts',(0.137929356340621,0.0167100404698593,
0.908524364406779));
#42417=CARTESIAN_POINT('Ctrl Pts',(0.0614290966487016,0.124766721395902,
0.916424576271187));
#42418=CARTESIAN_POINT('Ctrl Pts',(-0.0710668305166857,0.11939070761148,
0.924324788135593));
#42419=CARTESIAN_POINT('Ctrl Pts',(-0.116012267804409,0.0439444575637681,
0.929591596045198));
#42420=CARTESIAN_POINT('Ctrl Pts',(-0.11766859746431,0.00500517689817995,
0.932225));
#42421=CARTESIAN_POINT('',(0.0684664424539459,-0.0958295198918398,0.));
#42422=CARTESIAN_POINT('Ctrl Pts',(0.0684664424539458,-0.0958295198918399,
-1.80411241501588E-16));
#42423=CARTESIAN_POINT('Ctrl Pts',(0.100178663484274,-0.0731723787654901,
0.00263340395480208));
#42424=CARTESIAN_POINT('Ctrl Pts',(0.138824709433362,0.00568643248440989,
0.00790021186440659));
#42425=CARTESIAN_POINT('Ctrl Pts',(0.0709548212776815,0.119606362792331,
0.0158004237288134));
#42426=CARTESIAN_POINT('Ctrl Pts',(-0.0613439889848912,0.1246621346218,
0.0237006355932201));
#42427=CARTESIAN_POINT('Ctrl Pts',(-0.115532083261749,0.0483695320037083,
0.0292882571924104));
#42428=CARTESIAN_POINT('Ctrl Pts',(-0.117931878255507,0.00481801833454289,
0.0322424748367984));
#42429=CARTESIAN_POINT('Ctrl Pts',(-0.117896184020664,8.43438525024954E-5,
0.0325632885263842));
#42430=CARTESIAN_POINT('Ctrl Pts',(0.0635538308725813,0.132076982143461,
2.60208521396521E-18));
#42431=CARTESIAN_POINT('Ctrl Pts',(0.0672186180130936,0.129896798349724,
2.66126088244575E-18));
#42432=CARTESIAN_POINT('Ctrl Pts',(0.0707747244255609,0.12755097155874,
-6.59520968701772E-18));
#42433=CARTESIAN_POINT('Ctrl Pts',(0.0742090918971922,0.125038932664582,
-4.55364912443912E-18));
#42434=CARTESIAN_POINT('Ctrl Pts',(0.080224006754745,0.120639374320277,
-2.50552574932592E-18));
#42435=CARTESIAN_POINT('Ctrl Pts',(0.0858662145577153,0.115730301363634,
1.59702880631994E-17));
#42436=CARTESIAN_POINT('Ctrl Pts',(0.0911015321007297,0.110378142457541,
2.25514051876985E-17));
#42437=CARTESIAN_POINT('Ctrl Pts',(0.0937720491785869,0.107648025011046,
2.59084099019214E-17));
#42438=CARTESIAN_POINT('Ctrl Pts',(0.0963357255281008,0.104802798728268,
-1.64960383635052E-18));
#42439=CARTESIAN_POINT('Ctrl Pts',(0.0987794574485338,0.101861414187154,
-4.33680868994202E-19));
#42440=CARTESIAN_POINT('Ctrl Pts',(0.10293496714428,0.0968596577026072,
1.63396805676607E-18));
#42441=CARTESIAN_POINT('Ctrl Pts',(0.106751261320725,0.0915729561578743,
3.03784192455847E-17));
#42442=CARTESIAN_POINT('Ctrl Pts',(0.110204305377691,0.08604549563647,2.73218947466347E-17));
#42443=CARTESIAN_POINT('Ctrl Pts',(0.111935557805272,0.0832741931890737,
2.57894452987073E-17));
#42444=CARTESIAN_POINT('Ctrl Pts',(0.113575375365209,0.0804423219653594,
5.7323915193469E-18));
#42445=CARTESIAN_POINT('Ctrl Pts',(0.115119932079619,0.077555293108205,
9.54097911787244E-18));
#42446=CARTESIAN_POINT('Ctrl Pts',(0.116773389847001,0.0744647103902093,
1.36180963184181E-17));
#42447=CARTESIAN_POINT('Ctrl Pts',(0.118313357645953,0.0713188633723711,
-9.33067413676427E-18));
#42448=CARTESIAN_POINT('Ctrl Pts',(0.119735247150481,0.0681278580844796,
-4.33680868994202E-18));
#42449=CARTESIAN_POINT('Ctrl Pts',(0.123742606948277,0.059134538797346,
9.73757301374157E-18));
#42450=CARTESIAN_POINT('Ctrl Pts',(0.126819919828835,0.0497749725291024,
2.44496492997929E-17));
#42451=CARTESIAN_POINT('Ctrl Pts',(0.128866909768778,0.040203097865136,
1.21430643318376E-17));
#42452=CARTESIAN_POINT('Ctrl Pts',(0.129678753995803,0.0364068548860612,
7.26222453596554E-18));
#42453=CARTESIAN_POINT('Ctrl Pts',(0.130327963181773,0.0325772120613575,
7.16378425601151E-18));
#42454=CARTESIAN_POINT('Ctrl Pts',(0.130805907644987,0.0287241348669356,
3.46944695195361E-18));
#42455=CARTESIAN_POINT('Ctrl Pts',(0.131145551201884,0.0259860074399329,
8.44125478642762E-19));
#42456=CARTESIAN_POINT('Ctrl Pts',(0.131398222957245,0.023238193513084,
1.89851870451249E-17));
#42457=CARTESIAN_POINT('Ctrl Pts',(0.131560851492827,0.0204930145081475,
1.56125112837913E-17));
#42458=CARTESIAN_POINT('Ctrl Pts',(0.131856680066531,0.0154994112226654,
9.47746335708933E-18));
#42459=CARTESIAN_POINT('Ctrl Pts',(0.131855937211452,0.0105061465300757,
1.21882171850414E-17));
#42460=CARTESIAN_POINT('Ctrl Pts',(0.131544012134307,0.00553446959878105,
1.73472347597681E-17));
#42461=CARTESIAN_POINT('Ctrl Pts',(0.131183605376493,-0.00020994178392047,
2.50428281171472E-17));
#42462=CARTESIAN_POINT('Ctrl Pts',(0.130407809774817,-0.00592569963173127,
6.69723701682335E-18));
#42463=CARTESIAN_POINT('Ctrl Pts',(0.129236296320737,-0.0115776207498215,
6.93889390390723E-18));
#42464=CARTESIAN_POINT('Ctrl Pts',(0.128494418700647,-0.0151567804883794,
7.09192657770507E-18));
#42465=CARTESIAN_POINT('Ctrl Pts',(0.127593716302061,-0.0187102876496501,
1.81123981287573E-17));
#42466=CARTESIAN_POINT('Ctrl Pts',(0.126538054496122,-0.0222283432593045,
1.73472347597681E-17));
#42467=CARTESIAN_POINT('Ctrl Pts',(0.125628643409289,-0.0252590096692432,
1.66880766401104E-17));
#42468=CARTESIAN_POINT('Ctrl Pts',(0.124606340862147,-0.0282558643089978,
1.76789329645073E-17));
#42469=CARTESIAN_POINT('Ctrl Pts',(0.123476980164864,-0.0312080791264482,
1.38777878078145E-17));
#42470=CARTESIAN_POINT('Ctrl Pts',(0.120897724271906,-0.0379504046593839,
5.19665867965098E-18));
#42471=CARTESIAN_POINT('Ctrl Pts',(0.117758352703866,-0.0444696874516502,
3.23003755723985E-17));
#42472=CARTESIAN_POINT('Ctrl Pts',(0.114097802370374,-0.050694248232474,
2.94902990916057E-17));
#42473=CARTESIAN_POINT('Ctrl Pts',(0.11100985408088,-0.0559451313142133,
2.71197891759751E-17));
#42474=CARTESIAN_POINT('Ctrl Pts',(0.107550620981395,-0.0609862743257036,
5.91633367061488E-18));
#42475=CARTESIAN_POINT('Ctrl Pts',(0.103737131336817,-0.0657661572550731,
2.08166817117217E-17));
#42476=CARTESIAN_POINT('Ctrl Pts',(0.10192691642303,-0.0680351067400168,
2.78896869532561E-17));
#42477=CARTESIAN_POINT('Ctrl Pts',(0.10004287794431,-0.0702374362624183,
3.79094719020518E-18));
#42478=CARTESIAN_POINT('Ctrl Pts',(0.098088083467589,-0.0723681596371707,
3.46944695195361E-18));
#42479=CARTESIAN_POINT('Ctrl Pts',(0.092197190805992,-0.078789224788366,
2.50058632912494E-18));
#42480=CARTESIAN_POINT('Ctrl Pts',(0.0856641330198359,-0.0845647204793276,
-6.81778632605364E-18));
#42481=CARTESIAN_POINT('Ctrl Pts',(0.0785460746715851,-0.0895442682019542,
-6.93889390390723E-18));
#42482=CARTESIAN_POINT('Ctrl Pts',(0.0753062120776356,-0.0918107641495869,
-6.9940173507989E-18));
#42483=CARTESIAN_POINT('Ctrl Pts',(0.0719448689431282,-0.0939117521002605,
3.85531108019535E-18));
#42484=CARTESIAN_POINT('Ctrl Pts',(0.068466442453948,-0.0958295198918383,
3.46944695195361E-18));
#42485=CARTESIAN_POINT('Ctrl Pts',(-0.00156268643912563,0.146080787864432,
0.903650000000001));
#42486=CARTESIAN_POINT('Ctrl Pts',(0.0213629386064158,0.146372019480346,
0.902408930776365));
#42487=CARTESIAN_POINT('Ctrl Pts',(0.0443374951530579,0.14156774719521,
0.901167861552729));
#42488=CARTESIAN_POINT('Ctrl Pts',(0.0647363246762687,0.131545720210662,
0.899926792329093));
#42489=CARTESIAN_POINT('Ctrl Pts',(0.108020258655701,0.110280149367703,
0.897293388374291));
#42490=CARTESIAN_POINT('Ctrl Pts',(0.139707269215135,0.0655222203971333,
0.894659984419488));
#42491=CARTESIAN_POINT('Ctrl Pts',(0.145505194618115,0.0176494760483365,
0.892026580464686));
#42492=CARTESIAN_POINT('Ctrl Pts',(0.151303120021096,-0.0302232683004618,
0.889393176509884));
#42493=CARTESIAN_POINT('Ctrl Pts',(0.131211960267621,-0.0812108280274876,
0.886759772555081));
#42494=CARTESIAN_POINT('Ctrl Pts',(0.0943040817549728,-0.112221779952107,
0.884126368600279));
#42495=CARTESIAN_POINT('Ctrl Pts',(0.0573962032423251,-0.143232731876727,
0.881492964645477));
#42496=CARTESIAN_POINT('Ctrl Pts',(0.0036716059705044,-0.15426707599894,
0.878859560690674));
#42497=CARTESIAN_POINT('Ctrl Pts',(-0.0424770462874833,-0.140299462834264,
0.876226156735872));
#42498=CARTESIAN_POINT('Ctrl Pts',(-0.0886256985454704,-0.126331849669587,
0.87359275278107));
#42499=CARTESIAN_POINT('Ctrl Pts',(-0.127198405789625,-0.0873622792180203,
0.870959348826268));
#42500=CARTESIAN_POINT('Ctrl Pts',(-0.140708905127403,-0.0410788815094769,
0.868325944871466));
#42501=CARTESIAN_POINT('Ctrl Pts',(-0.144574583355673,-0.027836090226996,
0.867572464775741));
#42502=CARTESIAN_POINT('Ctrl Pts',(-0.146388495105525,-0.0139945382267495,
0.866818984680017));
#42503=CARTESIAN_POINT('Ctrl Pts',(-0.146273246343463,-0.000123611542196964,
0.866065504584292));
#42504=CARTESIAN_POINT('Origin',(0.,0.,-0.0924367114736152));
#42505=CARTESIAN_POINT('',(-0.0684664424539439,-0.0958295198918412,0.));
#42506=CARTESIAN_POINT('Ctrl Pts',(-0.0686121729278148,-0.0959472995825297,
4.17959937493162E-17));
#42507=CARTESIAN_POINT('Ctrl Pts',(-0.0396139635805184,-0.116414379406814,
0.00240676188548629));
#42508=CARTESIAN_POINT('Ctrl Pts',(0.042075530384929,-0.130578648252184,
0.00744886483747836));
#42509=CARTESIAN_POINT('Ctrl Pts',(0.133186295059001,-0.0398205273591854,
0.0151263088559762));
#42510=CARTESIAN_POINT('Ctrl Pts',(0.106043485420733,0.0899039768168324,
0.0230323320554937));
#42511=CARTESIAN_POINT('Ctrl Pts',(-0.0174538572390982,0.137906280269365,
0.0309383552550111));
#42512=CARTESIAN_POINT('Ctrl Pts',(-0.105510720744521,0.0746991700253994,
0.0374064817277185));
#42513=CARTESIAN_POINT('Ctrl Pts',(-0.11763008980369,0.0178164887288322,
0.0412392671339201));
#42514=CARTESIAN_POINT('Ctrl Pts',(-0.117591431864639,2.92794590778002E-5,
0.0424367114736158));
#42515=CARTESIAN_POINT('Origin',(0.,0.,0.));
#42516=CARTESIAN_POINT('Ctrl Pts',(-0.0510216505388444,0.106149619882937,
-0.0164977839420935));
#42517=CARTESIAN_POINT('Ctrl Pts',(-0.0861748725546967,0.0892529469510397,
-0.0138624428755877));
#42518=CARTESIAN_POINT('Ctrl Pts',(-0.137790539141881,0.0181049606281334,
-0.0085917607425761));
#42519=CARTESIAN_POINT('Ctrl Pts',(-0.0902797247787074,-0.10582739645577,
-0.000685737543058663));
#42520=CARTESIAN_POINT('Ctrl Pts',(0.0393629057248093,-0.133280773711466,
0.00722028565645879));
#42521=CARTESIAN_POINT('Ctrl Pts',(0.133186295059001,-0.0398205273591854,
0.0151263088559762));
#42522=CARTESIAN_POINT('Ctrl Pts',(0.106043485420733,0.0899039768168324,
0.0230323320554937));
#42523=CARTESIAN_POINT('Ctrl Pts',(-0.0174538572390982,0.137906280269365,
0.0309383552550111));
#42524=CARTESIAN_POINT('Ctrl Pts',(-0.125086200033906,0.0606479146403327,
0.0388443784545286));
#42525=CARTESIAN_POINT('Ctrl Pts',(-0.119084788854313,-0.0717206569949895,
0.046750401654046));
#42526=CARTESIAN_POINT('Ctrl Pts',(-0.00489492837772915,-0.138925734589418,
0.0546564248535634));
#42527=CARTESIAN_POINT('Ctrl Pts',(0.113740629398734,-0.0799231888543136,
0.062562448053081));
#42528=CARTESIAN_POINT('Ctrl Pts',(0.129045816271948,0.0516898037714297,
0.0704684712525983));
#42529=CARTESIAN_POINT('Ctrl Pts',(0.0271151839788463,0.136342686033388,
0.0783744944521158));
#42530=CARTESIAN_POINT('Ctrl Pts',(-0.0994488545192835,0.097131556418157,
0.0862805176516332));
#42531=CARTESIAN_POINT('Ctrl Pts',(-0.135665746467832,-0.0303218706918135,
0.0941865408511506));
#42532=CARTESIAN_POINT('Ctrl Pts',(-0.0486330432543111,-0.130228357167641,
0.102092564050668));
#42533=CARTESIAN_POINT('Ctrl Pts',(0.0825817545836372,-0.111825131042891,
0.109998587250186));
#42534=CARTESIAN_POINT('Ctrl Pts',(0.138772738128538,0.00816897019039422,
0.117904610449703));
#42535=CARTESIAN_POINT('Ctrl Pts',(0.0688915313895657,0.120741708772585,
0.12581063364922));
#42536=CARTESIAN_POINT('Ctrl Pts',(-0.0635762130827019,0.123623095373164,
0.133716656848738));
#42537=CARTESIAN_POINT('Ctrl Pts',(-0.138286275523292,0.014195432572335,
0.141622680048255));
#42538=CARTESIAN_POINT('Ctrl Pts',(-0.0873660952430369,-0.108128486159945,
0.149528703247773));
#42539=CARTESIAN_POINT('Ctrl Pts',(0.0429243879661372,-0.132219897211806,
0.15743472644729));
#42540=CARTESIAN_POINT('Ctrl Pts',(0.134218946443888,-0.0361922458912883,
0.165340749646808));
#42541=CARTESIAN_POINT('Ctrl Pts',(0.103578348063976,0.0927153171784346,
0.173246772846325));
#42542=CARTESIAN_POINT('Ctrl Pts',(-0.0211610525014389,0.137392918706172,
0.181152796045843));
#42543=CARTESIAN_POINT('Ctrl Pts',(-0.126676071448117,0.0572518747851005,
0.18905881924536));
#42544=CARTESIAN_POINT('Ctrl Pts',(-0.117108480713923,-0.074901321664099,
0.196964842444878));
#42545=CARTESIAN_POINT('Ctrl Pts',(-0.00115024004832317,-0.139008205490464,
0.204870865644395));
#42546=CARTESIAN_POINT('Ctrl Pts',(0.115852970087698,-0.0768289890996742,
0.212776888843912));
#42547=CARTESIAN_POINT('Ctrl Pts',(0.127606135899372,0.055147786219953,
0.22068291204343));
#42548=CARTESIAN_POINT('Ctrl Pts',(0.0234317475993789,0.137023930205902,
0.228588935242947));
#42549=CARTESIAN_POINT('Ctrl Pts',(-0.102029902232137,0.0944166473397004,
0.236494958442465));
#42550=CARTESIAN_POINT('Ctrl Pts',(-0.134799481036655,-0.0339662208175969,
0.244400981641982));
#42551=CARTESIAN_POINT('Ctrl Pts',(-0.0451064993838265,-0.131491474848312,
0.252307004841499));
#42552=CARTESIAN_POINT('Ctrl Pts',(0.0855648107118161,-0.1095594241143,
0.260213028041017));
#42553=CARTESIAN_POINT('Ctrl Pts',(0.138502247321704,0.0119051136596435,
0.268119051240535));
#42554=CARTESIAN_POINT('Ctrl Pts',(0.0656132363391791,0.122554100141606,
0.276025074440052));
#42555=CARTESIAN_POINT('Ctrl Pts',(-0.066884052510702,0.121865203254083,
0.283931097639569));
#42556=CARTESIAN_POINT('Ctrl Pts',(-0.138618553097211,0.010464271673199,
0.291837120839087));
#42557=CARTESIAN_POINT('Ctrl Pts',(-0.0844209446825288,-0.110443235842333,
0.299743144038604));
#42558=CARTESIAN_POINT('Ctrl Pts',(0.046471358419155,-0.131015331511595,
0.307649167238122));
#42559=CARTESIAN_POINT('Ctrl Pts',(0.135145386671506,-0.0325626888604762,
0.315555190437639));
#42560=CARTESIAN_POINT('Ctrl Pts',(0.101042606300054,0.0954724879559945,
0.323461213637157));
#42561=CARTESIAN_POINT('Ctrl Pts',(-0.0248553070174182,0.136772869961425,
0.331367236836674));
#42562=CARTESIAN_POINT('Ctrl Pts',(-0.12817268430534,0.0538179081940093,
0.339273260036191));
#42563=CARTESIAN_POINT('Ctrl Pts',(-0.115047809886908,-0.0780295180341452,
0.347179283235709));
#42564=CARTESIAN_POINT('Ctrl Pts',(0.00259563734382704,-0.138988729439456,
0.355085306435226));
#42565=CARTESIAN_POINT('Ctrl Pts',(0.117881001348277,-0.0736795342380946,
0.362991329634744));
#42566=CARTESIAN_POINT('Ctrl Pts',(0.12607389627645,0.0585660048329233,
0.370897352834261));
#42567=CARTESIAN_POINT('Ctrl Pts',(0.0197312453245754,0.137605531147394,
0.378803376033779));
#42568=CARTESIAN_POINT('Ctrl Pts',(-0.104536836829869,0.0916332580999962,
0.386709399233296));
#42569=CARTESIAN_POINT('Ctrl Pts',(-0.133835349354862,-0.0375859482716227,
0.394615422432814));
#42570=CARTESIAN_POINT('Ctrl Pts',(-0.0415471952570256,-0.13265909245389,
0.40252144563233));
#42571=CARTESIAN_POINT('Ctrl Pts',(0.0884857325734624,-0.107214175253801,
0.410427468831849));
#42572=CARTESIAN_POINT('Ctrl Pts',(0.138131189387156,0.0156326185555932,
0.418333492031365));
#42573=CARTESIAN_POINT('Ctrl Pts',(0.062287297122381,0.124277499418049,
0.426239515230884));
#42574=CARTESIAN_POINT('Ctrl Pts',(-0.0701433255283678,0.120018824057881,
0.4341455384304));
#42575=CARTESIAN_POINT('Ctrl Pts',(-0.138850177307333,0.00672551158926456,
0.442051561629919));
#42576=CARTESIAN_POINT('Ctrl Pts',(-0.0814144942465354,-0.11267779005197,
0.449957584829435));
#42577=CARTESIAN_POINT('Ctrl Pts',(0.0499845850166584,-0.129715633233345,
0.457863608028953));
#42578=CARTESIAN_POINT('Ctrl Pts',(0.135973695209673,-0.0289094872912353,
0.465769631228471));
#42579=CARTESIAN_POINT('Ctrl Pts',(0.0984334954810092,0.0981603342078928,
0.473675654427988));
#42580=CARTESIAN_POINT('Ctrl Pts',(-0.0285315135918273,0.136053507770195,
0.481581677627505));
#42581=CARTESIAN_POINT('Ctrl Pts',(-0.129576228451988,0.0503448633385094,
0.489487700827023));
#42582=CARTESIAN_POINT('Ctrl Pts',(-0.112903600569895,-0.0811010556205559,
0.49739372402654));
#42583=CARTESIAN_POINT('Ctrl Pts',(0.00633962999064621,-0.138868330932566,
0.505299747226058));
#42584=CARTESIAN_POINT('Ctrl Pts',(0.119823436886959,-0.0704765792090683,
0.513205770425575));
#42585=CARTESIAN_POINT('Ctrl Pts',(0.124450111907394,0.0619416975118724,
0.521111793625093));
#42586=CARTESIAN_POINT('Ctrl Pts',(0.0160164158031762,0.138087213996209,
0.52901781682461));
#42587=CARTESIAN_POINT('Ctrl Pts',(-0.106967865166254,0.0887833321417318,
0.536923840024128));
#42588=CARTESIAN_POINT('Ctrl Pts',(-0.132774037183017,-0.0411783838262002,
0.544829863223645));
#42589=CARTESIAN_POINT('Ctrl Pts',(-0.0379577228913647,-0.133730383672961,
0.552735886423163));
#42590=CARTESIAN_POINT('Ctrl Pts',(0.0913424031974019,-0.104791076063462,
0.56064190962268));
#42591=CARTESIAN_POINT('Ctrl Pts',(0.137659831668342,0.0193487722984857,
0.568547932822197));
#42592=CARTESIAN_POINT('Ctrl Pts',(0.0589161298691768,0.125910658348106,
0.576453956021715));
#42593=CARTESIAN_POINT('Ctrl Pts',(-0.0733516660922674,0.11808529682354,
0.584359979221232));
#42594=CARTESIAN_POINT('Ctrl Pts',(-0.138980979661871,0.00298186797856315,
0.59226600242075));
#42595=CARTESIAN_POINT('Ctrl Pts',(-0.0783489271385985,-0.114830526693234,
0.600172025620267));
#42596=CARTESIAN_POINT('Ctrl Pts',(0.0534615168199478,-0.12832174587234,
0.608078048819785));
#42597=CARTESIAN_POINT('Ctrl Pts',(0.136703270562712,-0.0252352939724056,
0.615984072019302));
#42598=CARTESIAN_POINT('Ctrl Pts',(0.0957529101571512,0.100776904302778,
0.623890095218819));
#42599=CARTESIAN_POINT('Ctrl Pts',(-0.0321870028708045,0.135235354440354,
0.631796118418337));
#42600=CARTESIAN_POINT('Ctrl Pts',(-0.130885684740464,0.0468352620836017,
0.639702141617854));
#42601=CARTESIAN_POINT('Ctrl Pts',(-0.110677409719003,-0.0841137041290149,
0.647608164817372));
#42602=CARTESIAN_POINT('Ctrl Pts',(0.0100790193068892,-0.138647097388359,
0.655514188016889));
#42603=CARTESIAN_POINT('Ctrl Pts',(0.121678866262096,-0.0672224497442505,
0.663420211216407));
#42604=CARTESIAN_POINT('Ctrl Pts',(0.122735961854403,0.0652724131012164,
0.671326234415924));
#42605=CARTESIAN_POINT('Ctrl Pts',(0.0122899564463577,0.138468628991968,
0.679232257615441));
#42606=CARTESIAN_POINT('Ctrl Pts',(-0.109321222024174,0.0858689388531973,
0.687138280814959));
#42607=CARTESIAN_POINT('Ctrl Pts',(-0.131616315159593,-0.0447409189438641,
0.695044304014476));
#42608=CARTESIAN_POINT('Ctrl Pts',(-0.0343406886760894,-0.134704570618338,
0.702950327213994));
#42609=CARTESIAN_POINT('Ctrl Pts',(0.0941327483034478,-0.102291886006113,
0.710856350413511));
#42610=CARTESIAN_POINT('Ctrl Pts',(0.137088516418336,0.0230508765206803,
0.718762373613029));
#42611=CARTESIAN_POINT('Ctrl Pts',(0.0555021824679276,0.127452391053421,
0.726668396812546));
#42612=CARTESIAN_POINT('Ctrl Pts',(-0.0765067445957343,0.116066025541209,
0.734574420012063));
#42613=CARTESIAN_POINT('Ctrl Pts',(-0.139010865120405,-0.000763940859230431,
0.742480443211581));
#42614=CARTESIAN_POINT('Ctrl Pts',(-0.0752264694457675,-0.116899882557203,
0.750386466411098));
#42615=CARTESIAN_POINT('Ctrl Pts',(0.0568996293847587,-0.126834681679914,
0.758292489610617));
#42616=CARTESIAN_POINT('Ctrl Pts',(0.137333582544999,-0.0215427765762162,
0.766198512810132));
#42617=CARTESIAN_POINT('Ctrl Pts',(0.0930027975645983,0.103320297856606,
0.774104536009652));
#42618=CARTESIAN_POINT('Ctrl Pts',(-0.035819122070238,0.13431900488649,
0.782010559209168));
#42619=CARTESIAN_POINT('Ctrl Pts',(-0.13210009942588,0.0432916512297215,
0.789916582408685));
#42620=CARTESIAN_POINT('Ctrl Pts',(-0.108370859366875,-0.0870652729953126,
0.797822605608204));
#42621=CARTESIAN_POINT('Ctrl Pts',(0.0138111005924944,-0.138325195186183,
0.80572862880772));
#42622=CARTESIAN_POINT('Ctrl Pts',(0.123445922182148,-0.0639194978340518,
0.813634652007238));
#42623=CARTESIAN_POINT('Ctrl Pts',(0.120932728835538,0.0685557124046954,
0.821540675206756));
#42624=CARTESIAN_POINT('Ctrl Pts',(0.0085545008581314,0.138749538494654,
0.829446698406273));
#42625=CARTESIAN_POINT('Ctrl Pts',(-0.111595061352101,0.0828921197631381,
0.837352721605791));
#42626=CARTESIAN_POINT('Ctrl Pts',(-0.130363284584795,-0.0482708249720888,
0.845258744805308));
#42627=CARTESIAN_POINT('Ctrl Pts',(-0.0306982239304521,-0.135581215292453,
0.853164768004825));
#42628=CARTESIAN_POINT('Ctrl Pts',(0.0968538014257187,-0.0997179081430208,
0.861070791204343));
#42629=CARTESIAN_POINT('Ctrl Pts',(0.136419444538435,0.0267352712365894,
0.86897681440386));
#42630=CARTESIAN_POINT('Ctrl Pts',(0.0520445414416943,0.128903423908239,
0.876882837603378));
#42631=CARTESIAN_POINT('Ctrl Pts',(-0.0795998263876522,0.113958970288921,
0.884788860802895));
#42632=CARTESIAN_POINT('Ctrl Pts',(-0.138952053011478,-0.00450253390371847,
0.892694884002413));
#42633=CARTESIAN_POINT('Ctrl Pts',(-0.0720261204166176,-0.118897020856024,
0.90060090720193));
#42634=CARTESIAN_POINT('Ctrl Pts',(0.0602520802431792,-0.125231345176025,
0.908506930401448));
#42635=CARTESIAN_POINT('Ctrl Pts',(0.137949690524835,-0.017881538827179,
0.916412953600965));
#42636=CARTESIAN_POINT('Ctrl Pts',(0.0900118016872842,0.105886249500893,
0.924318976800482));
#42637=CARTESIAN_POINT('Ctrl Pts',(0.00399973323748277,0.12400080376067,
0.929589658933494));
#42638=CARTESIAN_POINT('Ctrl Pts',(-0.0334019664626807,0.112939183906322,
0.932225));
#42639=CARTESIAN_POINT('Ctrl Pts',(-0.0551480035117367,0.114734422509853,
-0.0109985226280624));
#42640=CARTESIAN_POINT('Ctrl Pts',(-0.0931442265014884,0.0964712387762041,
-0.00836318156155655));
#42641=CARTESIAN_POINT('Ctrl Pts',(-0.148934286841532,0.0195691911522949,
-0.00309249942854491));
#42642=CARTESIAN_POINT('Ctrl Pts',(-0.097581056797534,-0.114386139408358,
0.00481352377097251));
#42643=CARTESIAN_POINT('Ctrl Pts',(0.0425463629697991,-0.144059796166161,
0.01271954697049));
#42644=CARTESIAN_POINT('Ctrl Pts',(0.143957676595294,-0.0430409945474375,
0.0206255701700074));
#42645=CARTESIAN_POINT('Ctrl Pts',(0.114619704470892,0.0971749203887298,
0.0285315933695248));
#42646=CARTESIAN_POINT('Ctrl Pts',(-0.0188654300703636,0.149059388480494,
0.0364376165690423));
#42647=CARTESIAN_POINT('Ctrl Pts',(-0.13520249003877,0.065552787380297,
0.0443436397685597));
#42648=CARTESIAN_POINT('Ctrl Pts',(-0.128715717437097,-0.0775210327782809,
0.0522496629680772));
#42649=CARTESIAN_POINT('Ctrl Pts',(-0.0052908035023142,-0.150161290708834,
0.0601556861675946));
#42650=CARTESIAN_POINT('Ctrl Pts',(0.122939351496148,-0.0863869407017978,
0.0680617093671122));
#42651=CARTESIAN_POINT('Ctrl Pts',(0.139482338453993,0.0558701933356218,
0.0759677325666295));
#42652=CARTESIAN_POINT('Ctrl Pts',(0.0293081122522375,0.147369339265975,
0.0838737557661469));
#42653=CARTESIAN_POINT('Ctrl Pts',(-0.10749173576994,0.104987027230155,
0.0917797789656645));
#42654=CARTESIAN_POINT('Ctrl Pts',(-0.146637652518404,-0.032774138306667,
0.0996858021651818));
#42655=CARTESIAN_POINT('Ctrl Pts',(-0.0525662186905025,-0.140760516811213,
0.107591825364699));
#42656=CARTESIAN_POINT('Ctrl Pts',(0.089260516735274,-0.120868938074804,
0.115497848564217));
#42657=CARTESIAN_POINT('Ctrl Pts',(0.149995920728193,0.0088296319697477,
0.123403871763734));
#42658=CARTESIAN_POINT('Ctrl Pts',(0.0744631029156597,0.130506640006368,
0.131309894963252));
#42659=CARTESIAN_POINT('Ctrl Pts',(-0.0687179106383172,0.133621057448557,
0.139215918162769));
#42660=CARTESIAN_POINT('Ctrl Pts',(-0.149470115679177,0.0153434817784622,
0.147121941362287));
#42661=CARTESIAN_POINT('Ctrl Pts',(-0.0944317887874227,-0.116873328704402,
0.155027964561804));
#42662=CARTESIAN_POINT('Ctrl Pts',(0.0463958784809096,-0.142913121758123,
0.162933987761322));
#42663=CARTESIAN_POINT('Ctrl Pts',(0.145073843195134,-0.0391192774524402,
0.170840010960839));
#42664=CARTESIAN_POINT('Ctrl Pts',(0.111955200242363,0.10021362663396,0.178746034160356));
#42665=CARTESIAN_POINT('Ctrl Pts',(-0.0228724430773341,0.148504509032441,
0.186652057359874));
#42666=CARTESIAN_POINT('Ctrl Pts',(-0.136920941586459,0.0618820943336314,
0.194558080559391));
#42667=CARTESIAN_POINT('Ctrl Pts',(-0.12657957626731,-0.0809589322677961,
0.202464103758909));
#42668=CARTESIAN_POINT('Ctrl Pts',(-0.00124326519339163,-0.150250431406802,
0.210370126958426));
#42669=CARTESIAN_POINT('Ctrl Pts',(0.125222526785514,-0.0830424989377088,
0.218276150157944));
#42670=CARTESIAN_POINT('Ctrl Pts',(0.137926224580685,0.0596078385548706,
0.226182173357461));
#42671=CARTESIAN_POINT('Ctrl Pts',(0.0253267796170755,0.148105678753651,
0.234088196556978));
#42672=CARTESIAN_POINT('Ctrl Pts',(-0.110281524552332,0.102052551104597,
0.241994219756496));
#42673=CARTESIAN_POINT('Ctrl Pts',(-0.145701328261229,-0.036713223605009,
0.249900242956013));
#42674=CARTESIAN_POINT('Ctrl Pts',(-0.0487544671752176,-0.142125788564551,
0.25780626615553));
#42675=CARTESIAN_POINT('Ctrl Pts',(0.0924848261822464,-0.11841999312036,
0.265712289355049));
#42676=CARTESIAN_POINT('Ctrl Pts',(0.149703554099366,0.012867934356803,
0.273618312554565));
#42677=CARTESIAN_POINT('Ctrl Pts',(0.0709196772318203,0.132465607709839,
0.281524335754083));
#42678=CARTESIAN_POINT('Ctrl Pts',(-0.0722932700879834,0.131720996597282,
0.289430358953601));
#42679=CARTESIAN_POINT('Ctrl Pts',(-0.149829266052005,0.0113105649246307,
0.297336382153118));
#42680=CARTESIAN_POINT('Ctrl Pts',(-0.0912484505038084,-0.119375282723234,
0.305242405352635));
#42681=CARTESIAN_POINT('Ctrl Pts',(0.0502297085693762,-0.141611137350254,
0.313148428552153));
#42682=CARTESIAN_POINT('Ctrl Pts',(0.14607520885827,-0.0351961816339526,
0.32105445175167));
#42683=CARTESIAN_POINT('Ctrl Pts',(0.109214381507085,0.103193782354472,
0.328960474951188));
#42684=CARTESIAN_POINT('Ctrl Pts',(-0.0268654687609187,0.147834314125149,
0.336866498150705));
#42685=CARTESIAN_POINT('Ctrl Pts',(-0.13853859233343,0.0581704072434516,
0.344772521350223));
#42686=CARTESIAN_POINT('Ctrl Pts',(-0.124352249616671,-0.0843401201082281,
0.35267854454974));
#42687=CARTESIAN_POINT('Ctrl Pts',(0.00280555834318869,-0.150229380238954,
0.360584567749258));
#42688=CARTESIAN_POINT('Ctrl Pts',(0.127414574159504,-0.0796383333348297,
0.368490590948775));
#42689=CARTESIAN_POINT('Ctrl Pts',(0.136270065769409,0.0633025040563021,
0.376396614148293));
#42690=CARTESIAN_POINT('Ctrl Pts',(0.0213270008899901,0.148734316408943,
0.38430263734781));
#42691=CARTESIAN_POINT('Ctrl Pts',(-0.112991206354848,0.0990440565156409,
0.392208660547328));
#42692=CARTESIAN_POINT('Ctrl Pts',(-0.144659222864564,-0.0406256948841215,
0.400114683746845));
#42693=CARTESIAN_POINT('Ctrl Pts',(-0.0449073059326639,-0.143387836717301,
0.408020706946362));
#42694=CARTESIAN_POINT('Ctrl Pts',(0.0956419762819073,-0.115885073316145,
0.41592673014588));
#42695=CARTESIAN_POINT('Ctrl Pts',(0.149302487021736,0.0168968995298395,
0.423832753345397));
#42696=CARTESIAN_POINT('Ctrl Pts',(0.0673247541811015,0.134328386125389,
0.431738776544915));
#42697=CARTESIAN_POINT('Ctrl Pts',(-0.0758161353407861,0.129725292316436,
0.439644799744432));
#42698=CARTESIAN_POINT('Ctrl Pts',(-0.150079622765641,0.007269434305358,
0.447550822943949));
#42699=CARTESIAN_POINT('Ctrl Pts',(-0.0879988547449296,-0.121790555496631,
0.455456846143467));
#42700=CARTESIAN_POINT('Ctrl Pts',(0.0540270657832349,-0.140206326560007,
0.463362869342984));
#42701=CARTESIAN_POINT('Ctrl Pts',(0.146970506475833,-0.0312475290356562,
0.471268892542502));
#42702=CARTESIAN_POINT('Ctrl Pts',(0.106394260027447,0.106099006959581,
0.479174915742019));
#42703=CARTESIAN_POINT('Ctrl Pts',(-0.0308389868837996,0.147056773841187,
0.487080938941536));
#42704=CARTESIAN_POINT('Ctrl Pts',(-0.140055647479839,0.0544164814518564,
0.494986962141054));
#42705=CARTESIAN_POINT('Ctrl Pts',(-0.122034628338338,-0.0876600669114554,
0.502892985340571));
#42706=CARTESIAN_POINT('Ctrl Pts',(0.00685234470650933,-0.150099244557128,
0.51079900854009));
#42707=CARTESIAN_POINT('Ctrl Pts',(0.129514103296199,-0.076176340762594,
0.518705031739606));
#42708=CARTESIAN_POINT('Ctrl Pts',(0.134514958571949,0.066951204357981,
0.526611054939125));
#42709=CARTESIAN_POINT('Ctrl Pts',(0.0173117362067031,0.149254955140882,
0.534517078138641));
#42710=CARTESIAN_POINT('Ctrl Pts',(-0.11561884301137,0.0959636440810236,
0.542423101338159));
#42711=CARTESIAN_POINT('Ctrl Pts',(-0.143512077549549,-0.0445086670437286,
0.550329124537675));
#42712=CARTESIAN_POINT('Ctrl Pts',(-0.0410275366085405,-0.144545768130486,
0.558235147737195));
#42713=CARTESIAN_POINT('Ctrl Pts',(0.098729678853994,-0.113266007071779,
0.56614117093671));
#42714=CARTESIAN_POINT('Ctrl Pts',(0.14879300846003,0.0209135955304358,
0.57404719413623));
#42715=CARTESIAN_POINT('Ctrl Pts',(0.0636809452969333,0.136093626047241,
0.581953217335745));
#42716=CARTESIAN_POINT('Ctrl Pts',(-0.0792839490005986,0.127635391939178,
0.589859240535265));
#42717=CARTESIAN_POINT('Ctrl Pts',(-0.150221003701602,0.00322302520629366,
0.59776526373478));
#42718=CARTESIAN_POINT('Ctrl Pts',(-0.0846853612799296,-0.124117393742718,
0.605671286934299));
#42719=CARTESIAN_POINT('Ctrl Pts',(0.0577851928777687,-0.138699709187424,
0.613577310133815));
#42720=CARTESIAN_POINT('Ctrl Pts',(0.147759085906459,-0.0272761869894916,
0.621483333333334));
#42721=CARTESIAN_POINT('Ctrl Pts',(0.103496883574659,0.108927190980628,
0.62938935653285));
#42722=CARTESIAN_POINT('Ctrl Pts',(-0.0347901122093251,0.146172452729842,
0.637295379732368));
#42723=CARTESIAN_POINT('Ctrl Pts',(-0.141471005454986,0.0506230427785409,
0.645201402931886));
#42724=CARTESIAN_POINT('Ctrl Pts',(-0.119628395306551,-0.0909163620091147,
0.653107426131403));
#42725=CARTESIAN_POINT('Ctrl Pts',(0.0108941554469695,-0.149860118849825,
0.661013449330921));
#42726=CARTESIAN_POINT('Ctrl Pts',(0.131519589685118,-0.0726590350451557,
0.668919472530437));
#42727=CARTESIAN_POINT('Ctrl Pts',(0.132662177406628,0.0705512900682209,
0.676825495729956));
#42728=CARTESIAN_POINT('Ctrl Pts',(0.0132839011303035,0.149667216902378,
0.684731518929473));
#42729=CARTESIAN_POINT('Ctrl Pts',(-0.118162526543641,0.0928135505498801,
0.69263754212899));
#42730=CARTESIAN_POINT('Ctrl Pts',(-0.142260725279696,-0.0483593205820741,
0.700543565328508));
#42731=CARTESIAN_POINT('Ctrl Pts',(-0.0371179763826477,-0.145598742005641,
0.708449588528025));
#42732=CARTESIAN_POINT('Ctrl Pts',(0.101745691861845,-0.110564696145857,
0.716355611727543));
#42733=CARTESIAN_POINT('Ctrl Pts',(0.148175488346884,0.0249151057616852,
0.72426163492706));
#42734=CARTESIAN_POINT('Ctrl Pts',(0.0599908964395442,0.137760045689666,
0.732167658126578));
#42735=CARTESIAN_POINT('Ctrl Pts',(-0.0826941930548661,0.125452813002725,
0.740073681326094));
#42736=CARTESIAN_POINT('Ctrl Pts',(-0.150253306133115,-0.000825724231627113,
0.747979704525614));
#42737=CARTESIAN_POINT('Ctrl Pts',(-0.081310376229644,-0.126354107828757,
0.755885727725129));
#42738=CARTESIAN_POINT('Ctrl Pts',(0.0615013612454227,-0.137092379349209,
0.763791750924648));
#42739=CARTESIAN_POINT('Ctrl Pts',(0.148440374085997,-0.0232850389144764,
0.771697774124165));
#42740=CARTESIAN_POINT('Ctrl Pts',(0.100524356866682,0.111676280340869,
0.779603797323682));
#42741=CARTESIAN_POINT('Ctrl Pts',(-0.0387159774106656,0.145181993819149,
0.7875098205232));
#42742=CARTESIAN_POINT('Ctrl Pts',(-0.142783635380297,0.0467928439952764,
0.795415843722717));
#42743=CARTESIAN_POINT('Ctrl Pts',(-0.117135303735115,-0.0941066376761042,
0.803321866922235));
#42744=CARTESIAN_POINT('Ctrl Pts',(0.0149280671231108,-0.149512182952249,
0.811227890121752));
#42745=CARTESIAN_POINT('Ctrl Pts',(0.133429555455635,-0.0690889583890887,
0.819133913321269));
#42746=CARTESIAN_POINT('Ctrl Pts',(0.13071310873075,0.0741001247218646,
0.827039936520788));
#42747=CARTESIAN_POINT('Ctrl Pts',(0.00924634225633868,0.149970844834382,
0.834945959720303));
#42748=CARTESIAN_POINT('Ctrl Pts',(-0.120620261601548,0.0895959825586721,
0.842851982919823));
#42749=CARTESIAN_POINT('Ctrl Pts',(-0.140906356422368,-0.0521747061680897,
0.850758006119338));
#42750=CARTESIAN_POINT('Ctrl Pts',(-0.0331809289437206,-0.146546284922345,
0.858664029318857));
#42751=CARTESIAN_POINT('Ctrl Pts',(0.104686808927989,-0.107782548984136,
0.866570052518374));
#42752=CARTESIAN_POINT('Ctrl Pts',(0.147452305580495,0.0288974742383162,
0.874476075717892));
#42753=CARTESIAN_POINT('Ctrl Pts',(0.0562536202549592,0.139328430172098,
0.882382098917409));
#42754=CARTESIAN_POINT('Ctrl Pts',(-0.0860374264415029,0.123175350607342,
0.890288122116927));
#42755=CARTESIAN_POINT('Ctrl Pts',(-0.150189737621406,-0.00486667430221375,
0.898194145316444));
#42756=CARTESIAN_POINT('Ctrl Pts',(-0.0778512004163494,-0.128512763786642,
0.906100168515961));
#42757=CARTESIAN_POINT('Ctrl Pts',(0.0651249400548213,-0.135359373728788,
0.914006191715479));
#42758=CARTESIAN_POINT('Ctrl Pts',(0.149106309520794,-0.0193277002139675,
0.921912214914997));
#42759=CARTESIAN_POINT('Ctrl Pts',(0.0972914655469444,0.114449752166959,
0.929818238114513));
#42760=CARTESIAN_POINT('Ctrl Pts',(0.00432320985889779,0.134029312831529,
0.935088920247525));
#42761=CARTESIAN_POINT('Ctrl Pts',(-0.0361033354336585,0.122073089461047,
0.937724261314031));
#42762=CARTESIAN_POINT('Ctrl Pts',(-0.0592743564846289,0.123319225136769,
-0.00549926131403118));
#42763=CARTESIAN_POINT('Ctrl Pts',(-0.10011358044828,0.103689530601369,
-0.00286392024752536));
#42764=CARTESIAN_POINT('Ctrl Pts',(-0.160078034541183,0.0210334216764563,
0.00240676188548625));
#42765=CARTESIAN_POINT('Ctrl Pts',(-0.104882388816361,-0.122944882360947,
0.0103127850850037));
#42766=CARTESIAN_POINT('Ctrl Pts',(0.0457298202147887,-0.154838818620857,
0.0182188082845211));
#42767=CARTESIAN_POINT('Ctrl Pts',(0.154729058131587,-0.0462614617356896,
0.0261248314840386));
#42768=CARTESIAN_POINT('Ctrl Pts',(0.123195923521052,0.104445863960627,
0.034030854683556));
#42769=CARTESIAN_POINT('Ctrl Pts',(-0.0202770029016287,0.160212496691623,
0.0419368778830735));
#42770=CARTESIAN_POINT('Ctrl Pts',(-0.145318780043635,0.0704576601202616,
0.049842901082591));
#42771=CARTESIAN_POINT('Ctrl Pts',(-0.138346646019881,-0.0833214085615725,
0.0577489242821084));
#42772=CARTESIAN_POINT('Ctrl Pts',(-0.00568667862689953,-0.16139684682825,
0.0656549474816259));
#42773=CARTESIAN_POINT('Ctrl Pts',(0.132138073593561,-0.0928506925492821,
0.0735609706811433));
#42774=CARTESIAN_POINT('Ctrl Pts',(0.149918860636037,0.060050582899814,
0.0814669938806607));
#42775=CARTESIAN_POINT('Ctrl Pts',(0.031501040525629,0.158395992498563,
0.0893730170801781));
#42776=CARTESIAN_POINT('Ctrl Pts',(-0.115534617020597,0.112842498042153,
0.0972790402796957));
#42777=CARTESIAN_POINT('Ctrl Pts',(-0.157609558568976,-0.0352264059215207,
0.105185063479213));
#42778=CARTESIAN_POINT('Ctrl Pts',(-0.0564993941266941,-0.151292676454786,
0.113091086678731));
#42779=CARTESIAN_POINT('Ctrl Pts',(0.0959392788869109,-0.129912745106718,
0.120997109878248));
#42780=CARTESIAN_POINT('Ctrl Pts',(0.161219103327847,0.00949029374910116,
0.128903133077765));
#42781=CARTESIAN_POINT('Ctrl Pts',(0.0800346744417541,0.140271571240151,
0.136809156277283));
#42782=CARTESIAN_POINT('Ctrl Pts',(-0.0738596081939327,0.143619019523951,
0.1447151794768));
#42783=CARTESIAN_POINT('Ctrl Pts',(-0.160653955835061,0.0164915309845896,
0.152621202676318));
#42784=CARTESIAN_POINT('Ctrl Pts',(-0.101497482331809,-0.125618171248858,
0.160527225875835));
#42785=CARTESIAN_POINT('Ctrl Pts',(0.0498673689956821,-0.15360634630444,
0.168433249075353));
#42786=CARTESIAN_POINT('Ctrl Pts',(0.15592873994638,-0.0420463090135921,
0.17633927227487));
#42787=CARTESIAN_POINT('Ctrl Pts',(0.120332052420749,0.107711936089485,
0.184245295474388));
#42788=CARTESIAN_POINT('Ctrl Pts',(-0.0245838336532294,0.15961609935871,
0.192151318673905));
#42789=CARTESIAN_POINT('Ctrl Pts',(-0.147165811724802,0.0665123138821622,
0.200057341873423));
#42790=CARTESIAN_POINT('Ctrl Pts',(-0.136050671820698,-0.0870165428714931,
0.20796336507294));
#42791=CARTESIAN_POINT('Ctrl Pts',(-0.00133629033845999,-0.16149265732314,
0.215869388272457));
#42792=CARTESIAN_POINT('Ctrl Pts',(0.134592083483329,-0.0892560087757434,
0.223775411471975));
#42793=CARTESIAN_POINT('Ctrl Pts',(0.148246313261997,0.0640678908897882,
0.231681434671492));
#42794=CARTESIAN_POINT('Ctrl Pts',(0.0272218116347722,0.159187427301401,
0.23958745787101));
#42795=CARTESIAN_POINT('Ctrl Pts',(-0.118533146872527,0.109688454869495,
0.247493481070527));
#42796=CARTESIAN_POINT('Ctrl Pts',(-0.156603175485803,-0.0394602263924212,
0.255399504270045));
#42797=CARTESIAN_POINT('Ctrl Pts',(-0.0524024349666086,-0.152760102280791,
0.263305527469562));
#42798=CARTESIAN_POINT('Ctrl Pts',(0.0994048416526766,-0.127280562126421,
0.27121155066908));
#42799=CARTESIAN_POINT('Ctrl Pts',(0.160904860877029,0.0138307550539624,
0.279117573868597));
#42800=CARTESIAN_POINT('Ctrl Pts',(0.0762261181244613,0.142377115278073,
0.287023597068114));
#42801=CARTESIAN_POINT('Ctrl Pts',(-0.0777024876652646,0.141576789940481,
0.294929620267632));
#42802=CARTESIAN_POINT('Ctrl Pts',(-0.1610399790068,0.0121568581760624,
0.302835643467149));
#42803=CARTESIAN_POINT('Ctrl Pts',(-0.098075956325088,-0.128307329604135,
0.310741666666667));
#42804=CARTESIAN_POINT('Ctrl Pts',(0.0539880587195976,-0.152206943188912,
0.318647689866184));
#42805=CARTESIAN_POINT('Ctrl Pts',(0.157005031045033,-0.037829674407429,
0.326553713065702));
#42806=CARTESIAN_POINT('Ctrl Pts',(0.117386156714116,0.11091507675295,0.334459736265219));
#42807=CARTESIAN_POINT('Ctrl Pts',(-0.0288756305044191,0.158895758288873,
0.342365759464736));
#42808=CARTESIAN_POINT('Ctrl Pts',(-0.14890450036152,0.0625229062928939,
0.350271782664254));
#42809=CARTESIAN_POINT('Ctrl Pts',(-0.133656689346435,-0.0906507221823109,
0.358177805863771));
#42810=CARTESIAN_POINT('Ctrl Pts',(0.0030154793425501,-0.161470031038451,
0.366083829063289));
#42811=CARTESIAN_POINT('Ctrl Pts',(0.136948146970731,-0.0855971324315648,
0.373989852262806));
#42812=CARTESIAN_POINT('Ctrl Pts',(0.146466235262368,0.0680390032796811,
0.381895875462324));
#42813=CARTESIAN_POINT('Ctrl Pts',(0.0229227564554051,0.159863101670492,
0.389801898661841));
#42814=CARTESIAN_POINT('Ctrl Pts',(-0.121445575879827,0.106454854931286,
0.397707921861359));
#42815=CARTESIAN_POINT('Ctrl Pts',(-0.155483096374265,-0.0436654414966204,
0.405613945060876));
#42816=CARTESIAN_POINT('Ctrl Pts',(-0.0482674166083024,-0.154116580980712,
0.413519968260394));
#42817=CARTESIAN_POINT('Ctrl Pts',(0.102798219990352,-0.124555971378489,
0.421425991459911));
#42818=CARTESIAN_POINT('Ctrl Pts',(0.160473784656316,0.018161180504086,
0.429332014659428));
#42819=CARTESIAN_POINT('Ctrl Pts',(0.072362211239822,0.144379272832728,
0.437238037858946));
#42820=CARTESIAN_POINT('Ctrl Pts',(-0.0814889451532045,0.139431760574992,
0.445144061058463));
#42821=CARTESIAN_POINT('Ctrl Pts',(-0.16130906822395,0.00781335702145124,
0.453050084257981));
#42822=CARTESIAN_POINT('Ctrl Pts',(-0.0945832152433237,-0.130903320941292,
0.460956107457498));
#42823=CARTESIAN_POINT('Ctrl Pts',(0.0580695465498112,-0.150697019886669,
0.468862130657016));
#42824=CARTESIAN_POINT('Ctrl Pts',(0.157967317741994,-0.033585570780077,
0.476768153856533));
#42825=CARTESIAN_POINT('Ctrl Pts',(0.114355024573885,0.114037679711269,
0.48467417705605));
#42826=CARTESIAN_POINT('Ctrl Pts',(-0.0331464601757716,0.15806003991218,
0.492580200255568));
#42827=CARTESIAN_POINT('Ctrl Pts',(-0.15053506650769,0.0584880995652034,
0.500486223455085));
#42828=CARTESIAN_POINT('Ctrl Pts',(-0.131165656106781,-0.0942190782023548,
0.508392246654604));
#42829=CARTESIAN_POINT('Ctrl Pts',(0.00736505942237213,-0.161330158181689,
0.51629826985412));
#42830=CARTESIAN_POINT('Ctrl Pts',(0.139204769705438,-0.0818761023161199,
0.524204293053638));
#42831=CARTESIAN_POINT('Ctrl Pts',(0.144579805236504,0.0719607112040898,
0.532110316253155));
#42832=CARTESIAN_POINT('Ctrl Pts',(0.0186070566102303,0.160422696285555,
0.540016339452673));
#42833=CARTESIAN_POINT('Ctrl Pts',(-0.124269820856485,0.103143956020315,
0.547922362652189));
#42834=CARTESIAN_POINT('Ctrl Pts',(-0.154250117916081,-0.047838950261257,
0.555828385851708));
#42835=CARTESIAN_POINT('Ctrl Pts',(-0.0440973503257164,-0.15536115258801,
0.563734409051225));
#42836=CARTESIAN_POINT('Ctrl Pts',(0.106116954510586,-0.121740938080097,
0.571640432250743));
#42837=CARTESIAN_POINT('Ctrl Pts',(0.159926185251717,0.022478418762386,
0.579546455450259));
#42838=CARTESIAN_POINT('Ctrl Pts',(0.06844576072469,0.146276593746376,0.587452478649778));
#42839=CARTESIAN_POINT('Ctrl Pts',(-0.08521623190893,0.137185487054817,
0.595358501849294));
#42840=CARTESIAN_POINT('Ctrl Pts',(-0.161461027741333,0.00346418243402402,
0.603264525048813));
#42841=CARTESIAN_POINT('Ctrl Pts',(-0.0910217954212606,-0.133404260792202,
0.611170548248329));
#42842=CARTESIAN_POINT('Ctrl Pts',(0.0621088689355897,-0.149077672502509,
0.619076571447848));
#42843=CARTESIAN_POINT('Ctrl Pts',(0.158814901250206,-0.0293170800065776,
0.626982594647363));
#42844=CARTESIAN_POINT('Ctrl Pts',(0.111240856992166,0.117077477658479,
0.634888617846883));
#42845=CARTESIAN_POINT('Ctrl Pts',(-0.0373932215478457,0.15710955101933,
0.642794641046398));
#42846=CARTESIAN_POINT('Ctrl Pts',(-0.152056326169508,0.0544108234734799,
0.650700664245917));
#42847=CARTESIAN_POINT('Ctrl Pts',(-0.1285793808941,-0.0977190198892145,
0.658606687445434));
#42848=CARTESIAN_POINT('Ctrl Pts',(0.0117092915870499,-0.161073140311291,
0.666512710644951));
#42849=CARTESIAN_POINT('Ctrl Pts',(0.14136031310814,-0.0780956203460609,
0.67441873384447));
#42850=CARTESIAN_POINT('Ctrl Pts',(0.142588392958853,0.0758301670352254,
0.682324757043986));
#42851=CARTESIAN_POINT('Ctrl Pts',(0.0142778458142493,0.160865804812787,
0.690230780243504));
#42852=CARTESIAN_POINT('Ctrl Pts',(-0.127003831063107,0.0997581622465629,
0.698136803443022));
#42853=CARTESIAN_POINT('Ctrl Pts',(-0.152905135399799,-0.0519777222202838,
0.706042826642539));
#42854=CARTESIAN_POINT('Ctrl Pts',(-0.0398952640892059,-0.156492913392945,
0.713948849842056));
#42855=CARTESIAN_POINT('Ctrl Pts',(0.109358635420242,-0.118837506285601,
0.721854873041575));
#42856=CARTESIAN_POINT('Ctrl Pts',(0.159262460275431,0.0267793350026898,
0.729760896241091));
#42857=CARTESIAN_POINT('Ctrl Pts',(0.0644796104111608,0.148067700325911,
0.737666919440608));
#42858=CARTESIAN_POINT('Ctrl Pts',(-0.0888816415139979,0.134839600464242,
0.745572942640127));
#42859=CARTESIAN_POINT('Ctrl Pts',(-0.161495747145824,-0.000887507604023794,
0.753478965839642));
#42860=CARTESIAN_POINT('Ctrl Pts',(-0.0873942830135206,-0.135808333100311,
0.761384989039162));
#42861=CARTESIAN_POINT('Ctrl Pts',(0.0661030931060867,-0.147350077018504,
0.769291012238677));
#42862=CARTESIAN_POINT('Ctrl Pts',(0.159547165626996,-0.0250273012527367,
0.777197035438197));
#42863=CARTESIAN_POINT('Ctrl Pts',(0.108045916168766,0.120032262825132,
0.785103058637712));
#42864=CARTESIAN_POINT('Ctrl Pts',(-0.0416128327510934,0.156044982751807,
0.793009081837232));
#42865=CARTESIAN_POINT('Ctrl Pts',(-0.153467171334714,0.0502940367608314,
0.800915105036747));
#42866=CARTESIAN_POINT('Ctrl Pts',(-0.125899748103356,-0.101148002356896,
0.808821128236267));
#42867=CARTESIAN_POINT('Ctrl Pts',(0.0160450336537275,-0.160699170718315,
0.816727151435783));
#42868=CARTESIAN_POINT('Ctrl Pts',(0.143413188729122,-0.0742584189441255,
0.824633174635301));
#42869=CARTESIAN_POINT('Ctrl Pts',(0.140493488625962,0.0796445370390336,
0.832539197834818));
#42870=CARTESIAN_POINT('Ctrl Pts',(0.00993818365454583,0.161192151174111,
0.840445221034335));
#42871=CARTESIAN_POINT('Ctrl Pts',(-0.129645461850996,0.0962998453542059,
0.848351244233853));
#42872=CARTESIAN_POINT('Ctrl Pts',(-0.151449428259942,-0.0560785873640905,
0.85625726743337));
#42873=CARTESIAN_POINT('Ctrl Pts',(-0.0356636339569891,-0.157511354552237,
0.864163290632887));
#42874=CARTESIAN_POINT('Ctrl Pts',(0.112519816430259,-0.115847189825252,
0.872069313832405));
#42875=CARTESIAN_POINT('Ctrl Pts',(0.158485166622555,0.0310596772400429,
0.879975337031923));
#42876=CARTESIAN_POINT('Ctrl Pts',(0.0604626990682241,0.149753436435956,
0.88788136023144));
#42877=CARTESIAN_POINT('Ctrl Pts',(-0.0924750264953536,0.132391730925763,
0.895787383430957));
#42878=CARTESIAN_POINT('Ctrl Pts',(-0.161427422231335,-0.00523081470070893,
0.903693406630475));
#42879=CARTESIAN_POINT('Ctrl Pts',(-0.083676280416081,-0.13812850671726,
0.911599429829993));
#42880=CARTESIAN_POINT('Ctrl Pts',(0.0699977998664634,-0.145487402281552,
0.91950545302951));
#42881=CARTESIAN_POINT('Ctrl Pts',(0.160262928516753,-0.020773861600756,
0.927411476229027));
#42882=CARTESIAN_POINT('Ctrl Pts',(0.104571129406605,0.123013254833025,
0.935317499428545));
#42883=CARTESIAN_POINT('Ctrl Pts',(0.0046466864803128,0.144057821902388,
0.940588181561556));
#42884=CARTESIAN_POINT('Ctrl Pts',(-0.0388047044046363,0.131206995015772,
0.943223522628062));
#42885=CARTESIAN_POINT('Ctrl Pts',(-0.0634007094575211,0.131904027763685,
0.));
#42886=CARTESIAN_POINT('Ctrl Pts',(-0.107082934395072,0.110907822426533,
0.00263534106650582));
#42887=CARTESIAN_POINT('Ctrl Pts',(-0.171221782240834,0.0224976522006178,
0.00790602319951745));
#42888=CARTESIAN_POINT('Ctrl Pts',(-0.112183720835187,-0.131503625313535,
0.0158120463990349));
#42889=CARTESIAN_POINT('Ctrl Pts',(0.0489132774597784,-0.165617841075552,
0.0237180695985523));
#42890=CARTESIAN_POINT('Ctrl Pts',(0.165500439667881,-0.0494819289239417,
0.0316240927980698));
#42891=CARTESIAN_POINT('Ctrl Pts',(0.131772142571212,0.111716807532525,
0.0395301159975872));
#42892=CARTESIAN_POINT('Ctrl Pts',(-0.0216885757328939,0.171365604902752,
0.0474361391971047));
#42893=CARTESIAN_POINT('Ctrl Pts',(-0.155435070048499,0.0753625328602259,
0.055342162396622));
#42894=CARTESIAN_POINT('Ctrl Pts',(-0.147977574602665,-0.0891217843448639,
0.0632481855961397));
#42895=CARTESIAN_POINT('Ctrl Pts',(-0.00608255375148451,-0.172632402947666,
0.0711542087956569));
#42896=CARTESIAN_POINT('Ctrl Pts',(0.141336795690974,-0.0993144443967663,
0.0790602319951745));
#42897=CARTESIAN_POINT('Ctrl Pts',(0.160355382818083,0.0642309724640062,
0.0869662551946919));
#42898=CARTESIAN_POINT('Ctrl Pts',(0.03369396879902,0.16942264573115,0.0948722783942093));
#42899=CARTESIAN_POINT('Ctrl Pts',(-0.123577498271253,0.120697968854151,
0.102778301593727));
#42900=CARTESIAN_POINT('Ctrl Pts',(-0.168581464619548,-0.0376786735363742,
0.110684324793244));
#42901=CARTESIAN_POINT('Ctrl Pts',(-0.0604325695628853,-0.161824836098358,
0.118590347992762));
#42902=CARTESIAN_POINT('Ctrl Pts',(0.102618041038548,-0.138956552138631,
0.126496371192279));
#42903=CARTESIAN_POINT('Ctrl Pts',(0.172442285927502,0.0101509555284547,
0.134402394391796));
#42904=CARTESIAN_POINT('Ctrl Pts',(0.085606245967848,0.150036502473934,
0.142308417591314));
#42905=CARTESIAN_POINT('Ctrl Pts',(-0.0790013057495479,0.153616981599344,
0.150214440790831));
#42906=CARTESIAN_POINT('Ctrl Pts',(-0.171837795990946,0.0176395801907167,
0.158120463990349));
#42907=CARTESIAN_POINT('Ctrl Pts',(-0.108563175876194,-0.134363013793315,
0.166026487189866));
#42908=CARTESIAN_POINT('Ctrl Pts',(0.0533388595104543,-0.164299570850757,
0.173932510389384));
#42909=CARTESIAN_POINT('Ctrl Pts',(0.166783636697626,-0.0449733405747439,
0.181838533588901));
#42910=CARTESIAN_POINT('Ctrl Pts',(0.128708904599136,0.11521024554501,0.189744556788419));
#42911=CARTESIAN_POINT('Ctrl Pts',(-0.0262952242291247,0.170727689684979,
0.197650579987936));
#42912=CARTESIAN_POINT('Ctrl Pts',(-0.157410681863144,0.071142533430693,
0.205556603187454));
#42913=CARTESIAN_POINT('Ctrl Pts',(-0.145521767374085,-0.0930741534751901,
0.213462626386971));
#42914=CARTESIAN_POINT('Ctrl Pts',(-0.00142931548352814,-0.172734883239477,
0.221368649586489));
#42915=CARTESIAN_POINT('Ctrl Pts',(0.143961640181145,-0.0954695186137778,
0.229274672786006));
#42916=CARTESIAN_POINT('Ctrl Pts',(0.15856640194331,0.0685279432247057,
0.237180695985524));
#42917=CARTESIAN_POINT('Ctrl Pts',(0.0291168436524689,0.17026917584915,
0.24508671918504));
#42918=CARTESIAN_POINT('Ctrl Pts',(-0.126784769192722,0.117324358634392,
0.252992742384559));
#42919=CARTESIAN_POINT('Ctrl Pts',(-0.167505022710376,-0.0422072291798334,
0.260898765584075));
#42920=CARTESIAN_POINT('Ctrl Pts',(-0.0560504027579997,-0.16339441599703,
0.268804788783594));
#42921=CARTESIAN_POINT('Ctrl Pts',(0.106324857123107,-0.136141131132482,
0.27671081198311));
#42922=CARTESIAN_POINT('Ctrl Pts',(0.172106167654692,0.0147935757511219,
0.284616835182629));
#42923=CARTESIAN_POINT('Ctrl Pts',(0.0815325590171024,0.152288622846307,
0.292522858382145));
#42924=CARTESIAN_POINT('Ctrl Pts',(-0.0831117052425459,0.151432583283679,
0.300428881581663));
#42925=CARTESIAN_POINT('Ctrl Pts',(-0.172250691961594,0.0130031514274941,
0.30833490478118));
#42926=CARTESIAN_POINT('Ctrl Pts',(-0.104903462146368,-0.137239376485036,
0.316240927980698));
#42927=CARTESIAN_POINT('Ctrl Pts',(0.0577464088698189,-0.16280274902757,
0.324146951180215));
#42928=CARTESIAN_POINT('Ctrl Pts',(0.167934853231796,-0.0404631671809053,
0.332052974379733));
#42929=CARTESIAN_POINT('Ctrl Pts',(0.125557931921148,0.118636371151428,
0.33995899757925));
#42930=CARTESIAN_POINT('Ctrl Pts',(-0.0308857922479196,0.169957202452597,
0.347865020778768));
#42931=CARTESIAN_POINT('Ctrl Pts',(-0.15927040838961,0.0668754053423362,
0.355771043978284));
#42932=CARTESIAN_POINT('Ctrl Pts',(-0.142961129076198,-0.0969613242563938,
0.363677067177803));
#42933=CARTESIAN_POINT('Ctrl Pts',(0.0032254003419117,-0.172710681837949,
0.371583090377319));
#42934=CARTESIAN_POINT('Ctrl Pts',(0.146481719781958,-0.0915559315282998,
0.379489113576838));
#42935=CARTESIAN_POINT('Ctrl Pts',(0.156662404755327,0.0727755025030601,
0.387395136776354));
#42936=CARTESIAN_POINT('Ctrl Pts',(0.0245185120208197,0.170991886932041,
0.395301159975873));
#42937=CARTESIAN_POINT('Ctrl Pts',(-0.129899945404805,0.113865653346931,
0.403207183175389));
#42938=CARTESIAN_POINT('Ctrl Pts',(-0.166306969883967,-0.0467051881091194,
0.411113206374907));
#42939=CARTESIAN_POINT('Ctrl Pts',(-0.0516275272839405,-0.164845325244123,
0.419019229574424));
#42940=CARTESIAN_POINT('Ctrl Pts',(0.109954463698797,-0.133226869440833,
0.426925252773942));
#42941=CARTESIAN_POINT('Ctrl Pts',(0.171645082290897,0.0194254614783324,
0.434831275973459));
#42942=CARTESIAN_POINT('Ctrl Pts',(0.0773996682985425,0.154430159540067,
0.442737299172977));
#42943=CARTESIAN_POINT('Ctrl Pts',(-0.0871617549656229,0.149138228833548,
0.450643322372495));
#42944=CARTESIAN_POINT('Ctrl Pts',(-0.172538513682259,0.00835727973754467,
0.458549345572012));
#42945=CARTESIAN_POINT('Ctrl Pts',(-0.101167575741718,-0.140016086385953,
0.466455368771529));
#42946=CARTESIAN_POINT('Ctrl Pts',(0.0621120273163875,-0.161187713213332,
0.474361391971047));
#42947=CARTESIAN_POINT('Ctrl Pts',(0.168964129008155,-0.0359236125244978,
0.482267415170563));
#42948=CARTESIAN_POINT('Ctrl Pts',(0.122315789120323,0.121976352462958,
0.490173438370083));
#42949=CARTESIAN_POINT('Ctrl Pts',(-0.0354539334677437,0.169063305983172,
0.498079461569598));
#42950=CARTESIAN_POINT('Ctrl Pts',(-0.161014485535541,0.0625597176785504,
0.505985484769117));
#42951=CARTESIAN_POINT('Ctrl Pts',(-0.140296683875224,-0.100778089493254,
0.513891507968634));
#42952=CARTESIAN_POINT('Ctrl Pts',(0.00787777413823514,-0.17256107180625,
0.521797531168151));
#42953=CARTESIAN_POINT('Ctrl Pts',(0.148895436114678,-0.0875758638696457,
0.529703554367669));
#42954=CARTESIAN_POINT('Ctrl Pts',(0.154644651901059,0.0769702180501986,
0.537609577567186));
#42955=CARTESIAN_POINT('Ctrl Pts',(0.0199023770137573,0.171590437430228,
0.545515600766704));
#42956=CARTESIAN_POINT('Ctrl Pts',(-0.132920798701601,0.110324267959608,
0.553421623966221));
#42957=CARTESIAN_POINT('Ctrl Pts',(-0.164988158282613,-0.0511692334787857,
0.561327647165738));
#42958=CARTESIAN_POINT('Ctrl Pts',(-0.0471671640428923,-0.166176537045534,
0.569233670365257));
#42959=CARTESIAN_POINT('Ctrl Pts',(0.113504230167178,-0.130215869088414,
0.577139693564773));
#42960=CARTESIAN_POINT('Ctrl Pts',(0.171059362043405,0.0240432419943362,
0.585045716764291));
#42961=CARTESIAN_POINT('Ctrl Pts',(0.0732105761524465,0.156459561445511,
0.592951739963808));
#42962=CARTESIAN_POINT('Ctrl Pts',(-0.0911485148172611,0.146735582170455,
0.600857763163326));
#42963=CARTESIAN_POINT('Ctrl Pts',(-0.172701051781065,0.00370533966175465,
0.608763786362843));
#42964=CARTESIAN_POINT('Ctrl Pts',(-0.0973582295625918,-0.142691127841686,
0.616669809562361));
#42965=CARTESIAN_POINT('Ctrl Pts',(0.0664325449934107,-0.159455635817593,
0.624575832761878));
#42966=CARTESIAN_POINT('Ctrl Pts',(0.169870716593952,-0.0313579730236637,
0.632481855961396));
#42967=CARTESIAN_POINT('Ctrl Pts',(0.118984830409674,0.12522776433633,0.640387879160913));
#42968=CARTESIAN_POINT('Ctrl Pts',(-0.0399963308863663,0.168046649308817,
0.648293902360431));
#42969=CARTESIAN_POINT('Ctrl Pts',(-0.162641646884031,0.0581986041684188,
0.656199925559947));
#42970=CARTESIAN_POINT('Ctrl Pts',(-0.137530366481649,-0.104521677769314,
0.664105948759466));
#42971=CARTESIAN_POINT('Ctrl Pts',(0.0125244277271302,-0.172286161772757,
0.672011971958982));
#42972=CARTESIAN_POINT('Ctrl Pts',(0.151201036531162,-0.0835322056469662,
0.679917995158501));
#42973=CARTESIAN_POINT('Ctrl Pts',(0.152514608511077,0.08110904400223,0.687824018358017));
#42974=CARTESIAN_POINT('Ctrl Pts',(0.015271790498195,0.172064392723197,
0.695730041557536));
#42975=CARTESIAN_POINT('Ctrl Pts',(-0.135845135582574,0.106702773943246,
0.703636064757053));
#42976=CARTESIAN_POINT('Ctrl Pts',(-0.163549545519903,-0.0555961238584937,
0.71154208795657));
#42977=CARTESIAN_POINT('Ctrl Pts',(-0.042672551795764,-0.167387084780248,
0.719448111156087));
#42978=CARTESIAN_POINT('Ctrl Pts',(0.116971578978639,-0.127110316425345,
0.727354134355605));
#42979=CARTESIAN_POINT('Ctrl Pts',(0.170349432203978,0.0286435642436946,
0.735260157555123));
#42980=CARTESIAN_POINT('Ctrl Pts',(0.0689683243827774,0.158375354962157,
0.74316618075464));
#42981=CARTESIAN_POINT('Ctrl Pts',(-0.0950690899731296,0.144226387925758,
0.751072203954158));
#42982=CARTESIAN_POINT('Ctrl Pts',(-0.172738188158534,-0.000949290976420475,
0.758978227153675));
#42983=CARTESIAN_POINT('Ctrl Pts',(-0.0934781897973971,-0.145262558371866,
0.766884250353192));
#42984=CARTESIAN_POINT('Ctrl Pts',(0.0707048249667505,-0.157607774687799,
0.77479027355271));
#42985=CARTESIAN_POINT('Ctrl Pts',(0.170653957167994,-0.026769563590997,
0.782696296752227));
#42986=CARTESIAN_POINT('Ctrl Pts',(0.115567475470849,0.128388245309395,
0.790602319951745));
#42987=CARTESIAN_POINT('Ctrl Pts',(-0.044509688091521,0.166907971684466,
0.798508343151262));
#42988=CARTESIAN_POINT('Ctrl Pts',(-0.164150707289131,0.0537952295263864,
0.806414366350779));
#42989=CARTESIAN_POINT('Ctrl Pts',(-0.134664192471597,-0.108189367037688,
0.814320389550297));
#42990=CARTESIAN_POINT('Ctrl Pts',(0.0171620001843438,-0.171886158484381,
0.822226412749814));
#42991=CARTESIAN_POINT('Ctrl Pts',(0.153396822002609,-0.0794278794991626,
0.830132435949332));
#42992=CARTESIAN_POINT('Ctrl Pts',(0.150273868521174,0.0851889493562029,
0.838038459148849));
#42993=CARTESIAN_POINT('Ctrl Pts',(0.010630025052753,0.17241345751384,0.845944482348367));
#42994=CARTESIAN_POINT('Ctrl Pts',(-0.138670662100443,0.10300370814974,
0.853850505547884));
#42995=CARTESIAN_POINT('Ctrl Pts',(-0.161992500097515,-0.0599824685600915,
0.861756528747401));
#42996=CARTESIAN_POINT('Ctrl Pts',(-0.0381463389702577,-0.16847642418213,
0.869662551946919));
#42997=CARTESIAN_POINT('Ctrl Pts',(0.120352823932529,-0.123911830666367,
0.877568575146436));
#42998=CARTESIAN_POINT('Ctrl Pts',(0.169518027664615,0.0332218802417698,
0.885474598345955));
#42999=CARTESIAN_POINT('Ctrl Pts',(0.064671777881489,0.160178442699814,
0.89338062154547));
#43000=CARTESIAN_POINT('Ctrl Pts',(-0.0989126265492044,0.141608111244184,
0.90128664474499));
#43001=CARTESIAN_POINT('Ctrl Pts',(-0.172665106841263,-0.00559495509920419,
0.909192667944505));
#43002=CARTESIAN_POINT('Ctrl Pts',(-0.0895013604158129,-0.147744249647878,
0.917098691144024));
#43003=CARTESIAN_POINT('Ctrl Pts',(0.0748706596781056,-0.155615430834315,
0.925004714343541));
#43004=CARTESIAN_POINT('Ctrl Pts',(0.171419547512711,-0.0222200229875446,
0.932910737543058));
#43005=CARTESIAN_POINT('Ctrl Pts',(0.111850793266265,0.131576757499091,
0.940816760742576));
#43006=CARTESIAN_POINT('Ctrl Pts',(0.00497016310172783,0.154086330973247,
0.946087442875587));
#43007=CARTESIAN_POINT('Ctrl Pts',(-0.0415060733756141,0.140340900570497,
0.948722783942093));
#43008=CARTESIAN_POINT('Ctrl Pts',(-0.146190615322833,-9.92620605964336E-5,
0.858934495415709));
#43009=CARTESIAN_POINT('Ctrl Pts',(-0.146299982018485,-0.0174419138812775,
0.85987517319294));
#43010=CARTESIAN_POINT('Ctrl Pts',(-0.143444813888727,-0.0347497500736094,
0.860815850970171));
#43011=CARTESIAN_POINT('Ctrl Pts',(-0.13746450024346,-0.0509004317121259,
0.861756528747401));
#43012=CARTESIAN_POINT('Ctrl Pts',(-0.120710446388429,-0.0961471204341042,
0.864391869813907));
#43013=CARTESIAN_POINT('Ctrl Pts',(-0.0794283926793434,-0.132311772308117,
0.867027210880413));
#43014=CARTESIAN_POINT('Ctrl Pts',(-0.032370838674336,-0.142966665992496,
0.869662551946919));
#43015=CARTESIAN_POINT('Ctrl Pts',(0.014686715330672,-0.153621559676876,
0.872297893013425));
#43016=CARTESIAN_POINT('Ctrl Pts',(0.0675197696316001,-0.138766695171622,
0.874933234079931));
#43017=CARTESIAN_POINT('Ctrl Pts',(0.10213049740408,-0.105150311100971,
0.877568575146437));
#43018=CARTESIAN_POINT('Ctrl Pts',(0.136741225176558,-0.0715339270303214,
0.880203916212942));
#43019=CARTESIAN_POINT('Ctrl Pts',(0.153129626420586,-0.019156023394278,
0.882839257279448));
#43020=CARTESIAN_POINT('Ctrl Pts',(0.143849452078747,0.028192355500085,
0.885474598345954));
#43021=CARTESIAN_POINT('Ctrl Pts',(0.134569277736908,0.0755407343944486,
0.88810993941246));
#43022=CARTESIAN_POINT('Ctrl Pts',(0.0996205278091978,0.117859588547133,
0.890745280478965));
#43023=CARTESIAN_POINT('Ctrl Pts',(0.0548820854402278,0.135923960380868,
0.893380621545471));
#43024=CARTESIAN_POINT('Ctrl Pts',(0.0101436430712571,0.153988332214605,
0.896015962611977));
#43025=CARTESIAN_POINT('Ctrl Pts',(-0.0443844917389754,0.147798221729394,
0.898651303678484));
#43026=CARTESIAN_POINT('Ctrl Pts',(-0.0839406391927675,0.120169322096223,
0.901286644744989));
#43027=CARTESIAN_POINT('Ctrl Pts',(-0.0957651970765149,0.111910188080244,
0.902074429829993));
#43028=CARTESIAN_POINT('Ctrl Pts',(-0.106251862209464,0.10173528965009,
0.902862214914997));
#43029=CARTESIAN_POINT('Ctrl Pts',(-0.115101970897794,0.0902398078595192,
0.903650000000001));
#43030=CARTESIAN_POINT('Ctrl Pts',(-0.0686121729278153,-0.0959472995825293,
-5.42101086242752E-19));
#43031=CARTESIAN_POINT('Ctrl Pts',(-0.0716149353959019,-0.0943161956304311,
-1.06730581618305E-18));
#43032=CARTESIAN_POINT('Ctrl Pts',(-0.0745354620527207,-0.0925505885939475,
1.1783117230653E-17));
#43033=CARTESIAN_POINT('Ctrl Pts',(-0.0773634912799965,-0.0906526488910235,
6.72205346941013E-18));
#43034=CARTESIAN_POINT('Ctrl Pts',(-0.0815539383946836,-0.0878403667988651,
-2.29049000805066E-18));
#43035=CARTESIAN_POINT('Ctrl Pts',(-0.0855414709026766,-0.0847378275400617,
-2.5182094749946E-17));
#43036=CARTESIAN_POINT('Ctrl Pts',(-0.089317923041959,-0.0813786482814292,
-3.31765864780564E-17));
#43037=CARTESIAN_POINT('Ctrl Pts',(-0.0927862368571965,-0.0782935601084891,
-4.05187703807701E-17));
#43038=CARTESIAN_POINT('Ctrl Pts',(-0.0960787339139733,-0.0749884873641515,
4.97114916498215E-19));
#43039=CARTESIAN_POINT('Ctrl Pts',(-0.0991698906024268,-0.0715076841230725,
-8.67361737988404E-19));
#43040=CARTESIAN_POINT('Ctrl Pts',(-0.103663297594998,-0.0664478740909087,
-2.85080986385392E-18));
#43041=CARTESIAN_POINT('Ctrl Pts',(-0.107740134647113,-0.0610110581939007,
-1.51788304147971E-17));
#43042=CARTESIAN_POINT('Ctrl Pts',(-0.111378619976329,-0.0552695407791115,
-1.51788304147971E-17));
#43043=CARTESIAN_POINT('Ctrl Pts',(-0.113566215904755,-0.0518175218802795,
-1.51788304147971E-17));
#43044=CARTESIAN_POINT('Ctrl Pts',(-0.115595886809481,-0.0482525855570875,
-3.79982201238933E-17));
#43045=CARTESIAN_POINT('Ctrl Pts',(-0.117451481229743,-0.0446106777439056,
-3.20923843055709E-17));
#43046=CARTESIAN_POINT('Ctrl Pts',(-0.121759272594108,-0.0361559319998316,
-1.83818944163349E-17));
#43047=CARTESIAN_POINT('Ctrl Pts',(-0.125146870804877,-0.027267170883122,
-1.0758832179559E-17));
#43048=CARTESIAN_POINT('Ctrl Pts',(-0.127551512867323,-0.0181239349359946,
-1.21430643318376E-17));
#43049=CARTESIAN_POINT('Ctrl Pts',(-0.128525246808636,-0.0144214798745123,
-1.27035942545157E-17));
#43050=CARTESIAN_POINT('Ctrl Pts',(-0.129337364222068,-0.0106768832185224,
-3.87407706984377E-19));
#43051=CARTESIAN_POINT('Ctrl Pts',(-0.129981634111732,-0.00690081199580598,
2.60208521396521E-18));
#43052=CARTESIAN_POINT('Ctrl Pts',(-0.130488787940845,-0.00392837915310221,
4.95534245334234E-18));
#43053=CARTESIAN_POINT('Ctrl Pts',(-0.130891436982594,-0.000937368841373321,
-5.77147351242312E-18));
#43054=CARTESIAN_POINT('Ctrl Pts',(-0.131185766414779,0.00205408358364406,
-5.20417042793042E-18));
#43055=CARTESIAN_POINT('Ctrl Pts',(-0.131681056523625,0.00708802390756766,
-4.24952717536476E-18));
#43056=CARTESIAN_POINT('Ctrl Pts',(-0.131871567589099,0.0121324651245783,
-2.3640808795201E-17));
#43057=CARTESIAN_POINT('Ctrl Pts',(-0.131747571113314,0.0171617682916428,
-1.73472347597681E-17));
#43058=CARTESIAN_POINT('Ctrl Pts',(-0.131588224313727,0.0236248823338087,
-9.16854279395534E-18));
#43059=CARTESIAN_POINT('Ctrl Pts',(-0.130910003388584,0.0300630957896326,
1.9164721863282E-18));
#43060=CARTESIAN_POINT('Ctrl Pts',(-0.129749448943416,0.0364359420359482,
1.73472347597681E-18));
#43061=CARTESIAN_POINT('Ctrl Pts',(-0.129188162258574,0.039518084159911,
1.64682313529719E-18));
#43062=CARTESIAN_POINT('Ctrl Pts',(-0.128513877700937,0.0425849598402651,
-2.5119873647686E-17));
#43063=CARTESIAN_POINT('Ctrl Pts',(-0.127729776371406,0.0456319959092621,
-2.60208521396521E-17));
#43064=CARTESIAN_POINT('Ctrl Pts',(-0.126905460209866,0.0488353077541379,
-2.69680398361349E-17));
#43065=CARTESIAN_POINT('Ctrl Pts',(-0.125961589290349,0.0520090496451376,
-6.80234412585701E-18));
#43066=CARTESIAN_POINT('Ctrl Pts',(-0.124905367512152,0.0551421622546814,
-8.67361737988404E-18));
#43067=CARTESIAN_POINT('Ctrl Pts',(-0.122242239861443,0.0630419035736882,
-1.33917927173935E-17));
#43068=CARTESIAN_POINT('Ctrl Pts',(-0.118863777535182,0.0706951392673794,
8.60987302363936E-19));
#43069=CARTESIAN_POINT('Ctrl Pts',(-0.114842094503769,0.0780194918792452,
1.73472347597681E-18));
#43070=CARTESIAN_POINT('Ctrl Pts',(-0.112169428435535,0.0828869935059547,
2.31537714896978E-18));
#43071=CARTESIAN_POINT('Ctrl Pts',(-0.109212095329563,0.0876093199712314,
1.58690079118504E-17));
#43072=CARTESIAN_POINT('Ctrl Pts',(-0.105985186696901,0.0921609434032714,
1.90819582357449E-17));
#43073=CARTESIAN_POINT('Ctrl Pts',(-0.104153982707569,0.0947438956760198,
2.09052411731938E-17));
#43074=CARTESIAN_POINT('Ctrl Pts',(-0.102235981964729,0.0972711925776025,
1.37027400976072E-17));
#43075=CARTESIAN_POINT('Ctrl Pts',(-0.10024275281245,0.0997277902811201,
1.21430643318376E-17));
#43076=CARTESIAN_POINT('Ctrl Pts',(-0.0937332858648147,0.107750521403832,
7.04949150570437E-18));
#43077=CARTESIAN_POINT('Ctrl Pts',(-0.0864043214638765,0.115051138974542,
-2.08047340785725E-18));
#43078=CARTESIAN_POINT('Ctrl Pts',(-0.0783638198438572,0.121477900017692,
0.));
#43079=CARTESIAN_POINT('Ctrl Pts',(-0.0736196559743728,0.125269903176152,
1.22754863308587E-18));
#43080=CARTESIAN_POINT('Ctrl Pts',(-0.0686268317545984,0.128757413629593,
6.34938948147863E-19));
#43081=CARTESIAN_POINT('Ctrl Pts',(-0.0634007094575211,0.131904027763685,
0.));
#43082=CARTESIAN_POINT('Origin',(0.,0.,0.));
#43083=CARTESIAN_POINT('Origin',(-0.0577350269189626,-0.1,-0.3));
#43084=CARTESIAN_POINT('',(-0.0577350269189626,-0.1,-0.3));
#43085=CARTESIAN_POINT('',(0.0577350269189626,-0.1,-0.3));
#43086=CARTESIAN_POINT('',(-0.0288675134594813,-0.1,-0.3));
#43087=CARTESIAN_POINT('',(-0.0577350269189626,-0.1,-0.1));
#43088=CARTESIAN_POINT('',(-0.0577350269189626,-0.1,-0.3));
#43089=CARTESIAN_POINT('',(0.0577350269189626,-0.1,-0.1));
#43090=CARTESIAN_POINT('',(-0.0577350269189626,-0.1,-0.1));
#43091=CARTESIAN_POINT('',(0.0577350269189626,-0.1,-0.3));
#43092=CARTESIAN_POINT('Origin',(-0.115470053837925,1.41410031829988E-17,
-0.3));
#43093=CARTESIAN_POINT('',(-0.115470053837925,1.41410031829988E-17,-0.3));
#43094=CARTESIAN_POINT('',(-0.101036297108185,-0.025,-0.3));
#43095=CARTESIAN_POINT('',(-0.115470053837925,1.38777878078145E-17,-0.1));
#43096=CARTESIAN_POINT('',(-0.115470053837925,1.41410031829988E-17,-0.3));
#43097=CARTESIAN_POINT('',(-0.115470053837925,1.41410031829988E-17,-0.1));
#43098=CARTESIAN_POINT('Origin',(-0.0577350269189626,0.1,-0.3));
#43099=CARTESIAN_POINT('',(-0.0577350269189626,0.1,-0.3));
#43100=CARTESIAN_POINT('',(-0.0721687836487032,0.075,-0.3));
#43101=CARTESIAN_POINT('',(-0.0577350269189626,0.1,-0.1));
#43102=CARTESIAN_POINT('',(-0.0577350269189626,0.1,-0.3));
#43103=CARTESIAN_POINT('',(-0.0577350269189626,0.1,-0.1));
#43104=CARTESIAN_POINT('Origin',(0.0577350269189626,0.1,-0.3));
#43105=CARTESIAN_POINT('',(0.0577350269189626,0.1,-0.3));
#43106=CARTESIAN_POINT('',(0.0288675134594813,0.1,-0.3));
#43107=CARTESIAN_POINT('',(0.0577350269189626,0.1,-0.1));
#43108=CARTESIAN_POINT('',(0.0577350269189626,0.1,-0.3));
#43109=CARTESIAN_POINT('',(0.0577350269189626,0.1,-0.1));
#43110=CARTESIAN_POINT('Origin',(0.115470053837925,0.,-0.3));
#43111=CARTESIAN_POINT('',(0.115470053837925,0.,-0.3));
#43112=CARTESIAN_POINT('',(0.101036297108185,0.025,-0.3));
#43113=CARTESIAN_POINT('',(0.115470053837925,0.,-0.1));
#43114=CARTESIAN_POINT('',(0.115470053837925,0.,-0.3));
#43115=CARTESIAN_POINT('',(0.115470053837925,0.,-0.1));
#43116=CARTESIAN_POINT('Origin',(0.0577350269189626,-0.1,-0.3));
#43117=CARTESIAN_POINT('',(0.0721687836487032,-0.075,-0.3));
#43118=CARTESIAN_POINT('',(0.0577350269189626,-0.1,-0.1));
#43119=CARTESIAN_POINT('Origin',(0.,0.,-0.1));
#43120=CARTESIAN_POINT('Origin',(0.,0.,0.));
#43121=CARTESIAN_POINT('',(-0.3,-3.67394039744206E-17,0.));
#43122=CARTESIAN_POINT('Origin',(0.,0.,0.));
#43123=CARTESIAN_POINT('Origin',(0.,0.,-0.3));
#43124=CARTESIAN_POINT('',(-0.3,-3.67394039744206E-17,-0.3));
#43125=CARTESIAN_POINT('',(-0.3,-3.67394039744206E-17,-0.3));
#43126=CARTESIAN_POINT('Origin',(0.,0.,-0.3));
#43127=CARTESIAN_POINT('Origin',(0.,0.,-0.3));
#43128=CARTESIAN_POINT('Origin',(0.,0.,1.));
#43959=UNCERTAINTY_MEASURE_WITH_UNIT(LENGTH_MEASURE(0.001),#43981,
'DISTANCE_ACCURACY_VALUE',
'Maximum model space distance between geometric entities at asserted c
onnectivities');
#43961=UNCERTAINTY_MEASURE_WITH_UNIT(LENGTH_MEASURE(0.001),#43981,
'DISTANCE_ACCURACY_VALUE',
'Maximum model space distance between geometric entities at asserted c
onnectivities');
#43978=(
GEOMETRIC_REPRESENTATION_CONTEXT(3)
GLOBAL_UNCERTAINTY_ASSIGNED_CONTEXT((#43959))
GLOBAL_UNIT_ASSIGNED_CONTEXT((#43981,#43983,#43984))
REPRESENTATION_CONTEXT('','3D')
);
#43980=(
GEOMETRIC_REPRESENTATION_CONTEXT(3)
GLOBAL_UNCERTAINTY_ASSIGNED_CONTEXT((#43961))
GLOBAL_UNIT_ASSIGNED_CONTEXT((#43981,#43983,#43984))
REPRESENTATION_CONTEXT('','3D')
);
#43981=(
LENGTH_UNIT()
NAMED_UNIT(*)
SI_UNIT(.CENTI.,.METRE.)
);
#43983=(
NAMED_UNIT(*)
PLANE_ANGLE_UNIT()
SI_UNIT($,.RADIAN.)
);
#43984=(
NAMED_UNIT(*)
SI_UNIT($,.STERADIAN.)
SOLID_ANGLE_UNIT()
);
#44001=SHAPE_DEFINITION_REPRESENTATION(#44019,#44071);
#44019=PRODUCT_DEFINITION_SHAPE('',$,#44090);
#44071=SHAPE_REPRESENTATION('',(#12149),#43978);
#44073=PRODUCT_DEFINITION_CONTEXT('part definition',#44129,'design');
#44090=PRODUCT_DEFINITION('Socket head cap screw M3x10',
'Socket head cap screw M3x10',#44108,#44073);
#44108=PRODUCT_DEFINITION_FORMATION('',$,#44147);
#44129=APPLICATION_CONTEXT(
'Core Data for Automotive Mechanical Design Process');
#44130=PRODUCT_CONTEXT('part definition',#44129,'mechanical');
#44147=PRODUCT('Socket head cap screw M3x10',
'Socket head cap screw M3x10',$,(#44130));
#44160=PRESENTATION_STYLE_ASSIGNMENT((#44172));
#44172=SURFACE_STYLE_USAGE(.BOTH.,#44184);
#44184=SURFACE_SIDE_STYLE('',(#44196));
#44196=SURFACE_STYLE_FILL_AREA(#44208);
#44208=FILL_AREA_STYLE('Dark gray',(#44220));
#44220=FILL_AREA_STYLE_COLOUR('Dark gray',#44232);
#44232=COLOUR_RGB('Dark gray',0.250980392156863,0.282352941176471,0.32156862745098);
ENDSEC;
END-ISO-10303-21;
